ISO-10303-21;
HEADER;
FILE_DESCRIPTION (('STEP AP214'),
    '1' );
FILE_NAME ('Speed Governor Worm Gear Train.step',
    '2026-10-09T09:51:18',
    ( '' ),
    ( '' ),
    'SwSTEP 2.0',
    'SolidWorks 2026',
    '' );
FILE_SCHEMA (( 'AUTOMOTIVE_DESIGN' ));
ENDSEC;

DATA;
#5=ADVANCED_FACE ( 'NONE', ( #2758, #44164 ), #246, .T. ) ;
#29=CARTESIAN_POINT ( 'NONE',  ( 18.07590614458695200, 1.644079634528023526, 49.42952874619304282 ) ) ;
#31=CARTESIAN_POINT ( 'NONE',  ( -20.58659385650551599, -9.302874398569244363, 51.68646062012417985 ) ) ;
#38=CARTESIAN_POINT ( 'NONE',  ( -22.35534385541302527, -8.623186033802584305, 49.24843789510462955 ) ) ;
#66=CARTESIAN_POINT ( 'NONE',  ( -21.34284385541298334, -7.587656875400150547, 49.25157356644804452 ) ) ;
#71=CARTESIAN_POINT ( 'NONE',  ( -14.25534385541304339, -8.623186033802571870, 49.24843789510467218 ) ) ;
#83=EDGE_LOOP ( 'NONE', ( #31315, #30572, #42863, #38063 ) ) ;
#94=CARTESIAN_POINT ( 'NONE',  ( 10.57590614458695377, 0.6407533398237040823, 50.52649563099625851 ) ) ;
#97=ORIENTED_EDGE ( 'NONE', *, *, #12541, .T. ) ;
#100=( BOUNDED_CURVE ( )  B_SPLINE_CURVE ( 2, ( #3305, #14589, #15340, #3801, #41715, #30399, #23018, #10693, #7264 ),
 .UNSPECIFIED., .F., .F. ) 
 B_SPLINE_CURVE_WITH_KNOTS ( ( 3, 2, 2, 2, 3 ),
 ( 0.08333333333333348136, 0.09375000000000012490, 0.1041666666666667684, 0.1145833333333334120, 0.1250000000000000555 ),
 .UNSPECIFIED. ) 
 CURVE ( )  GEOMETRIC_REPRESENTATION_ITEM ( )  RATIONAL_B_SPLINE_CURVE ( ( 0.9999999999999988898, 0.9238795325112878487, 1.000000000000000000, 0.9238795325112867385, 1.000000000000000000, 0.9238795325112867385, 1.000000000000000000, 0.9238795325112862944, 1.000000000000000444 ) ) 
 REPRESENTATION_ITEM ( '' )  );
#110=CARTESIAN_POINT ( 'NONE',  ( -20.49909385650551741, -8.114302828567740988, 52.18300498402516041 ) ) ;
#126=CARTESIAN_POINT ( 'NONE',  ( -15.38034385650552061, -6.424090610841176385, 49.80797279389977916 ) ) ;
#136=CARTESIAN_POINT ( 'NONE',  ( -16.53659385650551528, -6.915538690918075382, 49.31353937987644542 ) ) ;
#142=CARTESIAN_POINT ( 'NONE',  ( -14.45534385650551989, -7.417179338643134834, 52.18511593390279302 ) ) ;
#169=DIRECTION ( 'NONE',  ( 1.000000000000000000, -4.164305804376849172E-17, 1.614929280266638808E-16 ) ) ;
#172=DIRECTION ( 'NONE',  ( 1.000000000000000000, 1.669677910507523057E-21, 6.493791346278465266E-22 ) ) ;
#187=ORIENTED_EDGE ( 'NONE', *, *, #3019, .F. ) ;
#200=VECTOR ( 'NONE', #37343, 1000.000000000000000 ) ;
#206=CARTESIAN_POINT ( 'NONE',  ( -15.09909385650551705, -8.114302828567740988, 52.18300498402516041 ) ) ;
#209=CARTESIAN_POINT ( 'NONE',  ( -13.42364920204782841, -9.064338107659910548, 49.69363550579117117 ) ) ;
#224=ORIENTED_EDGE ( 'NONE', *, *, #25555, .F. ) ;
#244=CARTESIAN_POINT ( 'NONE',  ( -19.18034385759799321, -9.360768649639298999, 51.01397948905921709 ) ) ;
#246=PLANE ( 'NONE',  #37799 ) ;
#247=CARTESIAN_POINT ( 'NONE',  ( -22.58034385650552167, -6.424090610841174609, 49.80797279389977916 ) ) ;
#284=CARTESIAN_POINT ( 'NONE',  ( -20.98034385650551314, -6.424090610841176385, 49.80797279389978627 ) ) ;
#286=ADVANCED_FACE ( 'NONE', ( #25686 ), #14968, .F. ) ;
#291=CARTESIAN_POINT ( 'NONE',  ( -22.18659385541302242, -7.222650657624079429, 49.61879703869474412 ) ) ;
#294=CARTESIAN_POINT ( 'NONE',  ( -36.42409385541304800, -9.359200813967566646, 50.49621490985803263 ) ) ;
#315=CARTESIAN_POINT ( 'NONE',  ( -13.69284385541304161, -8.630756214087126565, 51.74842643355248129 ) ) ;
#326=ORIENTED_EDGE ( 'NONE', *, *, #4929, .T. ) ;
#333=CARTESIAN_POINT ( 'NONE',  ( -18.19284385541303450, -8.630756214087130118, 51.74842643355250260 ) ) ;
#343=CARTESIAN_POINT ( 'NONE',  ( 6.575906144586949331, -6.109215713985405749, 50.50605614422795497 ) ) ;
#349=CARTESIAN_POINT ( 'NONE',  ( -18.19284385650551528, -7.406986770994972602, 48.81910596585309747 ) ) ;
#353=DIRECTION ( 'NONE',  ( 1.000000000000000000, -4.164305804376849788E-17, 1.614929280266638808E-16 ) ) ;
#365=CARTESIAN_POINT ( 'NONE',  ( -15.09909385650551705, -8.114302828567740988, 52.18300498402516041 ) ) ;
#372=CARTESIAN_POINT ( 'NONE',  ( -13.33034385650551812, -9.794322478646142471, 51.19202720610083901 ) ) ;
#375=CARTESIAN_POINT ( 'NONE',  ( -16.25534385650551528, -7.417179338643134834, 52.18511593390279302 ) ) ;
#419=CARTESIAN_POINT ( 'NONE',  ( -13.17364477763805652, -9.395196358873663556, 49.41429196092195042 ) ) ;
#428=CARTESIAN_POINT ( 'NONE',  ( -19.03659385541296345, -8.995762431863310482, 51.38120296130595221 ) ) ;
#444=CARTESIAN_POINT ( 'NONE',  ( -15.15534385650552096, -7.417179338643134834, 52.18511593390279302 ) ) ;
#471=ORIENTED_EDGE ( 'NONE', *, *, #38149, .T. ) ;
#480=CARTESIAN_POINT ( 'NONE',  ( -22.97409385650551528, -9.792211528768504536, 50.49490371617623197 ) ) ;
#501=VERTEX_POINT ( 'NONE', #17504 ) ;
#514=CARTESIAN_POINT ( 'NONE',  ( -22.16159385650551528, -9.295667164867525756, 49.30633214617472504 ) ) ;
#549=CARTESIAN_POINT ( 'NONE',  ( -22.41159385650551528, -6.922745924619793101, 51.69366785382590024 ) ) ;
#559=EDGE_CURVE ( 'NONE', #47460, #43020, #7166, .T. ) ;
#574=DIRECTION ( 'NONE',  ( -1.000000000000000000, -1.669677910507523057E-21, -6.493791346278465266E-22 ) ) ;
#582=CARTESIAN_POINT ( 'NONE',  ( -21.45534385650551812, -7.417179338643134834, 52.18511593390279302 ) ) ;
#597=CARTESIAN_POINT ( 'NONE',  ( -15.49284385650551776, -7.406986770994973490, 48.81910596585309747 ) ) ;
#604=CARTESIAN_POINT ( 'NONE',  ( -14.34284385650551563, -8.811426318492348031, 52.18089403414752070 ) ) ;
#614=DIRECTION ( 'NONE',  ( -1.000000000000000000, 0.000000000000000000, 0.000000000000000000 ) ) ;
#616=AXIS2_PLACEMENT_3D ( 'NONE', #41938, #33542, #44666 ) ;
#649=EDGE_CURVE ( 'NONE', #8229, #44349, #41798, .T. ) ;
#658=VECTOR ( 'NONE', #26141, 1000.000000000000114 ) ;
#671=ORIENTED_EDGE ( 'NONE', *, *, #10542, .F. ) ;
#673=CARTESIAN_POINT ( 'NONE',  ( -15.83034385650551634, -9.794322478646142471, 51.19202720610083901 ) ) ;
#678=AXIS2_PLACEMENT_3D ( 'NONE', #4820, #19589, #20074 ) ;
#681=EDGE_CURVE ( 'NONE', #47374, #501, #32348, .T. ) ;
#691=AXIS2_PLACEMENT_3D ( 'NONE', #27217, #8045, #38779 ) ;
#698=EDGE_CURVE ( 'NONE', #20557, #17825, #15830, .T. ) ;
#701=CARTESIAN_POINT ( 'NONE',  ( -18.22409385759798894, -9.359200813967568422, 50.49621490985803263 ) ) ;
#706=PLANE ( 'NONE',  #16311 ) ;
#707=ORIENTED_EDGE ( 'NONE', *, *, #43794, .F. ) ;
#714=ORIENTED_EDGE ( 'NONE', *, *, #34422, .F. ) ;
#717=CARTESIAN_POINT ( 'NONE',  ( -19.34909385759798894, -8.112991634885936776, 51.74999426922421719 ) ) ;
#719=DIRECTION ( 'NONE',  ( 0.9524241471993249997, 0.0009228828802128017121, -0.3047743298226210928 ) ) ;
#720=CARTESIAN_POINT ( 'NONE',  ( -22.07409385650551670, -9.792211528768504536, 50.49490371617623197 ) ) ;
#734=ORIENTED_EDGE ( 'NONE', *, *, #46518, .T. ) ;
#761=CARTESIAN_POINT ( 'NONE',  ( -18.50534385650551528, -8.801233750844183135, 48.81488406609782515 ) ) ;
#767=CARTESIAN_POINT ( 'NONE',  ( -16.44909385541304303, -8.112991634885936776, 51.74999426922421719 ) ) ;
#768=CARTESIAN_POINT ( 'NONE',  ( -15.77409385541301035, -6.859212275519753099, 50.50378509014291240 ) ) ;
#779=CARTESIAN_POINT ( 'NONE',  ( -20.98034385759799392, -9.360768649639302552, 51.01397948905921709 ) ) ;
#796=CARTESIAN_POINT ( 'NONE',  ( -23.31159385541299756, -8.990409506049253707, 49.61344411288070688 ) ) ;
#801=CARTESIAN_POINT ( 'NONE',  ( -13.38659385759799214, -7.222650657624104298, 49.61879703869476543 ) ) ;
#812=EDGE_LOOP ( 'NONE', ( #12953, #5812, #37264, #19449 ) ) ;
#819=DIRECTION ( 'NONE',  ( 1.000000000000000000, -4.164305804376849172E-17, 1.614929280266638808E-16 ) ) ;
#820=CARTESIAN_POINT ( 'NONE',  ( -17.43659385759799108, -8.995762431863214559, 51.38120296130585274 ) ) ;
#826=CYLINDRICAL_SURFACE ( 'NONE', #44109, 1.949999999999999734 ) ;
#827=CARTESIAN_POINT ( 'NONE',  ( -19.43034385650552309, -9.794322478646142471, 51.19202720610083190 ) ) ;
#849=CARTESIAN_POINT ( 'NONE',  ( -16.87409385759798752, -6.859212275519751323, 50.50378509014259265 ) ) ;
#854=CARTESIAN_POINT ( 'NONE',  ( -21.56784385541304516, -9.357632978295830739, 49.97845033065684106 ) ) ;
#865=EDGE_CURVE ( 'NONE', #1563, #42690, #28247, .T. ) ;
#890=CARTESIAN_POINT ( 'NONE',  ( 18.51825960693462392, 3.131787348086252365, 50.70169625874538610 ) ) ;
#906=CARTESIAN_POINT ( 'NONE',  ( -22.01784385541265365, -6.860780111193850672, 51.02154966934617164 ) ) ;
#911=CARTESIAN_POINT ( 'NONE',  ( -19.99284385541303166, -8.630756214087139000, 51.74842643355250971 ) ) ;
#914=CARTESIAN_POINT ( 'NONE',  ( -21.88034385650551883, -6.424090610841176385, 49.80797279389977916 ) ) ;
#919=CARTESIAN_POINT ( 'NONE',  ( -15.49284385650551776, -7.406986770994973490, 48.81910596585309747 ) ) ;
#921=COLOUR_RGB ( '', 0.08235294, 0.09019608, 0.10196078) ;
#924=AXIS2_PLACEMENT_3D ( 'NONE', #9917, #31839, #5505 ) ;
#941=ORIENTED_EDGE ( 'NONE', *, *, #5847, .F. ) ;
#962=CARTESIAN_POINT ( 'NONE',  ( -12.99284385759798965, -8.630756214087126565, 51.74842643355248129 ) ) ;
#969=ORIENTED_EDGE ( 'NONE', *, *, #6552, .T. ) ;
#1000=CARTESIAN_POINT ( 'NONE',  ( -15.97409385650551705, -9.792211528768504536, 50.49490371617623197 ) ) ;
#1007=CARTESIAN_POINT ( 'NONE',  ( -15.66159385541290838, -7.228003583437949686, 51.38655588712003208 ) ) ;
#1019=CARTESIAN_POINT ( 'NONE',  ( -22.27409385759798965, -6.859212275519751323, 50.50378509014259265 ) ) ;
#1032=ORIENTED_EDGE ( 'NONE', *, *, #8638, .T. ) ;
#1053=CARTESIAN_POINT ( 'NONE',  ( -18.08034385541301603, -9.360768649639462424, 51.01397948905908919 ) ) ;
#1065=CARTESIAN_POINT ( 'NONE',  ( -14.64909385650551776, -8.104110260919579645, 48.81699501597546487 ) ) ;
#1085=CARTESIAN_POINT ( 'NONE',  ( -18.67409385759799179, -6.859212275519751323, 50.50378509014259265 ) ) ;
#1088=CARTESIAN_POINT ( 'NONE',  ( -20.94909385541304303, -8.112991634885936776, 51.74999426922421719 ) ) ;
#1096=DIRECTION ( 'NONE',  ( 1.000000000000000000, 1.669677910507523057E-21, 6.493791346278465266E-22 ) ) ;
#1118=LINE ( 'NONE', #16118, #43196 ) ;
#1128=EDGE_LOOP ( 'NONE', ( #17501, #1465, #32847, #25776, #7913, #11061 ) ) ;
#1132=CARTESIAN_POINT ( 'NONE',  ( -16.19909385759799036, -8.105421454601382081, 49.25000573077640098 ) ) ;
#1145=CARTESIAN_POINT ( 'NONE',  ( -13.80534385650551776, -8.801233750844183135, 48.81488406609782515 ) ) ;
#1156=CARTESIAN_POINT ( 'NONE',  ( -21.06159385541298334, -7.228003583438046498, 51.38655588711993261 ) ) ;
#1170=DIRECTION ( 'NONE',  ( 5.539632631852608384E-05, 0.6451160323795128715, -0.7640846168443403696 ) ) ;
#1188=CARTESIAN_POINT ( 'NONE',  ( -20.27409385650551599, -9.792211528768504536, 50.49490371617623197 ) ) ;
#1226=CARTESIAN_POINT ( 'NONE',  ( -18.28034385650551741, -6.424090610841176385, 49.80797279389978627 ) ) ;
#1230=CARTESIAN_POINT ( 'NONE',  ( -35.42409385541304800, -8.109206544743658540, 50.50000000000030553 ) ) ;
#1231=ORIENTED_EDGE ( 'NONE', *, *, #27331, .F. ) ;
#1246=EDGE_CURVE ( 'NONE', #12395, #24862, #28441, .T. ) ;
#1261=CARTESIAN_POINT ( 'NONE',  ( -21.51159385650551670, -6.922745924619793101, 51.69366785382590024 ) ) ;
#1286=DIRECTION ( 'NONE',  ( 0.000000000000000000, -0.9999954153791273948, -0.003028072113819838245 ) ) ;
#1295=CARTESIAN_POINT ( 'NONE',  ( -17.57409385650551314, -9.792211528768504536, 50.49490371617623197 ) ) ;
#1318=CARTESIAN_POINT ( 'NONE',  ( -23.42409385541304090, -9.359200813967568422, 50.49621490985803263 ) ) ;
#1349=EDGE_CURVE ( 'NONE', #33983, #40074, #17412, .T. ) ;
#1376=CARTESIAN_POINT ( 'NONE',  ( -21.03659385650551528, -6.915538690918074494, 49.31353937987644542 ) ) ;
#1383=CARTESIAN_POINT ( 'NONE',  ( -20.86784385650551954, -6.428312510596451368, 51.20221977374900035 ) ) ;
#1391=CARTESIAN_POINT ( 'NONE',  ( -20.83659385541298548, -8.995762431863285613, 51.38120296130592379 ) ) ;
#1397=VECTOR ( 'NONE', #15816, 1000.000000000000114 ) ;
#1422=ADVANCED_FACE ( 'NONE', ( #42435 ), #30630, .T. ) ;
#1431=CARTESIAN_POINT ( 'NONE',  ( -18.24909385650551741, -8.104110260919579645, 48.81699501597546487 ) ) ;
#1453=ORIENTED_EDGE ( 'NONE', *, *, #1885, .F. ) ;
#1463=CARTESIAN_POINT ( 'NONE',  ( -17.15534385759799108, -8.623186033802570094, 49.24843789510466507 ) ) ;
#1465=ORIENTED_EDGE ( 'NONE', *, *, #36181, .F. ) ;
#1469=CARTESIAN_POINT ( 'NONE',  ( -16.64909385650551599, -8.104110260919579645, 48.81699501597546487 ) ) ;
#1470=AXIS2_PLACEMENT_3D ( 'NONE', #1230, #23414, #38667 ) ;
#1545=CARTESIAN_POINT ( 'NONE',  ( -15.38034385650552061, -6.424090610841176385, 49.80797279389978627 ) ) ;
#1563=VERTEX_POINT ( 'NONE', #43644 ) ;
#1572=CARTESIAN_POINT ( 'NONE',  ( -22.91784385541304303, -6.860780111191487229, 51.02154966934377001 ) ) ;
#1575=EDGE_CURVE ( 'NONE', #17990, #7797, #36227, .T. ) ;
#1578=EDGE_CURVE ( 'NONE', #46443, #1741, #15049, .T. ) ;
#1588=DIRECTION ( 'NONE',  ( 6.493791346278465266E-22, 1.084253996632606248E-42, -1.000000000000000000 ) ) ;
#1594=CARTESIAN_POINT ( 'NONE',  ( -35.42409385541304800, -8.109206544743658540, 50.50000000000030553 ) ) ;
#1616=EDGE_CURVE ( 'NONE', #42061, #46061, #37166, .T. ) ;
#1619=ORIENTED_EDGE ( 'NONE', *, *, #3036, .F. ) ;
#1635=CARTESIAN_POINT ( 'NONE',  ( -21.82409385650551670, -6.426201560718813433, 50.50509628382439331 ) ) ;
#1643=AXIS2_PLACEMENT_3D ( 'NONE', #40956, #37235, #2793 ) ;
#1652=EDGE_LOOP ( 'NONE', ( #23167, #224 ) ) ;
#1655=DIRECTION ( 'NONE',  ( 0.000000000000000000, -0.9999954153791272837, -0.003028072113821676185 ) ) ;
#1677=CARTESIAN_POINT ( 'NONE',  ( -36.42409385541304800, -6.859212275519750435, 50.50378509014258555 ) ) ;
#1683=EDGE_CURVE ( 'NONE', #6741, #11159, #44202, .T. ) ;
#1685=CARTESIAN_POINT ( 'NONE',  ( -19.03659385650551528, -6.915538690918074494, 49.31353937987644542 ) ) ;
#1687=( BOUNDED_CURVE ( )  B_SPLINE_CURVE ( 2, ( #33353, #28309, #5415, #43074, #20434, #7049, #13020, #31754, #1720 ),
 .UNSPECIFIED., .F., .F. ) 
 B_SPLINE_CURVE_WITH_KNOTS ( ( 3, 2, 2, 2, 3 ),
 ( 0.000000000000000000, 0.01041666666666664007, 0.02083333333333328014, 0.03124999999999992020, 0.04166666666666656027 ),
 .UNSPECIFIED. ) 
 CURVE ( )  GEOMETRIC_REPRESENTATION_ITEM ( )  RATIONAL_B_SPLINE_CURVE ( ( 1.000000000000000000, 0.9238795325112867385, 1.000000000000000000, 0.9238795325112867385, 1.000000000000000000, 0.9238795325112867385, 1.000000000000000000, 0.9238795325112875156, 0.9999999999999992228 ) ) 
 REPRESENTATION_ITEM ( '' )  );
#1692=VERTEX_POINT ( 'NONE', #18728 ) ;
#1697=CARTESIAN_POINT ( 'NONE',  ( -36.42409385541304800, -6.859212275519750435, 50.50378509014258555 ) ) ;
#1702=( BOUNDED_CURVE ( )  B_SPLINE_CURVE ( 2, ( #32253, #28315, #5669, #24857, #13978, #43581, #20918, #21413, #46778 ),
 .UNSPECIFIED., .F., .F. ) 
 B_SPLINE_CURVE_WITH_KNOTS ( ( 3, 2, 2, 2, 3 ),
 ( 0.7083333333333332593, 0.7187499999999998890, 0.7291666666666665186, 0.7395833333333333703, 0.7500000000000000000 ),
 .UNSPECIFIED. ) 
 CURVE ( )  GEOMETRIC_REPRESENTATION_ITEM ( )  RATIONAL_B_SPLINE_CURVE ( ( 1.000000000000000888, 0.9238795325112859613, 1.000000000000000000, 0.9238795325112867385, 1.000000000000000000, 0.9238795325112867385, 1.000000000000000000, 0.9238795325112867385, 1.000000000000000000 ) ) 
 REPRESENTATION_ITEM ( '' )  );
#1720=CARTESIAN_POINT ( 'NONE',  ( -22.27409385759798965, -6.859212275519751323, 50.50378509014259265 ) ) ;
#1729=CARTESIAN_POINT ( 'NONE',  ( -16.31159385650551386, -6.922745924619793101, 51.69366785382590024 ) ) ;
#1741=VERTEX_POINT ( 'NONE', #34729 ) ;
#1748=CARTESIAN_POINT ( 'NONE',  ( -18.16784385759799392, -9.357632978295830739, 49.97845033065684106 ) ) ;
#1755=CARTESIAN_POINT ( 'NONE',  ( 18.46573386768564973, 0.6652513346184721899, 50.77657095919170871 ) ) ;
#1795=CARTESIAN_POINT ( 'NONE',  ( -17.51784385650551812, -9.790100578890868377, 49.79778022625163203 ) ) ;
#1819=CARTESIAN_POINT ( 'NONE',  ( -20.61159385541304445, -8.990409506049200417, 49.61344411288074951 ) ) ;
#1821=CIRCLE ( 'NONE', #18313, 1.249999999999999334 ) ;
#1854=AXIS2_PLACEMENT_3D ( 'NONE', #26248, #169, #29697 ) ;
#1872=CARTESIAN_POINT ( 'NONE',  ( -21.59909385650551528, -8.114302828567740988, 52.18300498402516041 ) ) ;
#1876=CARTESIAN_POINT ( 'NONE',  ( -21.71159385650551599, -6.922745924619793101, 51.69366785382590024 ) ) ;
#1881=VECTOR ( 'NONE', #25166, 1000.000000000000000 ) ;
#1885=EDGE_CURVE ( 'NONE', #48035, #16853, #9368, .T. ) ;
#1923=CARTESIAN_POINT ( 'NONE',  ( -18.13659385650551670, -6.915538690918074494, 49.31353937987644542 ) ) ;
#1940=CYLINDRICAL_SURFACE ( 'NONE', #27644, 1.249999999999998668 ) ;
#1946=CARTESIAN_POINT ( 'NONE',  ( 10.57590614458695377, 1.890747609047609190, 50.53028072113853142 ) ) ;
#1950=( BOUNDED_SURFACE ( )  B_SPLINE_SURFACE ( 1, 2, ( 
 ( #27373, #35892, #12115, #19260, #8675, #8915, #4480, #19990, #42406, #34262, #549, #38696, #8193, #42159, #8422, #23448, #38443, #46339, #4733, #23704, #13491, #42655, #4980, #34995, #2174, #28536, #1261, #39605, #24607, #17177, #32229, #47244, #43560, #14675, #14199, #40099, #28766, #7096, #36612, #3146, #44054, #17436, #2893, #32924, #21858, #6114, #29741, #10305, #36379, #24838, #25550, #39847, #2662, #21143, #32467, #36140, #33163, #2425, #13722, #48439, #48201, #47491, #29255, #40812, #44776, #43801, #25797, #10056, #25078, #10777, #6361, #21394, #17668, #44290, #32693, #47718, #22114, #17899, #18150, #25322, #13957, #47965, #10543, #36854, #29005, #40333, #6605, #21626, #37104, #40563, #14431, #6842, #29491, #3384, #44521, #18395, #33400, #26532, #33647, #29990, #4142, #26784, #34386, #45263, #27017, #7348, #33913, #19140, #11507, #11760, #12003, #18902, #45502, #22855, #34147, #4364, #3892, #45024, #19380, #11275, #26048, #23323, #41803, #37850, #38319, #4607, #8085, #673, #19627, #34638, #30962, #41552, #41067, #919, #22594, #7836, #37589, #22346, #23093, #444, #206, #3631, #37345, #14933, #18635, #15419, #8311, #15181, #11028, #38085, #48691, #30244, #15674, #30488, #30728, #45754, #42039, #15917, #26287, #41300, #7589, #24057, #24549, #1145, #24301, #42533, #9274, #39306, #46468, #27499, #39053, #31429, #28224, #38572, #42283, #4862, #19878, #31919, #34876 ),
 ( #43257, #9040, #5590, #16400, #16151, #5340, #20355, #42999, #27256, #35835, #12720, #8803, #9526, #23821, #20603, #35116, #31193, #39544, #27737, #35601, #42769, #35364, #46216, #12471, #1635, #12948, #1876, #16647, #13177, #8548, #20108, #31679, #46703, #27974, #46934, #5100, #16878, #5825, #20837, #2117, #38821, #1383, #17115, #45979, #12236, #23575, #17837, #43990, #10714, #25730, #29193, #40504, #44460, #40749, #3326, #17604, #13428, #7029, #43741, #28943, #9991, #43500, #32865, #10247, #40038, #24783, #9763, #36077, #39784, #25261, #29429, #21331, #44233, #47902, #25488, #47430, #32167, #22048, #33097, #36320, #2360, #2832, #37041, #47182, #21569, #40279, #14135, #10486, #25017, #48143, #13660, #6545, #14372, #6302, #28477, #6782, #3078, #32410, #21793, #36548, #6050, #21081, #36788, #17370, #2605, #28704, #32638, #47659, #18083, #13900, #25984, #4311, #19078, #10964, #30181, #45439, #19319, #48376, #11693, #22286, #33336, #48628, #7774, #375, #44961, #15359, #45199, #7527, #11443, #41239, #33581, #22791, #34323, #26469, #18835, #8025, #41005, #37784, #18571, #4080, #34086, #22529, #3567, #33843, #37523, #26718, #44709, #14609, #7284, #37279, #41481, #3824, #14864, #11216, #29926, #142, #26225, #30423, #15122, #41736, #23037, #18329, #38022, #29673, #25899, #21960, #25647, #18003, #10877, #21717, #21490, #40912, #39952, #33499, #2754, #44383, #33019, #47589, #7203 ) ),
 .UNSPECIFIED., .F., .F., .F. ) 
 B_SPLINE_SURFACE_WITH_KNOTS ( ( 2, 2 ),
 ( 3, 2, 2, 2, 2, 2, 2, 2, 2, 2, 2, 2, 2, 2, 2, 2, 2, 2, 2, 2, 2, 2, 2, 2, 2, 2, 2, 2, 2, 2, 2, 2, 2, 2, 2, 2, 2, 2, 2, 2, 2, 2, 2, 2, 2, 2, 2, 2, 2, 2, 2, 2, 2, 2, 2, 2, 2, 2, 2, 2, 2, 2, 2, 2, 2, 2, 2, 2, 2, 2, 2, 2, 2, 2, 2, 2, 2, 2, 2, 2, 2, 2, 2, 2, 2, 2, 2, 2, 2, 3 ),
 ( 0.000000000000000000, 1.000000000000000000 ),
 ( 0.000000000000000000, 0.01041666666666666609, 0.02083333333333333218, 0.03125000000000000000, 0.04166666666666666435, 0.05208333333333333565, 0.06250000000000000000, 0.07291666666666667129, 0.08333333333333332871, 0.09375000000000000000, 0.1041666666666666713, 0.1145833333333333287, 0.1250000000000000000, 0.1354166666666666574, 0.1458333333333333426, 0.1562500000000000000, 0.1666666666666666574, 0.1770833333333333426, 0.1875000000000000000, 0.1979166666666666574, 0.2083333333333333426, 0.2187500000000000000, 0.2291666666666666574, 0.2395833333333333426, 0.2500000000000000000, 0.2604166666666666852, 0.2708333333333333148, 0.2812500000000000000, 0.2916666666666666852, 0.3020833333333333148, 0.3125000000000000000, 0.3229166666666666852, 0.3333333333333333148, 0.3437500000000000000, 0.3541666666666666852, 0.3645833333333333148, 0.3750000000000000000, 0.3854166666666666852, 0.3958333333333333148, 0.4062500000000000000, 0.4166666666666666852, 0.4270833333333333148, 0.4375000000000000000, 0.4479166666666666852, 0.4583333333333333148, 0.4687500000000000000, 0.4791666666666666852, 0.4895833333333333148, 0.5000000000000000000, 0.5104166666666666297, 0.5208333333333333703, 0.5312500000000000000, 0.5416666666666666297, 0.5520833333333333703, 0.5625000000000000000, 0.5729166666666666297, 0.5833333333333333703, 0.5937500000000000000, 0.6041666666666666297, 0.6145833333333333703, 0.6250000000000000000, 0.6354166666666666297, 0.6458333333333333703, 0.6562500000000000000, 0.6666666666666666297, 0.6770833333333333703, 0.6875000000000000000, 0.6979166666666666297, 0.7083333333333333703, 0.7187500000000000000, 0.7291666666666666297, 0.7395833333333333703, 0.7500000000000000000, 0.7604166666666666297, 0.7708333333333333703, 0.7812500000000000000, 0.7916666666666666297, 0.8020833333333333703, 0.8125000000000000000, 0.8229166666666666297, 0.8333333333333333703, 0.8437500000000000000, 0.8541666666666666297, 0.8645833333333333703, 0.8750000000000000000, 0.8854166666666666297, 0.8958333333333333703, 0.9062500000000000000, 0.9166666666666666297, 0.9259051122687710356 ),
 .UNSPECIFIED. ) 
 GEOMETRIC_REPRESENTATION_ITEM ( )  RATIONAL_B_SPLINE_SURFACE ( (
 ( 1.000000000000000000, 0.9238795325112867385, 1.000000000000000000, 0.9238795325112867385, 1.000000000000000000, 0.9238795325112867385, 1.000000000000000000, 0.9238795325112867385, 1.000000000000000000, 0.9238795325112867385, 1.000000000000000000, 0.9238795325112867385, 1.000000000000000000, 0.9238795325112867385, 1.000000000000000000, 0.9238795325112867385, 1.000000000000000000, 0.9238795325112867385, 1.000000000000000000, 0.9238795325112867385, 1.000000000000000000, 0.9238795325112867385, 1.000000000000000000, 0.9238795325112867385, 1.000000000000000000, 0.9238795325112867385, 1.000000000000000000, 0.9238795325112867385, 1.000000000000000000, 0.9238795325112867385, 1.000000000000000000, 0.9238795325112867385, 1.000000000000000000, 0.9238795325112867385, 1.000000000000000000, 0.9238795325112867385, 1.000000000000000000, 0.9238795325112867385, 1.000000000000000000, 0.9238795325112867385, 1.000000000000000000, 0.9238795325112867385, 1.000000000000000000, 0.9238795325112867385, 1.000000000000000000, 0.9238795325112867385, 1.000000000000000000, 0.9238795325112867385, 1.000000000000000000, 0.9238795325112867385, 1.000000000000000000, 0.9238795325112867385, 1.000000000000000000, 0.9238795325112867385, 1.000000000000000000, 0.9238795325112867385, 1.000000000000000000, 0.9238795325112867385, 1.000000000000000000, 0.9238795325112867385, 1.000000000000000000, 0.9238795325112867385, 1.000000000000000000, 0.9238795325112867385, 1.000000000000000000, 0.9238795325112867385, 1.000000000000000000, 0.9238795325112867385, 1.000000000000000000, 0.9238795325112867385, 1.000000000000000000, 0.9238795325112867385, 1.000000000000000000, 0.9238795325112867385, 1.000000000000000000, 0.9238795325112867385, 1.000000000000000000, 0.9238795325112867385, 1.000000000000000000, 0.9238795325112867385, 1.000000000000000000, 0.9238795325112867385, 1.000000000000000000, 0.9238795325112867385, 1.000000000000000000, 0.9238795325112867385, 1.000000000000000000, 0.9238795325112867385, 1.000000000000000000, 0.9238795325112867385, 1.000000000000000000, 0.9238795325112867385, 1.000000000000000000, 0.9238795325112867385, 1.000000000000000000, 0.9238795325112867385, 1.000000000000000000, 0.9238795325112867385, 1.000000000000000000, 0.9238795325112867385, 1.000000000000000000, 0.9238795325112867385, 1.000000000000000000, 0.9238795325112867385, 1.000000000000000000, 0.9238795325112867385, 1.000000000000000000, 0.9238795325112867385, 1.000000000000000000, 0.9238795325112867385, 1.000000000000000000, 0.9238795325112867385, 1.000000000000000000, 0.9238795325112867385, 1.000000000000000000, 0.9238795325112867385, 1.000000000000000000, 0.9238795325112867385, 1.000000000000000000, 0.9238795325112867385, 1.000000000000000000, 0.9238795325112867385, 1.000000000000000000, 0.9238795325112867385, 1.000000000000000000, 0.9238795325112867385, 1.000000000000000000, 0.9238795325112867385, 1.000000000000000000, 0.9238795325112867385, 1.000000000000000000, 0.9238795325112867385, 1.000000000000000000, 0.9238795325112867385, 1.000000000000000000, 0.9238795325112867385, 1.000000000000000000, 0.9238795325112867385, 1.000000000000000000, 0.9238795325112867385, 1.000000000000000000, 0.9238795325112867385, 1.000000000000000000, 0.9238795325112867385, 1.000000000000000000, 0.9238795325112867385, 1.000000000000000000, 0.9238795325112867385, 1.000000000000000000, 0.9238795325112867385, 1.000000000000000000, 0.9238795325112867385, 1.000000000000000000, 0.9238795325112867385, 1.000000000000000000, 0.9238795325112867385, 1.000000000000000000, 0.9238795325112867385, 1.000000000000000000, 0.9238795325112867385, 1.000000000000000000, 0.9238795325112867385, 1.000000000000000000, 0.9238795325112867385, 1.000000000000000000, 0.9238795325112867385, 1.000000000000000000, 0.9238795325112867385, 1.000000000000000000, 0.9238795325112867385, 1.000000000000000000, 0.9238795325112867385, 1.000000000000000000, 0.9238795325112867385, 1.000000000000000000, 0.9238795325112867385, 1.000000000000000000, 0.9324894593822820044, 0.9847278705211290895),
 ( 1.000000000000000000, 0.9238795325112867385, 1.000000000000000000, 0.9238795325112867385, 1.000000000000000000, 0.9238795325112867385, 1.000000000000000000, 0.9238795325112867385, 1.000000000000000000, 0.9238795325112867385, 1.000000000000000000, 0.9238795325112867385, 1.000000000000000000, 0.9238795325112867385, 1.000000000000000000, 0.9238795325112867385, 1.000000000000000000, 0.9238795325112867385, 1.000000000000000000, 0.9238795325112867385, 1.000000000000000000, 0.9238795325112867385, 1.000000000000000000, 0.9238795325112867385, 1.000000000000000000, 0.9238795325112867385, 1.000000000000000000, 0.9238795325112867385, 1.000000000000000000, 0.9238795325112867385, 1.000000000000000000, 0.9238795325112867385, 1.000000000000000000, 0.9238795325112867385, 1.000000000000000000, 0.9238795325112867385, 1.000000000000000000, 0.9238795325112867385, 1.000000000000000000, 0.9238795325112867385, 1.000000000000000000, 0.9238795325112867385, 1.000000000000000000, 0.9238795325112867385, 1.000000000000000000, 0.9238795325112867385, 1.000000000000000000, 0.9238795325112867385, 1.000000000000000000, 0.9238795325112867385, 1.000000000000000000, 0.9238795325112867385, 1.000000000000000000, 0.9238795325112867385, 1.000000000000000000, 0.9238795325112867385, 1.000000000000000000, 0.9238795325112867385, 1.000000000000000000, 0.9238795325112867385, 1.000000000000000000, 0.9238795325112867385, 1.000000000000000000, 0.9238795325112867385, 1.000000000000000000, 0.9238795325112867385, 1.000000000000000000, 0.9238795325112867385, 1.000000000000000000, 0.9238795325112867385, 1.000000000000000000, 0.9238795325112867385, 1.000000000000000000, 0.9238795325112867385, 1.000000000000000000, 0.9238795325112867385, 1.000000000000000000, 0.9238795325112867385, 1.000000000000000000, 0.9238795325112867385, 1.000000000000000000, 0.9238795325112867385, 1.000000000000000000, 0.9238795325112867385, 1.000000000000000000, 0.9238795325112867385, 1.000000000000000000, 0.9238795325112867385, 1.000000000000000000, 0.9238795325112867385, 1.000000000000000000, 0.9238795325112867385, 1.000000000000000000, 0.9238795325112867385, 1.000000000000000000, 0.9238795325112867385, 1.000000000000000000, 0.9238795325112867385, 1.000000000000000000, 0.9238795325112867385, 1.000000000000000000, 0.9238795325112867385, 1.000000000000000000, 0.9238795325112867385, 1.000000000000000000, 0.9238795325112867385, 1.000000000000000000, 0.9238795325112867385, 1.000000000000000000, 0.9238795325112867385, 1.000000000000000000, 0.9238795325112867385, 1.000000000000000000, 0.9238795325112867385, 1.000000000000000000, 0.9238795325112867385, 1.000000000000000000, 0.9238795325112867385, 1.000000000000000000, 0.9238795325112867385, 1.000000000000000000, 0.9238795325112867385, 1.000000000000000000, 0.9238795325112867385, 1.000000000000000000, 0.9238795325112867385, 1.000000000000000000, 0.9238795325112867385, 1.000000000000000000, 0.9238795325112867385, 1.000000000000000000, 0.9238795325112867385, 1.000000000000000000, 0.9238795325112867385, 1.000000000000000000, 0.9238795325112867385, 1.000000000000000000, 0.9238795325112867385, 1.000000000000000000, 0.9238795325112867385, 1.000000000000000000, 0.9238795325112867385, 1.000000000000000000, 0.9238795325112867385, 1.000000000000000000, 0.9238795325112867385, 1.000000000000000000, 0.9238795325112867385, 1.000000000000000000, 0.9238795325112867385, 1.000000000000000000, 0.9238795325112867385, 1.000000000000000000, 0.9238795325112867385, 1.000000000000000000, 0.9238795325112867385, 1.000000000000000000, 0.9238795325112867385, 1.000000000000000000, 0.9238795325112867385, 1.000000000000000000, 0.9238795325112867385, 1.000000000000000000, 0.9238795325112867385, 1.000000000000000000, 0.9238795325112867385, 1.000000000000000000, 0.9238795325112867385, 1.000000000000000000, 0.9238795325112867385, 1.000000000000000000, 0.9238795325112867385, 1.000000000000000000, 0.9238795325112867385, 1.000000000000000000, 0.9238795325112867385, 1.000000000000000000, 0.9324894593822820044, 0.9847278705211290895) ) ) 
 REPRESENTATION_ITEM ( '' )  SURFACE ( )  );
#1957=ORIENTED_EDGE ( 'NONE', *, *, #43597, .T. ) ;
#1959=CARTESIAN_POINT ( 'NONE',  ( -13.94909385650551492, -8.104110260919579645, 48.81699501597546487 ) ) ;
#1979=CARTESIAN_POINT ( 'NONE',  ( -20.36159385759798823, -7.228003583438117552, 51.38655588711986155 ) ) ;
#1991=CARTESIAN_POINT ( 'NONE',  ( 10.57590614458695377, 1.637040139411225059, 51.75426295951076838 ) ) ;
#2004=ORIENTED_EDGE ( 'NONE', *, *, #32512, .T. ) ;
#2014=CARTESIAN_POINT ( 'NONE',  ( -18.56159385759799108, -7.228003583438117552, 51.38655588711986155 ) ) ;
#2015=FACE_BOUND ( 'NONE', #10500, .T. ) ;
#2025=CARTESIAN_POINT ( 'NONE',  ( 18.07590614458695200, 0.7915096701590282890, 50.27695098796855433 ) ) ;
#2031=CARTESIAN_POINT ( 'NONE',  ( -16.84284385650551741, -8.811426318492348031, 52.18089403414752070 ) ) ;
#2033=ORIENTED_EDGE ( 'NONE', *, *, #9350, .T. ) ;
#2042=CARTESIAN_POINT ( 'NONE',  ( -36.42409385541304800, -6.859212275519750435, 50.50378509014258555 ) ) ;
#2058=CARTESIAN_POINT ( 'NONE',  ( -17.46159385541304232, -7.228003583438117552, 51.38655588711986155 ) ) ;
#2071=VERTEX_POINT ( 'NONE', #19171 ) ;
#2113=CARTESIAN_POINT ( 'NONE',  ( -19.74284385650551599, -8.811426318492348031, 52.18089403414751359 ) ) ;
#2117=CARTESIAN_POINT ( 'NONE',  ( -20.98034385650551314, -6.424090610841176385, 49.80797279389977916 ) ) ;
#2132=CARTESIAN_POINT ( 'NONE',  ( 18.57590614458695200, 3.151498850453765321, 50.28409723815717314 ) ) ;
#2159=CARTESIAN_POINT ( 'NONE',  ( -17.68659385650551741, -9.302874398569244363, 51.68646062012417985 ) ) ;
#2174=CARTESIAN_POINT ( 'NONE',  ( -21.62409385650551741, -6.426201560718812544, 50.50509628382439331 ) ) ;
#2195=VECTOR ( 'NONE', #353, 1000.000000000000000 ) ;
#2200=CARTESIAN_POINT ( 'NONE',  ( -14.79284385650551492, -7.406986770994972602, 48.81910596585309747 ) ) ;
#2208=DIRECTION ( 'NONE',  ( -1.000000000000000000, -1.669677910507523057E-21, -6.493791346278465266E-22 ) ) ;
#2211=ORIENTED_EDGE ( 'NONE', *, *, #19807, .F. ) ;
#2218=CARTESIAN_POINT ( 'NONE',  ( -19.63034385759799605, -6.857644439848013640, 49.98602051094139398 ) ) ;
#2219=DIRECTION ( 'NONE',  ( 1.000000000000000000, -4.164305804376849172E-17, 1.614929280266638808E-16 ) ) ;
#2229=PLANE ( 'NONE',  #26908 ) ;
#2242=EDGE_CURVE ( 'NONE', #9318, #12877, #15099, .T. ) ;
#2248=ORIENTED_EDGE ( 'NONE', *, *, #44277, .F. ) ;
#2256=CARTESIAN_POINT ( 'NONE',  ( -18.33659385759798965, -8.995762431863214559, 51.38120296130585274 ) ) ;
#2274=EDGE_CURVE ( 'NONE', #30416, #44513, #43256, .T. ) ;
#2288=DIRECTION ( 'NONE',  ( 6.374839753205895344E-22, 0.007114381193220357599, -0.9999746924698832418 ) ) ;
#2289=CARTESIAN_POINT ( 'NONE',  ( -21.62409385541304374, -9.359200813967568422, 50.49621490985803263 ) ) ;
#2301=CARTESIAN_POINT ( 'NONE',  ( -19.59909385541304516, -8.105421454601382081, 49.25000573077640098 ) ) ;
#2328=DIRECTION ( 'NONE',  ( 0.000000000000000000, 0.007114381193220285608, -0.9999746924698833528 ) ) ;
#2338=DIRECTION ( 'NONE',  ( 1.000000000000000000, -4.164305804376849172E-17, 1.614929280266638808E-16 ) ) ;
#2351=CARTESIAN_POINT ( 'NONE',  ( -22.21784385759799108, -6.860780111191482789, 51.02154966934377001 ) ) ;
#2354=CARTESIAN_POINT ( 'NONE',  ( -18.44909385650551670, -8.104110260919579645, 48.81699501597546487 ) ) ;
#2360=CARTESIAN_POINT ( 'NONE',  ( -18.67409385650551457, -9.792211528768504536, 50.49490371617623197 ) ) ;
#2370=CARTESIAN_POINT ( 'NONE',  ( -19.54284385541296842, -7.587656875400136336, 49.25157356644799478 ) ) ;
#2375=DIRECTION ( 'NONE',  ( 0.000000000000000000, 0.007114381193220344589, -0.9999746924698832418 ) ) ;
#2377=CARTESIAN_POINT ( 'NONE',  ( -16.78659385541304161, -7.222650657624102521, 49.61879703869476543 ) ) ;
#2408=CARTESIAN_POINT ( 'NONE',  ( -19.09284385650552096, -7.406986770994973490, 48.81910596585309747 ) ) ;
#2417=DIRECTION ( 'NONE',  ( 0.000000000000000000, -0.9999954153791273948, -0.003028072113819838245 ) ) ;
#2425=CARTESIAN_POINT ( 'NONE',  ( -19.76784385650551812, -6.428312510596451368, 51.20221977374900035 ) ) ;
#2426=ORIENTED_EDGE ( 'NONE', *, *, #46649, .T. ) ;
#2434=DIRECTION ( 'NONE',  ( -1.000000000000000000, 4.164305804376849172E-17, -1.614929280266638808E-16 ) ) ;
#2467=CARTESIAN_POINT ( 'NONE',  ( -18.73034385759799036, -6.857644439848013640, 49.98602051094139398 ) ) ;
#2493=CIRCLE ( 'NONE', #26090, 3.249999999999999112 ) ;
#2504=VERTEX_POINT ( 'NONE', #20753 ) ;
#2519=CARTESIAN_POINT ( 'NONE',  ( -12.97364571557156232, -9.395203622806569399, 49.41430056510258595 ) ) ;
#2520=ORIENTED_EDGE ( 'NONE', *, *, #41580, .T. ) ;
#2539=ADVANCED_FACE ( 'NONE', ( #35752 ), #17529, .F. ) ;
#2552=CARTESIAN_POINT ( 'NONE',  ( -19.26159385541304303, -7.228003583438117552, 51.38655588711986155 ) ) ;
#2567=CARTESIAN_POINT ( 'NONE',  ( -12.72364920584387349, -9.064356868646193277, 49.69365772853683438 ) ) ;
#2579=CARTESIAN_POINT ( 'NONE',  ( -21.84909385650551528, -8.104110260919577868, 48.81699501597546487 ) ) ;
#2602=CARTESIAN_POINT ( 'NONE',  ( -18.39284385650552167, -7.406986770994973490, 48.81910596585309747 ) ) ;
#2605=CARTESIAN_POINT ( 'NONE',  ( -17.32409385650551314, -6.426201560718813433, 50.50509628382439331 ) ) ;
#2626=ORIENTED_EDGE ( 'NONE', *, *, #13686, .F. ) ;
#2629=FACE_OUTER_BOUND ( 'NONE', #5332, .T. ) ;
#2662=CARTESIAN_POINT ( 'NONE',  ( -20.04909385650551457, -8.104110260919579645, 48.81699501597546487 ) ) ;
#2682=CARTESIAN_POINT ( 'NONE',  ( -14.62409385650551386, -6.426201560718813433, 50.50509628382439331 ) ) ;
#2700=CARTESIAN_POINT ( 'NONE',  ( -17.88659385759798681, -7.222650657624104298, 49.61879703869476543 ) ) ;
#2710=AXIS2_PLACEMENT_3D ( 'NONE', #4888, #1170, #37618 ) ;
#2716=CARTESIAN_POINT ( 'NONE',  ( -15.26784385541301425, -9.357632978295642445, 49.97845033065664921 ) ) ;
#2726=CARTESIAN_POINT ( 'NONE',  ( -14.62409385759799108, -9.359200813967568422, 50.49621490985803263 ) ) ;
#2738=CARTESIAN_POINT ( 'NONE',  ( -13.89284385759799356, -8.630756214087126565, 51.74842643355248129 ) ) ;
#2754=CARTESIAN_POINT ( 'NONE',  ( -13.38659385650551847, -9.302874398569244363, 51.68646062012417985 ) ) ;
#2758=FACE_OUTER_BOUND ( 'NONE', #35585, .T. ) ;
#2775=CARTESIAN_POINT ( 'NONE',  ( -16.73034385541304303, -6.857644439848013640, 49.98602051094139398 ) ) ;
#2793=DIRECTION ( 'NONE',  ( 6.374839753205896285E-22, 0.007114381193220324640, -0.9999746924698832418 ) ) ;
#2804=CYLINDRICAL_SURFACE ( 'NONE', #21896, 1.249999999999999334 ) ;
#2813=CYLINDRICAL_SURFACE ( 'NONE', #42338, 1.249999999999999334 ) ;
#2828=CARTESIAN_POINT ( 'NONE',  ( -18.56159385650551741, -9.295667164867525756, 49.30633214617472504 ) ) ;
#2832=CARTESIAN_POINT ( 'NONE',  ( -18.61784385650552309, -9.790100578890868377, 49.79778022625163203 ) ) ;
#2893=CARTESIAN_POINT ( 'NONE',  ( -20.61159385650551812, -6.922745924619793101, 51.69366785382590024 ) ) ;
#2905=DIRECTION ( 'NONE',  ( 1.616182858256114592E-16, 0.003028072113811714535, -0.9999954153791273948 ) ) ;
#2917=CARTESIAN_POINT ( 'NONE',  ( -21.17409385541299116, -6.859212275519752211, 50.50378509014304029 ) ) ;
#2933=CARTESIAN_POINT ( 'NONE',  ( -16.53659385759799250, -8.995762431863214559, 51.38120296130585274 ) ) ;
#2950=FACE_OUTER_BOUND ( 'NONE', #46296, .T. ) ;
#2981=AXIS2_PLACEMENT_3D ( 'NONE', #8332, #20626, #46491 ) ;
#3013=CARTESIAN_POINT ( 'NONE',  ( -16.16784385541304303, -9.357632978295830739, 49.97845033065684106 ) ) ;
#3017=DIRECTION ( 'NONE',  ( 0.000000000000000000, -0.9999954153791273948, -0.003028072113819838245 ) ) ;
#3019=EDGE_CURVE ( 'NONE', #45804, #16141, #8310, .T. ) ;
#3036=EDGE_CURVE ( 'NONE', #13279, #4206, #38354, .T. ) ;
#3045=CARTESIAN_POINT ( 'NONE',  ( -22.35534385650551670, -7.417179338643134834, 52.18511593390279302 ) ) ;
#3050=LINE ( 'NONE', #32842, #33116 ) ;
#3067=CARTESIAN_POINT ( 'NONE',  ( -22.16159385759798894, -7.228003583438117552, 51.38655588711986155 ) ) ;
#3068=EDGE_CURVE ( 'NONE', #45257, #20025, #17116, .T. ) ;
#3071=CARTESIAN_POINT ( 'NONE',  ( -16.87409385650551386, -9.792211528768504536, 50.49490371617623197 ) ) ;
#3078=CARTESIAN_POINT ( 'NONE',  ( -17.77409385650551243, -9.792211528768504536, 50.49490371617623197 ) ) ;
#3123=AXIS2_PLACEMENT_3D ( 'NONE', #35313, #1588, #20062 ) ;
#3125=ORIENTED_CLOSED_SHELL ( 'NONE', *, #8687, .F. );
#3139=DIRECTION ( 'NONE',  ( -1.000000000000000000, -1.669677910507523057E-21, -6.493791346278465266E-22 ) ) ;
#3146=CARTESIAN_POINT ( 'NONE',  ( -20.78034385650551386, -6.424090610841174609, 49.80797279389977916 ) ) ;
#3147=VERTEX_POINT ( 'NONE', #9320 ) ;
#3148=CARTESIAN_POINT ( 'NONE',  ( -15.32409385541304481, -9.359200813967568422, 50.49621490985804684 ) ) ;
#3184=CARTESIAN_POINT ( 'NONE',  ( -14.45534385759799179, -8.623186033802571870, 49.24843789510467218 ) ) ;
#3191=EDGE_CURVE ( 'NONE', #24967, #48035, #5864, .T. ) ;
#3202=FILL_AREA_STYLE ('',( #18451 ) ) ;
#3222=ORIENTED_EDGE ( 'NONE', *, *, #1885, .T. ) ;
#3225=CARTESIAN_POINT ( 'NONE',  ( -22.04909385650551457, -8.104110260919577868, 48.81699501597546487 ) ) ;
#3241=CARTESIAN_POINT ( 'NONE',  ( 23.52590614458706852, 1.890747609047893185, 50.53028072113869484 ) ) ;
#3256=VERTEX_POINT ( 'NONE', #17652 ) ;
#3268=CARTESIAN_POINT ( 'NONE',  ( -14.70534385541304623, -7.595227055684746986, 51.75156210489594599 ) ) ;
#3299=CARTESIAN_POINT ( 'NONE',  ( -21.96159385650551599, -9.295667164867525756, 49.30633214617472504 ) ) ;
#3305=CARTESIAN_POINT ( 'NONE',  ( -21.82409385759798681, -9.359200813967568422, 50.49621490985803263 ) ) ;
#3314=CARTESIAN_POINT ( 'NONE',  ( -13.46784385650551741, -6.428312510596451368, 51.20221977374900035 ) ) ;
#3321=CARTESIAN_POINT ( 'NONE',  ( -13.83659385650551776, -6.915538690918075382, 49.31353937987644542 ) ) ;
#3323=CARTESIAN_POINT ( 'NONE',  ( 18.51825960693461681, 0.6497078700089738978, 50.35886518353169095 ) ) ;
#3326=CARTESIAN_POINT ( 'NONE',  ( -20.13659385650551670, -6.915538690918075382, 49.31353937987644542 ) ) ;
#3349=CARTESIAN_POINT ( 'NONE',  ( 18.57590614458706924, 3.149984814396892485, 50.78409494584673922 ) ) ;
#3354=LINE ( 'NONE', #33130, #33658 ) ;
#3363=ORIENTED_EDGE ( 'NONE', *, *, #1246, .T. ) ;
#3367=ORIENTED_EDGE ( 'NONE', *, *, #28770, .T. ) ;
#3381=CARTESIAN_POINT ( 'NONE',  ( -35.42409385541304800, -8.109206544743658540, 50.50000000000030553 ) ) ;
#3384=CARTESIAN_POINT ( 'NONE',  ( -17.74284385650551599, -8.811426318492348031, 52.18089403414751359 ) ) ;
#3410=CARTESIAN_POINT ( 'NONE',  ( 18.46573386768564973, 1.637040139411225059, 51.75426295951076838 ) ) ;
#3423=VERTEX_POINT ( 'NONE', #27982 ) ;
#3427=CARTESIAN_POINT ( 'NONE',  ( -15.97409385759799072, -6.859212275519751323, 50.50378509014259265 ) ) ;
#3429=DIRECTION ( 'NONE',  ( 0.000000000000000000, 0.007114381193220381018, -0.9999746924698831307 ) ) ;
#3431=CARTESIAN_POINT ( 'NONE',  ( -14.34284385759798930, -7.587656875400192291, 49.25157356644813689 ) ) ;
#3435=EDGE_CURVE ( 'NONE', #28807, #21655, #21535, .T. ) ;
#3463=CARTESIAN_POINT ( 'NONE',  ( -20.36159385650551812, -9.295667164867525756, 49.30633214617472504 ) ) ;
#3474=CARTESIAN_POINT ( 'NONE',  ( 10.57590614458695377, 1.890747609047612521, 50.53028072113853142 ) ) ;
#3496=CARTESIAN_POINT ( 'NONE',  ( -15.52409385759799143, -9.359200813967568422, 50.49621490985803263 ) ) ;
#3503=CARTESIAN_POINT ( 'NONE',  ( -13.63659385541304481, -8.995762431863214559, 51.38120296130585274 ) ) ;
#3522=ORIENTED_EDGE ( 'NONE', *, *, #41529, .T. ) ;
#3526=LINE ( 'NONE', #7983, #41488 ) ;
#3537=CARTESIAN_POINT ( 'NONE',  ( -19.54284385650551670, -8.811426318492348031, 52.18089403414751359 ) ) ;
#3541=CARTESIAN_POINT ( 'NONE',  ( -20.92409385759799179, -9.359200813967568422, 50.49621490985803263 ) ) ;
#3543=CARTESIAN_POINT ( 'NONE',  ( 18.57590614458706924, 1.903197776136028807, 48.78032500931639959 ) ) ;
#3555=CARTESIAN_POINT ( 'NONE',  ( -13.80534385650551776, -8.801233750844183135, 48.81488406609782515 ) ) ;
#3563=CARTESIAN_POINT ( 'NONE',  ( -15.91784385650552025, -9.790100578890868377, 49.79778022625163203 ) ) ;
#3566=DIRECTION ( 'NONE',  ( -1.000000000000000000, -1.669677910507523057E-21, -6.493791346278465266E-22 ) ) ;
#3567=CARTESIAN_POINT ( 'NONE',  ( -15.18659385650551386, -9.302874398569244363, 51.68646062012417985 ) ) ;
#3595=CARTESIAN_POINT ( 'NONE',  ( -14.25534385541286397, -8.623186033802699768, 49.24843789510436665 ) ) ;
#3630=VERTEX_POINT ( 'NONE', #17122 ) ;
#3631=CARTESIAN_POINT ( 'NONE',  ( -15.04284385650551670, -8.811426318492348031, 52.18089403414752070 ) ) ;
#3650=CARTESIAN_POINT ( 'NONE',  ( -36.42409385541304800, -8.109206544743658540, 50.50000000000030553 ) ) ;
#3652=VERTEX_POINT ( 'NONE', #17380 ) ;
#3675=CARTESIAN_POINT ( 'NONE',  ( -16.14284385759799534, -7.587656875400192291, 49.25157356644813689 ) ) ;
#3686=( BOUNDED_CURVE ( )  B_SPLINE_CURVE ( 2, ( #44512, #44280, #25540, #25313, #33390, #18623, #33637, #25786, #29242 ),
 .UNSPECIFIED., .F., .F. ) 
 B_SPLINE_CURVE_WITH_KNOTS ( ( 3, 2, 2, 2, 3 ),
 ( 0.8750000000000000000, 0.8854166666666666297, 0.8958333333333333703, 0.9062500000000000000, 0.9166666666666666297 ),
 .UNSPECIFIED. ) 
 CURVE ( )  GEOMETRIC_REPRESENTATION_ITEM ( )  RATIONAL_B_SPLINE_CURVE ( ( 1.000000000000000000, 0.9238795325112867385, 1.000000000000000000, 0.9238795325112867385, 1.000000000000000000, 0.9238795325112867385, 1.000000000000000000, 0.9238795325112867385, 1.000000000000000000 ) ) 
 REPRESENTATION_ITEM ( '' )  );
#3717=CARTESIAN_POINT ( 'NONE',  ( -21.93659385650551741, -6.915538690918074494, 49.31353937987644542 ) ) ;
#3720=DIRECTION ( 'NONE',  ( -1.000000000000000000, -1.669677910507523057E-21, -6.493791346278465266E-22 ) ) ;
#3756=CARTESIAN_POINT ( 'NONE',  ( -16.11159385541304445, -8.990409506049202193, 49.61344411288074951 ) ) ;
#3764=CARTESIAN_POINT ( 'NONE',  ( -13.33034385759799001, -6.857644439848016304, 49.98602051094140819 ) ) ;
#3766=EDGE_LOOP ( 'NONE', ( #33173, #19959, #8479, #30937 ) ) ;
#3770=ORIENTED_EDGE ( 'NONE', *, *, #33455, .T. ) ;
#3794=CARTESIAN_POINT ( 'NONE',  ( -19.59909385650551883, -8.114302828567740988, 52.18300498402516041 ) ) ;
#3800=CARTESIAN_POINT ( 'NONE',  ( 18.07590614458695200, 2.137415583567194854, 51.63103269608403423 ) ) ;
#3801=CARTESIAN_POINT ( 'NONE',  ( -21.65534385759799818, -8.623186033802570094, 49.24843789510466507 ) ) ;
#3807=CARTESIAN_POINT ( 'NONE',  ( -15.94284385650552238, -8.811426318492348031, 52.18089403414752070 ) ) ;
#3815=CIRCLE ( 'NONE', #26626, 1.700000000000001954 ) ;
#3818=CARTESIAN_POINT ( 'NONE',  ( -15.41159385650551705, -6.922745924619793101, 51.69366785382590024 ) ) ;
#3824=CARTESIAN_POINT ( 'NONE',  ( -14.68034385650551599, -6.424090610841176385, 49.80797279389977916 ) ) ;
#3857=ORIENTED_EDGE ( 'NONE', *, *, #33166, .T. ) ;
#3861=CARTESIAN_POINT ( 'NONE',  ( -14.87409385541153917, -6.859212275519794844, 50.50378509015643402 ) ) ;
#3872=ORIENTED_EDGE ( 'NONE', *, *, #23253, .F. ) ;
#3880=CARTESIAN_POINT ( 'NONE',  ( -19.37409385541300111, -6.859212275519753099, 50.50378509014300477 ) ) ;
#3882=CARTESIAN_POINT ( 'NONE',  ( -13.47466815348274594, -9.357823189459171687, 50.04126597187295289 ) ) ;
#3892=CARTESIAN_POINT ( 'NONE',  ( -16.44909385650551670, -8.104110260919579645, 48.81699501597546487 ) ) ;
#3900=AXIS2_PLACEMENT_3D ( 'NONE', #3241, #36697, #6699 ) ;
#3909=DIRECTION ( 'NONE',  ( -6.493791346278467147E-22, 1.224646799147353207E-16, 1.000000000000000000 ) ) ;
#3912=VERTEX_POINT ( 'NONE', #31872 ) ;
#3913=CYLINDRICAL_SURFACE ( 'NONE', #46235, 1.249999999999998668 ) ;
#3933=CARTESIAN_POINT ( 'NONE',  ( -13.49909385759798930, -8.105421454601382081, 49.25000573077640098 ) ) ;
#3965=ORIENTED_EDGE ( 'NONE', *, *, #41951, .T. ) ;
#3971=CARTESIAN_POINT ( 'NONE',  ( -19.34909385650551883, -8.104110260919579645, 48.81699501597546487 ) ) ;
#3976=CARTESIAN_POINT ( 'NONE',  ( -22.52409385541004383, -9.359200813967481380, 50.49621490983041383 ) ) ;
#4006=DIRECTION ( 'NONE',  ( -1.000000000000000000, -1.669677910507523057E-21, -6.493791346278465266E-22 ) ) ;
#4011=CARTESIAN_POINT ( 'NONE',  ( -15.21159385541304410, -8.990409506049202193, 49.61344411288074951 ) ) ;
#4013=DIRECTION ( 'NONE',  ( -1.000000000000000000, 0.000000000000000000, 0.000000000000000000 ) ) ;
#4040=VERTEX_POINT ( 'NONE', #43945 ) ;
#4045=DIRECTION ( 'NONE',  ( 1.616182858256118783E-16, 0.003028072113822189229, -0.9999954153791275058 ) ) ;
#4050=CARTESIAN_POINT ( 'NONE',  ( -19.37409385650551741, -9.792211528768504536, 50.49490371617623197 ) ) ;
#4056=CARTESIAN_POINT ( 'NONE',  ( -21.09284385759799108, -8.630756214087126565, 51.74842643355248129 ) ) ;
#4064=STYLED_ITEM ( 'NONE', ( #7403 ), #32048 ) ;
#4067=CARTESIAN_POINT ( 'NONE',  ( -13.91784385650551670, -9.790100578890868377, 49.79778022625163203 ) ) ;
#4070=CARTESIAN_POINT ( 'NONE',  ( -21.37409385759799108, -6.859212275519751323, 50.50378509014259265 ) ) ;
#4076=CARTESIAN_POINT ( 'NONE',  ( -15.18659385650551386, -9.302874398569244363, 51.68646062012417985 ) ) ;
#4080=CARTESIAN_POINT ( 'NONE',  ( -15.35534385650551847, -7.417179338643134834, 52.18511593390279302 ) ) ;
#4087=ORIENTED_EDGE ( 'NONE', *, *, #36552, .T. ) ;
#4122=EDGE_CURVE ( 'NONE', #16141, #10355, #24979, .T. ) ;
#4130=CARTESIAN_POINT ( 'NONE',  ( -19.09284385541296558, -8.630756214087181633, 51.74842643355260918 ) ) ;
#4142=CARTESIAN_POINT ( 'NONE',  ( -17.34909385650551883, -8.104110260919579645, 48.81699501597546487 ) ) ;
#4149=( BOUNDED_CURVE ( )  B_SPLINE_CURVE ( 2, ( #25431, #10892, #11143, #30112, #33270, #15053, #18265, #29607, #22464 ),
 .UNSPECIFIED., .F., .F. ) 
 B_SPLINE_CURVE_WITH_KNOTS ( ( 3, 2, 2, 2, 3 ),
 ( 0.1666666666666666297, 0.1770833333333332871, 0.1874999999999998890, 0.1979166666666665186, 0.2083333333333331761 ),
 .UNSPECIFIED. ) 
 CURVE ( )  GEOMETRIC_REPRESENTATION_ITEM ( )  RATIONAL_B_SPLINE_CURVE ( ( 1.000000000000000222, 0.9238795325112865164, 1.000000000000000000, 0.9238795325112867385, 1.000000000000000000, 0.9238795325112867385, 1.000000000000000000, 0.9238795325112879597, 0.9999999999999987788 ) ) 
 REPRESENTATION_ITEM ( '' )  );
#4150=DIRECTION ( 'NONE',  ( 1.000000000000000000, -4.164305804376849172E-17, 1.614929280266638808E-16 ) ) ;
#4164=CARTESIAN_POINT ( 'NONE',  ( 18.57132275349405504, 1.971407400791296949, 51.78906405069922414 ) ) ;
#4182=CARTESIAN_POINT ( 'NONE',  ( -21.28659385650551528, -9.302874398569244363, 51.68646062012417985 ) ) ;
#4185=CARTESIAN_POINT ( 'NONE',  ( -14.17409385759798823, -6.859212275519751323, 50.50378509014259265 ) ) ;
#4206=VERTEX_POINT ( 'NONE', #4747 ) ;
#4214=CARTESIAN_POINT ( 'NONE',  ( 8.575906144586951996, -8.109963562772117385, 50.74999885384509923 ) ) ;
#4216=CARTESIAN_POINT ( 'NONE',  ( -19.91159385650551528, -6.922745924619793101, 51.69366785382590024 ) ) ;
#4224=DIRECTION ( 'NONE',  ( 1.000000000000000000, -4.164305804376849172E-17, 1.614929280266638808E-16 ) ) ;
#4234=CARTESIAN_POINT ( 'NONE',  ( -21.26159385759799036, -7.228003583438117552, 51.38655588711986155 ) ) ;
#4249=ORIENTED_EDGE ( 'NONE', *, *, #21501, .T. ) ;
#4262=EDGE_CURVE ( 'NONE', #16853, #24967, #27148, .T. ) ;
#4271=( BOUNDED_CURVE ( )  B_SPLINE_CURVE ( 2, ( #13801, #40180, #6452, #17742, #32772, #29087, #10392, #43403, #19224, #29826, #6920, #44600, #21939, #7920, #14509, #18230, #36940, #15015, #514, #40894, #3225, #29569, #3717, #30567, #22940, #34227, #22429, #26365, #41635, #7424, #37929, #22192, #37422, #33479, #45593, #44854, #11350, #45103, #30326, #284, #10854, #25879, #25628, #18720, #7183, #33238, #31, #15262, #33986, #37177, #3463, #15502, #18472, #48519, #14754, #30079, #11108, #18981, #4216, #26131, #41143, #40642, #33734, #41380, #48278, #7673, #22678, #37679, #3971, #45337, #11590, #26616, #8387, #27338, #23411, #4445, #5424, #35201, #41884, #12316, #38404, #23662, #12561, #761, #31042, #15755, #42121, #1226, #15996, #16721, #12797, #27822, #46056, #34958, #42851, #42367, #12083, #20446, #8640, #20189, #30809, #45826, #31763, #35445, #9119, #16231, #19461, #38664, #24137, #5181, #27583, #31522, #4693, #19956, #4947, #38162, #1469, #16485, #19718, #42621, #27095, #39141, #1729, #31274, #8158, #34727, #23171, #11843, #1000, #34470, #46304, #8882, #26870, #23902, #38902, #46556, #5675, #17459, #16960, #32003, #43341, #47514, #13981, #28558, #29027, #9615, #43586, #5903, #17927, #2200, #32486, #13747, #2682, #21417, #35677, #28790, #9363, #43828, #9845, #47018, #17205, #36401, #6387, #28320, #1959, #40356, #13262, #24629, #39632, #36161, #20921, #40124, #44080, #35923, #32257, #47274, #10080, #17690, #24860 ),
 .UNSPECIFIED., .F., .F. ) 
 B_SPLINE_CURVE_WITH_KNOTS ( ( 3, 2, 2, 2, 2, 2, 2, 2, 2, 2, 2, 2, 2, 2, 2, 2, 2, 2, 2, 2, 2, 2, 2, 2, 2, 2, 2, 2, 2, 2, 2, 2, 2, 2, 2, 2, 2, 2, 2, 2, 2, 2, 2, 2, 2, 2, 2, 2, 2, 2, 2, 2, 2, 2, 2, 2, 2, 2, 2, 2, 2, 2, 2, 2, 2, 2, 2, 2, 2, 2, 2, 2, 2, 2, 2, 2, 2, 2, 2, 2, 2, 2, 2, 2, 2, 2, 2, 2, 2, 3 ),
 ( 0.000000000000000000, 0.01125025289161911933, 0.02250050578323823866, 0.03375075867485735626, 0.04500101156647647732, 0.05625126445809559839, 0.06750151734971471251, 0.07875177024133384052, 0.09000202313295295464, 0.1012522760245720688, 0.1125025289161911968, 0.1237527818078103109, 0.1350030346994294250, 0.1462532875910485530, 0.1575035404826676810, 0.1687537933742867813, 0.1800040462659059093, 0.1912542991575250373, 0.2025045520491441375, 0.2137548049407632655, 0.2250050578323823935, 0.2362553107240014938, 0.2475055636156206218, 0.2587558165072397776, 0.2700060693988588501, 0.2812563222904779781, 0.2925065751820971061, 0.3037568280737162341, 0.3150070809653353621, 0.3262573338569544346, 0.3375075867485735626, 0.3487578396401927461, 0.3600080925318118186, 0.3712583454234309466, 0.3825085983150500746, 0.3937588512066691471, 0.4050091040982882751, 0.4162593569899074586, 0.4275096098815265311, 0.4387598627731456591, 0.4500101156647647871, 0.4612603685563838596, 0.4725106214480029876, 0.4837608743396221711, 0.4950111272312412436, 0.5062613801228603716, 0.5175116330144795551, 0.5287618859060986276, 0.5400121387977177001, 0.5512623916893367726, 0.5625126445809559561, 0.5737628974725751396, 0.5850131503641942121, 0.5962634032558133956, 0.6075136561474324681, 0.6187639090390515406, 0.6300141619306707241, 0.6412644148222897966, 0.6525146677139088691, 0.6637649206055280526, 0.6750151734971471251, 0.6862654263887661976, 0.6975156792803854922, 0.7087659321720045646, 0.7200161850636236371, 0.7312664379552428207, 0.7425166908468618931, 0.7537669437384809656, 0.7650171966301001492, 0.7762674495217192217, 0.7875177024133382941, 0.7987679553049574777, 0.8100182081965765502, 0.8212684610881956226, 0.8325187139798149172, 0.8437689668714339897, 0.8550192197630530622, 0.8662694726546722457, 0.8775197255462913182, 0.8887699784379103907, 0.9000202313295295742, 0.9112704842211486467, 0.9225207371127677192, 0.9337709900043869027, 0.9450212428960059752, 0.9562714957876251587, 0.9675217486792443422, 0.9787720015708634147, 0.9900222544624824872, 1.000000000000000000 ),
 .UNSPECIFIED. ) 
 CURVE ( )  GEOMETRIC_REPRESENTATION_ITEM ( )  RATIONAL_B_SPLINE_CURVE ( ( 1.000000000000000000, 0.9238795325112867385, 1.000000000000000000, 0.9238795325112867385, 1.000000000000000000, 0.9238795325112867385, 1.000000000000000000, 0.9238795325112867385, 1.000000000000000000, 0.9238795325112867385, 1.000000000000000000, 0.9238795325112867385, 1.000000000000000000, 0.9238795325112867385, 1.000000000000000000, 0.9238795325112867385, 1.000000000000000000, 0.9238795325112867385, 1.000000000000000000, 0.9238795325112867385, 1.000000000000000000, 0.9238795325112867385, 1.000000000000000000, 0.9238795325112867385, 1.000000000000000000, 0.9238795325112867385, 1.000000000000000000, 0.9238795325112867385, 1.000000000000000000, 0.9238795325112867385, 1.000000000000000000, 0.9238795325112867385, 1.000000000000000000, 0.9238795325112867385, 1.000000000000000000, 0.9238795325112867385, 1.000000000000000000, 0.9238795325112867385, 1.000000000000000000, 0.9238795325112867385, 1.000000000000000000, 0.9238795325112867385, 1.000000000000000000, 0.9238795325112867385, 1.000000000000000000, 0.9238795325112867385, 1.000000000000000000, 0.9238795325112867385, 1.000000000000000000, 0.9238795325112867385, 1.000000000000000000, 0.9238795325112867385, 1.000000000000000000, 0.9238795325112867385, 1.000000000000000000, 0.9238795325112867385, 1.000000000000000000, 0.9238795325112867385, 1.000000000000000000, 0.9238795325112867385, 1.000000000000000000, 0.9238795325112867385, 1.000000000000000000, 0.9238795325112867385, 1.000000000000000000, 0.9238795325112867385, 1.000000000000000000, 0.9238795325112867385, 1.000000000000000000, 0.9238795325112867385, 1.000000000000000000, 0.9238795325112867385, 1.000000000000000000, 0.9238795325112867385, 1.000000000000000000, 0.9238795325112867385, 1.000000000000000000, 0.9238795325112867385, 1.000000000000000000, 0.9238795325112867385, 1.000000000000000000, 0.9238795325112867385, 1.000000000000000000, 0.9238795325112867385, 1.000000000000000000, 0.9238795325112867385, 1.000000000000000000, 0.9238795325112867385, 1.000000000000000000, 0.9238795325112867385, 1.000000000000000000, 0.9238795325112867385, 1.000000000000000000, 0.9238795325112867385, 1.000000000000000000, 0.9238795325112867385, 1.000000000000000000, 0.9238795325112867385, 1.000000000000000000, 0.9238795325112867385, 1.000000000000000000, 0.9238795325112867385, 1.000000000000000000, 0.9238795325112867385, 1.000000000000000000, 0.9238795325112867385, 1.000000000000000000, 0.9238795325112867385, 1.000000000000000000, 0.9238795325112867385, 1.000000000000000000, 0.9238795325112867385, 1.000000000000000000, 0.9238795325112867385, 1.000000000000000000, 0.9238795325112867385, 1.000000000000000000, 0.9238795325112867385, 1.000000000000000000, 0.9238795325112867385, 1.000000000000000000, 0.9238795325112867385, 1.000000000000000000, 0.9238795325112867385, 1.000000000000000000, 0.9238795325112867385, 1.000000000000000000, 0.9238795325112867385, 1.000000000000000000, 0.9238795325112867385, 1.000000000000000000, 0.9238795325112867385, 1.000000000000000000, 0.9238795325112867385, 1.000000000000000000, 0.9238795325112867385, 1.000000000000000000, 0.9238795325112867385, 1.000000000000000000, 0.9238795325112867385, 1.000000000000000000, 0.9238795325112867385, 1.000000000000000000, 0.9238795325112867385, 1.000000000000000000, 0.9238795325112867385, 1.000000000000000000, 0.9238795325112867385, 1.000000000000000000, 0.9238795325112867385, 1.000000000000000000, 0.9238795325112867385, 1.000000000000000000, 0.9238795325112867385, 1.000000000000000000, 0.9238795325112867385, 1.000000000000000000, 0.9238795325112867385, 1.000000000000000000, 0.9238795325112867385, 1.000000000000000000, 0.9238795325112867385, 1.000000000000000000, 0.9238795325112867385, 1.000000000000000000, 0.9238795325112867385, 1.000000000000000000, 0.9238795325112867385, 1.000000000000000000, 0.9238795325112867385, 1.000000000000000000, 0.9238795325112867385, 1.000000000000000000, 0.9238795325112867385, 1.000000000000000000, 0.9238795325112867385, 1.000000000000000000, 0.9324894593822820044, 0.9847278705211290895 ) ) 
 REPRESENTATION_ITEM ( '' )  );
#4282=CARTESIAN_POINT ( 'NONE',  ( -20.04909385650551457, -8.104110260919579645, 48.81699501597546487 ) ) ;
#4298=CARTESIAN_POINT ( 'NONE',  ( -15.32409385650551670, -6.426201560718813433, 50.50509628382439331 ) ) ;
#4307=CARTESIAN_POINT ( 'NONE',  ( -16.31159385650551386, -6.922745924619793101, 51.69366785382590024 ) ) ;
#4310=CARTESIAN_POINT ( 'NONE',  ( 18.57590614458706924, 1.878297441959757785, 52.28023643296099010 ) ) ;
#4311=CARTESIAN_POINT ( 'NONE',  ( -16.93034385650552309, -9.794322478646142471, 51.19202720610083901 ) ) ;
#4355=CARTESIAN_POINT ( 'NONE',  ( -16.42409385759798823, -9.359200813967568422, 50.49621490985803263 ) ) ;
#4364=CARTESIAN_POINT ( 'NONE',  ( -16.50534385650551883, -8.801233750844183135, 48.81488406609782515 ) ) ;
#4402=DIRECTION ( 'NONE',  ( 1.000000000000000000, -4.164305804376849172E-17, 1.614929280266638808E-16 ) ) ;
#4403=CARTESIAN_POINT ( 'NONE',  ( -20.83659385650551599, -6.915538690918074494, 49.31353937987644542 ) ) ;
#4407=CARTESIAN_POINT ( 'NONE',  ( -14.51159385759799214, -8.990409506049202193, 49.61344411288074951 ) ) ;
#4445=CARTESIAN_POINT ( 'NONE',  ( -18.95534385650551457, -7.417179338643134834, 52.18511593390279302 ) ) ;
#4451=CARTESIAN_POINT ( 'NONE',  ( -16.61784385541296416, -6.860780111192013919, 51.02154966934431002 ) ) ;
#4462=CARTESIAN_POINT ( 'NONE',  ( -21.09284385759799463, -8.630756214087126565, 51.74842643355248129 ) ) ;
#4469=DIRECTION ( 'NONE',  ( 1.000000000000000000, -4.164305804376849788E-17, 1.614929280266638808E-16 ) ) ;
#4477=CIRCLE ( 'NONE', #31997, 1.249999999999999556 ) ;
#4480=CARTESIAN_POINT ( 'NONE',  ( -22.63659385650551670, -6.915538690918074494, 49.31353937987644542 ) ) ;
#4487=CARTESIAN_POINT ( 'NONE',  ( -13.27409385759798965, -6.859212275519751323, 50.50378509014259265 ) ) ;
#4514=CARTESIAN_POINT ( 'NONE',  ( -21.17409385650551812, -9.792211528768504536, 50.49490371617623197 ) ) ;
#4534=CARTESIAN_POINT ( 'NONE',  ( -21.96159385541304232, -7.228003583438117552, 51.38655588711986155 ) ) ;
#4541=VECTOR ( 'NONE', #21937, 1000.000000000000000 ) ;
#4602=CARTESIAN_POINT ( 'NONE',  ( -22.78034385650551741, -6.424090610841176385, 49.80797279389977916 ) ) ;
#4607=CARTESIAN_POINT ( 'NONE',  ( -15.94284385650552238, -8.811426318492348031, 52.18089403414752070 ) ) ;
#4638=EDGE_CURVE ( 'NONE', #43983, #28258, #1687, .T. ) ;
#4650=CARTESIAN_POINT ( 'NONE',  ( -19.23659385759798823, -8.995762431863214559, 51.38120296130585274 ) ) ;
#4652=CIRCLE ( 'NONE', #32171, 1.249999999999999556 ) ;
#4655=CARTESIAN_POINT ( 'NONE',  ( -22.63659385650551670, -6.915538690918074494, 49.31353937987644542 ) ) ;
#4660=AXIS2_PLACEMENT_3D ( 'NONE', #26259, #24868, #37562 ) ;
#4693=CARTESIAN_POINT ( 'NONE',  ( -16.87409385650551386, -9.792211528768504536, 50.49490371617623197 ) ) ;
#4695=CIRCLE ( 'NONE', #3900, 2.000000000000000000 ) ;
#4724=FACE_OUTER_BOUND ( 'NONE', #48658, .T. ) ;
#4733=CARTESIAN_POINT ( 'NONE',  ( -21.96159385650551599, -9.295667164867525756, 49.30633214617472504 ) ) ;
#4741=CARTESIAN_POINT ( 'NONE',  ( -13.44284385759799605, -7.587656875400192291, 49.25157356644813689 ) ) ;
#4747=CARTESIAN_POINT ( 'NONE',  ( 9.825906144586951996, -0.1092432217106413528, 50.52422457691088908 ) ) ;
#4761=VECTOR ( 'NONE', #16697, 1000.000000000000000 ) ;
#4766=CARTESIAN_POINT ( 'NONE',  ( -16.39284385650552167, -7.406986770994972602, 48.81910596585309747 ) ) ;
#4784=EDGE_CURVE ( 'NONE', #29774, #45804, #17765, .T. ) ;
#4791=CARTESIAN_POINT ( 'NONE',  ( -21.17409385541304445, -6.859212275519751323, 50.50378509014259265 ) ) ;
#4813=CARTESIAN_POINT ( 'NONE',  ( -19.79909385759798823, -8.105421454601382081, 49.25000573077640098 ) ) ;
#4820=CARTESIAN_POINT ( 'NONE',  ( -36.42409385541304800, -8.109206544743658540, 50.50000000000030553 ) ) ;
#4854=CARTESIAN_POINT ( 'NONE',  ( -21.65534385650552096, -7.417179338643134834, 52.18511593390279302 ) ) ;
#4855=AXIS2_PLACEMENT_3D ( 'NONE', #12623, #574, #8704 ) ;
#4862=CARTESIAN_POINT ( 'NONE',  ( -13.13034385650551883, -9.794322478646142471, 51.19202720610083901 ) ) ;
#4867=CARTESIAN_POINT ( 'NONE',  ( 10.57590614458695377, 3.116243883476756515, 50.28399048308536123 ) ) ;
#4888=CARTESIAN_POINT ( 'NONE',  ( -13.36114594230879504, -9.147054927169216754, 49.62380229257679076 ) ) ;
#4898=CARTESIAN_POINT ( 'NONE',  ( 23.62590614458706639, 3.790747609047893540, 50.53028072113869484 ) ) ;
#4906=CARTESIAN_POINT ( 'NONE',  ( -12.77466918460613599, -9.357823218138582533, 50.04127544294632912 ) ) ;
#4912=ORIENTED_EDGE ( 'NONE', *, *, #41674, .T. ) ;
#4916=SHAPE_REPRESENTATION_RELATIONSHIP ( 'NONE' , 'NONE' ,  #34550, #44394 ) ;
#4925=DIRECTION ( 'NONE',  ( 1.000000000000000000, -4.164305804376849172E-17, 1.614929280266638808E-16 ) ) ;
#4927=CARTESIAN_POINT ( 'NONE',  ( -36.42409385541304800, -8.109206544743658540, 50.50000000000030553 ) ) ;
#4929=EDGE_CURVE ( 'NONE', #29888, #11159, #37004, .T. ) ;
#4941=VERTEX_POINT ( 'NONE', #43463 ) ;
#4947=CARTESIAN_POINT ( 'NONE',  ( -16.76159385650551314, -9.295667164867525756, 49.30633214617472504 ) ) ;
#4956=CYLINDRICAL_SURFACE ( 'NONE', #31368, 2.000000000000001776 ) ;
#4965=CARTESIAN_POINT ( 'NONE',  ( -21.03659385759798894, -8.995762431863214559, 51.38120296130585274 ) ) ;
#4980=CARTESIAN_POINT ( 'NONE',  ( -21.73659385650551812, -6.915538690918074494, 49.31353937987644542 ) ) ;
#4989=ADVANCED_FACE ( 'NONE', ( #14338 ), #7735, .T. ) ;
#4991=ORIENTED_EDGE ( 'NONE', *, *, #7776, .T. ) ;
#5002=CARTESIAN_POINT ( 'NONE',  ( 9.825906144586950219, -6.109215713985405749, 50.50605614422795497 ) ) ;
#5014=CARTESIAN_POINT ( 'NONE',  ( -17.79909385650551812, -8.114302828567740988, 52.18300498402516041 ) ) ;
#5033=DIRECTION ( 'NONE',  ( 1.616182858256118536E-16, 0.003028072113822188795, -0.9999954153791273948 ) ) ;
#5035=EDGE_LOOP ( 'NONE', ( #37757, #22593, #27606, #40868 ) ) ;
#5037=CARTESIAN_POINT ( 'NONE',  ( -20.21784385541304374, -6.860780111191487229, 51.02154966934377001 ) ) ;
#5048=PLANE ( 'NONE',  #11789 ) ;
#5052=EDGE_CURVE ( 'NONE', #33382, #17990, #3526, .T. ) ;
#5058=AXIS2_PLACEMENT_3D ( 'NONE', #37749, #38224, #34053 ) ;
#5093=CARTESIAN_POINT ( 'NONE',  ( -22.94909385650551314, -8.104110260919577868, 48.81699501597546487 ) ) ;
#5100=CARTESIAN_POINT ( 'NONE',  ( -21.20534385650551812, -8.801233750844183135, 48.81488406609782515 ) ) ;
#5143=CARTESIAN_POINT ( 'NONE',  ( -13.33034385759799001, -6.857644439848014528, 49.98602051094140819 ) ) ;
#5181=CARTESIAN_POINT ( 'NONE',  ( -17.04284385650551670, -8.811426318492348031, 52.18089403414751359 ) ) ;
#5191=CARTESIAN_POINT ( 'NONE',  ( -15.32409385541304481, -9.359200813967568422, 50.49621490985804684 ) ) ;
#5201=CARTESIAN_POINT ( 'NONE',  ( -21.65534385759799463, -8.623186033802570094, 49.24843789510466507 ) ) ;
#5223=CYLINDRICAL_SURFACE ( 'NONE', #30433, 1.249999999999998668 ) ;
#5229=ORIENTED_EDGE ( 'NONE', *, *, #47231, .F. ) ;
#5248=CARTESIAN_POINT ( 'NONE',  ( -17.34909385650551883, -8.104110260919579645, 48.81699501597546487 ) ) ;
#5250=CARTESIAN_POINT ( 'NONE',  ( 23.52590614458706852, -0.1092523909521068148, 50.53028072113869484 ) ) ;
#5272=DIRECTION ( 'NONE',  ( 1.000000000000000000, -4.164305804376849172E-17, 1.614929280266638808E-16 ) ) ;
#5277=CARTESIAN_POINT ( 'NONE',  ( -22.01784385541304090, -6.860780111191487229, 51.02154966934377001 ) ) ;
#5313=ORIENTED_EDGE ( 'NONE', *, *, #32512, .F. ) ;
#5332=EDGE_LOOP ( 'NONE', ( #8379, #14604, #44261, #14559 ) ) ;
#5335=CARTESIAN_POINT ( 'NONE',  ( -20.53034385650551386, -9.794322478646142471, 51.19202720610083901 ) ) ;
#5340=CARTESIAN_POINT ( 'NONE',  ( -22.89284385650552522, -7.406986770994973490, 48.81910596585309747 ) ) ;
#5380=EDGE_CURVE ( 'NONE', #32441, #17998, #4271, .T. ) ;
#5386=CARTESIAN_POINT ( 'NONE',  ( -19.76784385650551812, -6.428312510596451368, 51.20221977374900035 ) ) ;
#5395=LINE ( 'NONE', #1697, #4761 ) ;
#5415=CARTESIAN_POINT ( 'NONE',  ( -22.61159385759798823, -8.990409506049200417, 49.61344411288074951 ) ) ;
#5424=CARTESIAN_POINT ( 'NONE',  ( -18.89909385650551599, -8.114302828567740988, 52.18300498402516041 ) ) ;
#5449=CARTESIAN_POINT ( 'NONE',  ( -18.61784385759799321, -6.860780111191487229, 51.02154966934377001 ) ) ;
#5486=ORIENTED_EDGE ( 'NONE', *, *, #8390, .T. ) ;
#5495=ORIENTED_EDGE ( 'NONE', *, *, #21366, .T. ) ;
#5501=CARTESIAN_POINT ( 'NONE',  ( -15.66159385650551705, -9.295667164867525756, 49.30633214617472504 ) ) ;
#5505=DIRECTION ( 'NONE',  ( 0.000000000000000000, -0.9999954153791273948, -0.003028072113822395228 ) ) ;
#5508=CARTESIAN_POINT ( 'NONE',  ( -18.69909385541303948, -8.105421454601382081, 49.25000573077639388 ) ) ;
#5510=ORIENTED_EDGE ( 'NONE', *, *, #41529, .F. ) ;
#5523=EDGE_LOOP ( 'NONE', ( #45948, #47271, #14932, #671 ) ) ;
#5525=CARTESIAN_POINT ( 'NONE',  ( -22.07409385541304303, -6.859212275519751323, 50.50378509014259265 ) ) ;
#5565=CARTESIAN_POINT ( 'NONE',  ( 18.54465614458695200, 3.140741878271521070, 50.53406581128081143 ) ) ;
#5573=ADVANCED_FACE ( 'NONE', ( #15698 ), #706, .F. ) ;
#5583=ORIENTED_EDGE ( 'NONE', *, *, #29523, .T. ) ;
#5585=CARTESIAN_POINT ( 'NONE',  ( -22.66784385650551670, -6.428312510596451368, 51.20221977374900035 ) ) ;
#5590=CARTESIAN_POINT ( 'NONE',  ( -23.06159385650551386, -9.295667164867525756, 49.30633214617472504 ) ) ;
#5591=( BOUNDED_CURVE ( )  B_SPLINE_CURVE ( 2, ( #29366, #34019, #19015, #26402, #29608, #66, #36972, #15054, #41177 ),
 .UNSPECIFIED., .F., .F. ) 
 B_SPLINE_CURVE_WITH_KNOTS ( ( 3, 2, 2, 2, 3 ),
 ( 0.01573617513994363115, 0.01671960456604025536, 0.01770303399213687956, 0.01868646341823350029, 0.01966989284433012450 ),
 .UNSPECIFIED. ) 
 CURVE ( )  GEOMETRIC_REPRESENTATION_ITEM ( )  RATIONAL_B_SPLINE_CURVE ( ( 1.000000000000510925, 0.9238795325107758138, 1.000000000000000000, 0.9238795325112867385, 1.000000000000000000, 0.9238795325112867385, 1.000000000000000000, 0.9238795325112530987, 1.000000000000033751 ) ) 
 REPRESENTATION_ITEM ( '' )  );
#5639=CARTESIAN_POINT ( 'NONE',  ( -17.01159385650551670, -6.922745924619793101, 51.69366785382590024 ) ) ;
#5644=ORIENTED_EDGE ( 'NONE', *, *, #48391, .T. ) ;
#5656=AXIS2_PLACEMENT_3D ( 'NONE', #42603, #23881, #35424 ) ;
#5660=ADVANCED_FACE ( 'NONE', ( #2629 ), #13693, .T. ) ;
#5669=CARTESIAN_POINT ( 'NONE',  ( -14.96159385759799143, -7.228003583438117552, 51.38655588711986155 ) ) ;
#5673=CARTESIAN_POINT ( 'NONE',  ( -15.77409385541301035, -6.859212275519753099, 50.50378509014291240 ) ) ;
#5675=CARTESIAN_POINT ( 'NONE',  ( -15.52409385650551421, -6.426201560718813433, 50.50509628382439331 ) ) ;
#5695=CARTESIAN_POINT ( 'NONE',  ( -18.50534385759798894, -7.595227055684746986, 51.75156210489594599 ) ) ;
#5701=FACE_OUTER_BOUND ( 'NONE', #44006, .T. ) ;
#5721=ORIENTED_EDGE ( 'NONE', *, *, #37434, .F. ) ;
#5740=PLANE ( 'NONE',  #46708 ) ;
#5747=CARTESIAN_POINT ( 'NONE',  ( -15.15534385650551741, -7.417179338643134834, 52.18511593390279302 ) ) ;
#5751=ORIENTED_EDGE ( 'NONE', *, *, #1575, .T. ) ;
#5762=CARTESIAN_POINT ( 'NONE',  ( -22.07409385541323488, -6.859212275519745994, 50.50378509014079498 ) ) ;
#5770=CARTESIAN_POINT ( 'NONE',  ( -16.56159385541304019, -7.228003583438117552, 51.38655588711986155 ) ) ;
#5772=AXIS2_PLACEMENT_3D ( 'NONE', #34575, #1096, #38517 ) ;
#5805=EDGE_CURVE ( 'NONE', #26444, #45257, #32114, .T. ) ;
#5812=ORIENTED_EDGE ( 'NONE', *, *, #31229, .F. ) ;
#5821=CARTESIAN_POINT ( 'NONE',  ( -18.16784385650552025, -6.428312510596451368, 51.20221977374900035 ) ) ;
#5822=EDGE_CURVE ( 'NONE', #43599, #47374, #40781, .T. ) ;
#5825=CARTESIAN_POINT ( 'NONE',  ( -21.09284385650551741, -7.406986770994973490, 48.81910596585309747 ) ) ;
#5837=ORIENTED_EDGE ( 'NONE', *, *, #4262, .F. ) ;
#5839=DIRECTION ( 'NONE',  ( -1.000000000000000000, 4.164305804376849172E-17, -1.614929280266638808E-16 ) ) ;
#5847=EDGE_CURVE ( 'NONE', #15076, #11000, #36576, .T. ) ;
#5851=CARTESIAN_POINT ( 'NONE',  ( -36.42409385541304800, -8.109206544743658540, 50.50000000000030553 ) ) ;
#5864=LINE ( 'NONE', #39349, #24141 ) ;
#5866=CARTESIAN_POINT ( 'NONE',  ( -17.46159385650551599, -9.295667164867525756, 49.30633214617472504 ) ) ;
#5875=ORIENTED_EDGE ( 'NONE', *, *, #22439, .F. ) ;
#5903=CARTESIAN_POINT ( 'NONE',  ( -14.90534385650551918, -8.801233750844183135, 48.81488406609782515 ) ) ;
#5918=ORIENTED_EDGE ( 'NONE', *, *, #41490, .T. ) ;
#5921=CARTESIAN_POINT ( 'NONE',  ( -18.78659385759798894, -7.222650657624104298, 49.61879703869476543 ) ) ;
#5968=CARTESIAN_POINT ( 'NONE',  ( -14.03034385650551563, -9.794322478646142471, 51.19202720610083190 ) ) ;
#5995=CARTESIAN_POINT ( 'NONE',  ( -17.85534385541304303, -8.623186033802570094, 49.24843789510466507 ) ) ;
#6008=FACE_OUTER_BOUND ( 'NONE', #9653, .T. ) ;
#6044=ORIENTED_EDGE ( 'NONE', *, *, #1616, .F. ) ;
#6045=CARTESIAN_POINT ( 'NONE',  ( -20.19284385650551528, -7.406986770994973490, 48.81910596585309747 ) ) ;
#6050=CARTESIAN_POINT ( 'NONE',  ( -17.54909385650551812, -8.104110260919579645, 48.81699501597546487 ) ) ;
#6069=CARTESIAN_POINT ( 'NONE',  ( -17.01159385541303593, -8.990409506049202193, 49.61344411288074951 ) ) ;
#6089=EDGE_LOOP ( 'NONE', ( #8115, #16826, #33797, #30175 ) ) ;
#6098=AXIS2_PLACEMENT_3D ( 'NONE', #35627, #43027, #47688 ) ;
#6099=CARTESIAN_POINT ( 'NONE',  ( -17.74284385650551599, -8.811426318492348031, 52.18089403414751359 ) ) ;
#6114=CARTESIAN_POINT ( 'NONE',  ( -20.44284385650551883, -8.811426318492348031, 52.18089403414751359 ) ) ;
#6116=EDGE_CURVE ( 'NONE', #38445, #41647, #11120, .T. ) ;
#6119=APPLICATION_CONTEXT ( 'automotive_design' ) ;
#6131=ADVANCED_FACE ( 'NONE', ( #44863 ), #11851, .T. ) ;
#6160=ORIENTED_EDGE ( 'NONE', *, *, #9830, .F. ) ;
#6162=CARTESIAN_POINT ( 'NONE',  ( -20.19284385759799605, -8.630756214087126565, 51.74842643355248129 ) ) ;
#6193=ORIENTED_EDGE ( 'NONE', *, *, #28020, .T. ) ;
#6215=CARTESIAN_POINT ( 'NONE',  ( -13.07409385650551847, -9.792211528768506312, 50.49490371617623197 ) ) ;
#6224=CARTESIAN_POINT ( 'NONE',  ( -18.86784385541312048, -9.357632978296351212, 49.97845033065735265 ) ) ;
#6238=( BOUNDED_CURVE ( )  B_SPLINE_CURVE ( 2, ( #12223, #906, #39721, #34620, #8790, #47602, #38807, #23806, #2289 ),
 .UNSPECIFIED., .F., .F. ) 
 B_SPLINE_CURVE_WITH_KNOTS ( ( 3, 2, 2, 2, 3 ),
 ( 0.01180254302363409509, 0.01278595105271147780, 0.01376935908178886399, 0.01475276711086624844, 0.01573617513994363115 ),
 .UNSPECIFIED. ) 
 CURVE ( )  GEOMETRIC_REPRESENTATION_ITEM ( )  RATIONAL_B_SPLINE_CURVE ( ( 0.9999999999995410338, 0.9238795325117457047, 1.000000000000000000, 0.9238795325112867385, 1.000000000000000000, 0.9238795325112867385, 1.000000000000000000, 0.9238795325117954427, 0.9999999999994912958 ) ) 
 REPRESENTATION_ITEM ( '' )  );
#6248=CARTESIAN_POINT ( 'NONE',  ( -17.63034385541304516, -6.857644439848013640, 49.98602051094139398 ) ) ;
#6275=EDGE_CURVE ( 'NONE', #29888, #12705, #23476, .T. ) ;
#6296=CARTESIAN_POINT ( 'NONE',  ( -17.94284385650551528, -8.811426318492348031, 52.18089403414751359 ) ) ;
#6302=CARTESIAN_POINT ( 'NONE',  ( -17.94284385650551528, -8.811426318492348031, 52.18089403414751359 ) ) ;
#6332=ORIENTED_EDGE ( 'NONE', *, *, #38775, .F. ) ;
#6334=EDGE_CURVE ( 'NONE', #3912, #42266, #29142, .T. ) ;
#6341=ORIENTED_EDGE ( 'NONE', *, *, #22179, .F. ) ;
#6354=ORIENTED_EDGE ( 'NONE', *, *, #38850, .F. ) ;
#6361=CARTESIAN_POINT ( 'NONE',  ( -19.03659385650551528, -6.915538690918074494, 49.31353937987644542 ) ) ;
#6387=CARTESIAN_POINT ( 'NONE',  ( -14.06159385650551741, -9.295667164867525756, 49.30633214617472504 ) ) ;
#6402=DIRECTION ( 'NONE',  ( -1.000000000000000000, 4.164305804376849172E-17, -1.614929280266638808E-16 ) ) ;
#6407=CARTESIAN_POINT ( 'NONE',  ( -19.68659385759799108, -7.222650657624104298, 49.61879703869476543 ) ) ;
#6424=ADVANCED_FACE ( 'NONE', ( #38091 ), #41073, .T. ) ;
#6436=VECTOR ( 'NONE', #23331, 1000.000000000000000 ) ;
#6448=CARTESIAN_POINT ( 'NONE',  ( -18.67409385759799179, -6.859212275519751323, 50.50378509014259265 ) ) ;
#6450=ORIENTED_EDGE ( 'NONE', *, *, #25084, .F. ) ;
#6452=CARTESIAN_POINT ( 'NONE',  ( -23.06159385650551386, -9.295667164867525756, 49.30633214617472504 ) ) ;
#6454=CARTESIAN_POINT ( 'NONE',  ( -14.17409385759798823, -6.859212275519751323, 50.50378509014259265 ) ) ;
#6472=CARTESIAN_POINT ( 'NONE',  ( -18.58659385541303521, -7.222650657624098969, 49.61879703869476543 ) ) ;
#6480=ORIENTED_EDGE ( 'NONE', *, *, #20116, .T. ) ;
#6490=CARTESIAN_POINT ( 'NONE',  ( -17.01159385541303948, -8.990409506049200417, 49.61344411288074951 ) ) ;
#6497=CARTESIAN_POINT ( 'NONE',  ( -20.41784385759799036, -6.860780111191480124, 51.02154966934376290 ) ) ;
#6541=CARTESIAN_POINT ( 'NONE',  ( -17.26784385650551457, -6.428312510596451368, 51.20221977374900035 ) ) ;
#6542=EDGE_CURVE ( 'NONE', #10524, #26883, #43151, .T. ) ;
#6543=CARTESIAN_POINT ( 'NONE',  ( 18.07590614458695200, 2.989985547936196753, 50.78361045430852982 ) ) ;
#6545=CARTESIAN_POINT ( 'NONE',  ( -18.05534385650551599, -7.417179338643134834, 52.18511593390279302 ) ) ;
#6552=EDGE_CURVE ( 'NONE', #29515, #16353, #34452, .T. ) ;
#6557=CARTESIAN_POINT ( 'NONE',  ( -19.37409385541300111, -6.859212275519753099, 50.50378509014300477 ) ) ;
#6578=ORIENTED_EDGE ( 'NONE', *, *, #19366, .F. ) ;
#6604=ORIENTED_EDGE ( 'NONE', *, *, #26674, .T. ) ;
#6605=CARTESIAN_POINT ( 'NONE',  ( -18.13659385650551670, -6.915538690918074494, 49.31353937987644542 ) ) ;
#6626=ORIENTED_EDGE ( 'NONE', *, *, #31229, .T. ) ;
#6633=CARTESIAN_POINT ( 'NONE',  ( 18.07590614458695200, 0.7899956341021162620, 50.77694869565811331 ) ) ;
#6644=CARTESIAN_POINT ( 'NONE',  ( -14.84909385759799072, -8.112991634885936776, 51.74999426922421719 ) ) ;
#6691=VECTOR ( 'NONE', #45489, 1000.000000000000000 ) ;
#6699=DIRECTION ( 'NONE',  ( 0.000000000000000000, 1.000000000000000000, 0.000000000000000000 ) ) ;
#6723=CARTESIAN_POINT ( 'NONE',  ( -18.64284385541304445, -7.587656875400192291, 49.25157356644813689 ) ) ;
#6724=ORIENTED_EDGE ( 'NONE', *, *, #5822, .F. ) ;
#6734=EDGE_CURVE ( 'NONE', #8229, #33983, #36028, .T. ) ;
#6741=VERTEX_POINT ( 'NONE', #12196 ) ;
#6752=DIRECTION ( 'NONE',  ( 1.000000000000000000, 0.000000000000000000, 0.000000000000000000 ) ) ;
#6758=CARTESIAN_POINT ( 'NONE',  ( -22.24284385650551954, -8.811426318492348031, 52.18089403414751359 ) ) ;
#6764=FACE_OUTER_BOUND ( 'NONE', #35682, .T. ) ;
#6767=CARTESIAN_POINT ( 'NONE',  ( -17.57409385541300395, -6.859212275519753099, 50.50378509014294792 ) ) ;
#6777=CARTESIAN_POINT ( 'NONE',  ( -16.98659385650551812, -9.302874398569244363, 51.68646062012417985 ) ) ;
#6782=CARTESIAN_POINT ( 'NONE',  ( -17.83034385650551457, -9.794322478646142471, 51.19202720610083901 ) ) ;
#6823=ORIENTED_EDGE ( 'NONE', *, *, #7776, .F. ) ;
#6842=CARTESIAN_POINT ( 'NONE',  ( -17.85534385650552025, -7.417179338643134834, 52.18511593390279302 ) ) ;
#6857=ORIENTED_EDGE ( 'NONE', *, *, #3068, .F. ) ;
#6861=AXIS2_PLACEMENT_3D ( 'NONE', #32934, #47976, #36149 ) ;
#6867=DIRECTION ( 'NONE',  ( -1.616182858256117057E-16, -0.003028072113818697231, 0.9999954153791273948 ) ) ;
#6885=CARTESIAN_POINT ( 'NONE',  ( -15.07409385759798859, -6.859212275519751323, 50.50378509014259265 ) ) ;
#6893=AXIS2_PLACEMENT_3D ( 'NONE', #20975, #32308, #7178 ) ;
#6898=CYLINDRICAL_SURFACE ( 'NONE', #41419, 1.049999999999998934 ) ;
#6920=CARTESIAN_POINT ( 'NONE',  ( -22.61159385650551457, -6.922745924619793101, 51.69366785382590024 ) ) ;
#6935=CARTESIAN_POINT ( 'NONE',  ( -14.14284385650552167, -8.811426318492348031, 52.18089403414752070 ) ) ;
#6941=ORIENTED_EDGE ( 'NONE', *, *, #13388, .T. ) ;
#6953=CARTESIAN_POINT ( 'NONE',  ( 18.46573386768564973, 2.137037847100790255, 51.75577699556767897 ) ) ;
#6965=CARTESIAN_POINT ( 'NONE',  ( -15.09909385541304339, -8.105421454601382081, 49.25000573077640098 ) ) ;
#6996=CARTESIAN_POINT ( 'NONE',  ( -22.74909385650551386, -8.104110260919577868, 48.81699501597546487 ) ) ;
#7015=CARTESIAN_POINT ( 'NONE',  ( -13.86159385650551812, -9.295667164867525756, 49.30633214617472504 ) ) ;
#7025=ORIENTED_EDGE ( 'NONE', *, *, #41170, .T. ) ;
#7026=CARTESIAN_POINT ( 'NONE',  ( -16.08659385650551599, -9.302874398569244363, 51.68646062012417985 ) ) ;
#7029=CARTESIAN_POINT ( 'NONE',  ( -19.96784385650551741, -6.428312510596451368, 51.20221977374900035 ) ) ;
#7049=CARTESIAN_POINT ( 'NONE',  ( -22.44284385759798894, -7.587656875400192291, 49.25157356644813689 ) ) ;
#7096=CARTESIAN_POINT ( 'NONE',  ( -20.89284385650552167, -7.406986770994973490, 48.81910596585309747 ) ) ;
#7139=CARTESIAN_POINT ( 'NONE',  ( -14.68034385759798965, -9.360768649639302552, 51.01397948905922419 ) ) ;
#7142=CARTESIAN_POINT ( 'NONE',  ( -14.45534385759799179, -8.623186033802571870, 49.24843789510467218 ) ) ;
#7147=AXIS2_PLACEMENT_3D ( 'NONE', #47276, #17930, #29030 ) ;
#7152=ORIENTED_EDGE ( 'NONE', *, *, #37434, .T. ) ;
#7154=ADVANCED_FACE ( 'NONE', ( #15821 ), #7773, .T. ) ;
#7155=CARTESIAN_POINT ( 'NONE',  ( -36.42409385541304800, -8.109206544743658540, 50.50000000000030553 ) ) ;
#7165=LINE ( 'NONE', #13552, #29643 ) ;
#7166=CIRCLE ( 'NONE', #13433, 1.949999999999999956 ) ;
#7169=CARTESIAN_POINT ( 'NONE',  ( -35.42409385541304800, -6.859212275519750435, 50.50378509014258555 ) ) ;
#7170=CARTESIAN_POINT ( 'NONE',  ( -13.27409385759798965, -6.859212275519751323, 50.50378509014259265 ) ) ;
#7178=DIRECTION ( 'NONE',  ( -1.669677910507523057E-21, 1.000000000000000000, 0.000000000000000000 ) ) ;
#7183=CARTESIAN_POINT ( 'NONE',  ( -20.69909385650551670, -8.114302828567740988, 52.18300498402516041 ) ) ;
#7203=CARTESIAN_POINT ( 'NONE',  ( -13.17364361214796098, -9.395187332399693503, 49.41428126932424192 ) ) ;
#7222=CARTESIAN_POINT ( 'NONE',  ( -13.42364594203567307, -9.064338107776409359, 49.69363550592916567 ) ) ;
#7236=EDGE_CURVE ( 'NONE', #12395, #32426, #42388, .T. ) ;
#7238=CARTESIAN_POINT ( 'NONE',  ( -19.12409385759799108, -9.359200813967568422, 50.49621490985803263 ) ) ;
#7239=DIRECTION ( 'NONE',  ( 4.115385489419834812E-17, 0.9999954153791273948, 0.003028072113822188795 ) ) ;
#7256=CARTESIAN_POINT ( 'NONE',  ( -19.65534385650552451, -7.417179338643134834, 52.18511593390279302 ) ) ;
#7259=AXIS2_PLACEMENT_3D ( 'NONE', #34312, #18563, #45191 ) ;
#7264=CARTESIAN_POINT ( 'NONE',  ( -21.37409385759799108, -6.859212275519751323, 50.50378509014259265 ) ) ;
#7268=CARTESIAN_POINT ( 'NONE',  ( -17.91159385541293858, -8.990409506049328314, 49.61344411288062162 ) ) ;
#7271=ORIENTED_EDGE ( 'NONE', *, *, #29716, .F. ) ;
#7272=CARTESIAN_POINT ( 'NONE',  ( -14.76159385650551847, -9.295667164867525756, 49.30633214617472504 ) ) ;
#7274=DIRECTION ( 'NONE',  ( 6.374839753205896285E-22, 0.007114381193220334181, -0.9999746924698833528 ) ) ;
#7280=CARTESIAN_POINT ( 'NONE',  ( -14.28659385650551528, -9.302874398569244363, 51.68646062012417985 ) ) ;
#7284=CARTESIAN_POINT ( 'NONE',  ( -14.84909385650551705, -8.104110260919579645, 48.81699501597546487 ) ) ;
#7348=CARTESIAN_POINT ( 'NONE',  ( -17.06784385650551528, -6.428312510596451368, 51.20221977374900035 ) ) ;
#7356=DIRECTION ( 'NONE',  ( 1.000000000000000000, 1.669677910507523057E-21, 6.493791346278465266E-22 ) ) ;
#7367=DIRECTION ( 'NONE',  ( 0.000000000000000000, -0.9999954153791273948, -0.003028072113819838245 ) ) ;
#7389=CARTESIAN_POINT ( 'NONE',  ( 18.62590614458706995, 1.890747609047893185, 50.53028072113869484 ) ) ;
#7390=CARTESIAN_POINT ( 'NONE',  ( -16.87409385759798752, -6.859212275519751323, 50.50378509014259265 ) ) ;
#7393=CARTESIAN_POINT ( 'NONE',  ( -36.42409385541304800, -8.109206544743658540, 50.50000000000030553 ) ) ;
#7401=EDGE_CURVE ( 'NONE', #42690, #24436, #35144, .T. ) ;
#7403=PRESENTATION_STYLE_ASSIGNMENT (( #30057 ) ) ;
#7424=CARTESIAN_POINT ( 'NONE',  ( -21.54284385650551314, -8.811426318492348031, 52.18089403414751359 ) ) ;
#7445=CYLINDRICAL_SURFACE ( 'NONE', #23200, 1.249999999999998668 ) ;
#7454=LINE ( 'NONE', #30105, #19677 ) ;
#7465=CARTESIAN_POINT ( 'NONE',  ( -36.42409385541304800, -8.109206544743658540, 50.50000000000030553 ) ) ;
#7470=CARTESIAN_POINT ( 'NONE',  ( -15.43659385541304019, -8.995762431863214559, 51.38120296130585274 ) ) ;
#7474=CARTESIAN_POINT ( 'NONE',  ( -15.80534385759798788, -7.595227055684746986, 51.75156210489594599 ) ) ;
#7484=VECTOR ( 'NONE', #16025, 1000.000000000000000 ) ;
#7500=CARTESIAN_POINT ( 'NONE',  ( -19.09284385650552096, -7.406986770994972602, 48.81910596585309747 ) ) ;
#7512=CARTESIAN_POINT ( 'NONE',  ( -13.07409385650551847, -9.792211528768506312, 50.49490371617623197 ) ) ;
#7519=ORIENTED_EDGE ( 'NONE', *, *, #37454, .T. ) ;
#7522=CARTESIAN_POINT ( 'NONE',  ( -15.46784385650551918, -6.428312510596451368, 51.20221977374900035 ) ) ;
#7526=ADVANCED_FACE ( 'NONE', ( #39815 ), #35864, .T. ) ;
#7527=CARTESIAN_POINT ( 'NONE',  ( -16.03034385650551386, -9.794322478646142471, 51.19202720610083901 ) ) ;
#7537=CARTESIAN_POINT ( 'NONE',  ( -17.46159385541293929, -7.228003583437990542, 51.38655588711998945 ) ) ;
#7552=CARTESIAN_POINT ( 'NONE',  ( 18.62590614458706995, 1.890747609047893185, 50.53028072113869484 ) ) ;
#7576=CARTESIAN_POINT ( 'NONE',  ( -13.42364920204782841, -9.064338107659910548, 49.69363550579117117 ) ) ;
#7577=ORIENTED_EDGE ( 'NONE', *, *, #45036, .F. ) ;
#7589=CARTESIAN_POINT ( 'NONE',  ( -13.97409385650551528, -9.792211528768506312, 50.49490371617623197 ) ) ;
#7594=LINE ( 'NONE', #41556, #44210 ) ;
#7626=AXIS2_PLACEMENT_3D ( 'NONE', #43060, #27797, #13008 ) ;
#7635=CARTESIAN_POINT ( 'NONE',  ( -13.72409385759798894, -9.359200813967568422, 50.49621490985803263 ) ) ;
#7662=CARTESIAN_POINT ( 'NONE',  ( 18.07590614458695200, 2.989985547936196753, 50.78361045430852982 ) ) ;
#7673=CARTESIAN_POINT ( 'NONE',  ( -19.51784385650551457, -9.790100578890868377, 49.79778022625163203 ) ) ;
#7675=CARTESIAN_POINT ( 'NONE',  ( 18.07590614458695200, 2.991499583993109113, 50.28361274661895663 ) ) ;
#7712=CARTESIAN_POINT ( 'NONE',  ( -15.52409385759799143, -9.359200813967568422, 50.49621490985803263 ) ) ;
#7715=EDGE_CURVE ( 'NONE', #3256, #20955, #11175, .T. ) ;
#7735=CYLINDRICAL_SURFACE ( 'NONE', #616, 1.249999999999998668 ) ;
#7748=CARTESIAN_POINT ( 'NONE',  ( -18.53034385650551741, -9.794322478646142471, 51.19202720610083190 ) ) ;
#7756=ORIENTED_EDGE ( 'NONE', *, *, #13686, .T. ) ;
#7762=CARTESIAN_POINT ( 'NONE',  ( -15.77409385650551954, -9.792211528768504536, 50.49490371617623197 ) ) ;
#7771=CARTESIAN_POINT ( 'NONE',  ( -15.97409385650551705, -9.792211528768504536, 50.49490371617623197 ) ) ;
#7773=TOROIDAL_SURFACE ( 'NONE', #26639, 1.750000000000000000, 0.2500000000000000000 ) ;
#7774=CARTESIAN_POINT ( 'NONE',  ( -16.31159385650551386, -6.922745924619793101, 51.69366785382590024 ) ) ;
#7776=EDGE_CURVE ( 'NONE', #16419, #42266, #1118, .T. ) ;
#7797=VERTEX_POINT ( 'NONE', #20080 ) ;
#7831=CARTESIAN_POINT ( 'NONE',  ( 22.62590614458706639, 1.890747609047612077, 50.53028072113853142 ) ) ;
#7836=CARTESIAN_POINT ( 'NONE',  ( -15.38034385650552061, -6.424090610841176385, 49.80797279389977916 ) ) ;
#7844=ORIENTED_EDGE ( 'NONE', *, *, #38942, .F. ) ;
#7860=ORIENTED_EDGE ( 'NONE', *, *, #6734, .T. ) ;
#7879=CARTESIAN_POINT ( 'NONE',  ( -22.46784385650551741, -6.428312510596450480, 51.20221977374900035 ) ) ;
#7890=( BOUNDED_CURVE ( )  B_SPLINE_CURVE ( 2, ( #3976, #18731, #33742, #38, #18990, #33992, #291, #26624, #15269 ),
 .UNSPECIFIED., .F., .F. ) 
 B_SPLINE_CURVE_WITH_KNOTS ( ( 3, 2, 2, 2, 3 ),
 ( 0.007868113086928890665, 0.008851720571105191337, 0.009835328055281493745, 0.01081893553945779268, 0.01180254302363409509 ),
 .UNSPECIFIED. ) 
 CURVE ( )  GEOMETRIC_REPRESENTATION_ITEM ( )  RATIONAL_B_SPLINE_CURVE ( ( 0.9999999999977363663, 0.9238795325135503722, 1.000000000000000000, 0.9238795325112867385, 1.000000000000000000, 0.9238795325112867385, 1.000000000000000000, 0.9238795325108279943, 1.000000000000458744 ) ) 
 REPRESENTATION_ITEM ( '' )  );
#7892=ORIENTED_EDGE ( 'NONE', *, *, #698, .T. ) ;
#7894=( NAMED_UNIT ( * ) SI_UNIT ( $, .STERADIAN. ) SOLID_ANGLE_UNIT ( ) );
#7913=ORIENTED_EDGE ( 'NONE', *, *, #34422, .T. ) ;
#7914=CARTESIAN_POINT ( 'NONE',  ( -17.21159385759798965, -8.990409506049200417, 49.61344411288074951 ) ) ;
#7915=EDGE_CURVE ( 'NONE', #15477, #39727, #23833, .T. ) ;
#7920=CARTESIAN_POINT ( 'NONE',  ( -22.44284385650551528, -8.811426318492348031, 52.18089403414751359 ) ) ;
#7940=CARTESIAN_POINT ( 'NONE',  ( -21.88034385759799250, -9.360768649639302552, 51.01397948905921709 ) ) ;
#7956=DIRECTION ( 'NONE',  ( 0.000000000000000000, 0.007114381193220324640, -0.9999746924698832418 ) ) ;
#7959=CARTESIAN_POINT ( 'NONE',  ( -14.87409385541304019, -6.859212275519751323, 50.50378509014259265 ) ) ;
#7973=CARTESIAN_POINT ( 'NONE',  ( -18.84284385759798752, -7.587656875400192291, 49.25157356644813689 ) ) ;
#7983=CARTESIAN_POINT ( 'NONE',  ( 18.57590614458695200, 0.6315104036983664182, 50.27646649643033783 ) ) ;
#7994=CARTESIAN_POINT ( 'NONE',  ( -21.62409385650551741, -6.426201560718812544, 50.50509628382439331 ) ) ;
#8012=CARTESIAN_POINT ( 'NONE',  ( -14.87409385650551741, -9.792211528768504536, 50.49490371617623197 ) ) ;
#8020=CARTESIAN_POINT ( 'NONE',  ( -15.01784385650551457, -9.790100578890868377, 49.79778022625163203 ) ) ;
#8025=CARTESIAN_POINT ( 'NONE',  ( -15.58034385650551634, -6.424090610841176385, 49.80797279389977916 ) ) ;
#8031=DIRECTION ( 'NONE',  ( 1.000000000000000000, -4.164305804376849172E-17, 1.614929280266638808E-16 ) ) ;
#8045=DIRECTION ( 'NONE',  ( -1.000000000000000000, -1.669677910507523057E-21, -6.493791346278465266E-22 ) ) ;
#8064=CARTESIAN_POINT ( 'NONE',  ( 18.57590614458706924, 0.6315104036983326674, 50.27646649643033783 ) ) ;
#8073=CARTESIAN_POINT ( 'NONE',  ( -19.31784385541291016, -6.860780111191745689, 51.02154966934421765 ) ) ;
#8075=ORIENTED_EDGE ( 'NONE', *, *, #20174, .T. ) ;
#8085=CARTESIAN_POINT ( 'NONE',  ( -15.88659385650551670, -9.302874398569244363, 51.68646062012417985 ) ) ;
#8091=ORIENTED_EDGE ( 'NONE', *, *, #48520, .F. ) ;
#8115=ORIENTED_EDGE ( 'NONE', *, *, #4929, .F. ) ;
#8121=CARTESIAN_POINT ( 'NONE',  ( -20.66784385650552380, -6.428312510596450480, 51.20221977374900035 ) ) ;
#8158=CARTESIAN_POINT ( 'NONE',  ( -16.19909385650551670, -8.114302828567740988, 52.18300498402516041 ) ) ;
#8177=CARTESIAN_POINT ( 'NONE',  ( -21.48659385759799179, -7.222650657624104298, 49.61879703869476543 ) ) ;
#8184=PLANE ( 'NONE',  #43819 ) ;
#8193=CARTESIAN_POINT ( 'NONE',  ( -22.29909385650551812, -8.114302828567740988, 52.18300498402516041 ) ) ;
#8205=CARTESIAN_POINT ( 'NONE',  ( 10.57590614458695377, 0.6652513346184687482, 50.77657095919170871 ) ) ;
#8226=CARTESIAN_POINT ( 'NONE',  ( 18.57590614458695200, 1.636933384339416264, 51.78951792648778252 ) ) ;
#8227=CARTESIAN_POINT ( 'NONE',  ( -18.81159385650551741, -6.922745924619793101, 51.69366785382590024 ) ) ;
#8229=VERTEX_POINT ( 'NONE', #5250 ) ;
#8248=CARTESIAN_POINT ( 'NONE',  ( -22.29909385541304090, -8.105421454601382081, 49.25000573077640098 ) ) ;
#8258=CARTESIAN_POINT ( 'NONE',  ( 22.62590614458706639, 1.904620652374673151, 48.58033007082241994 ) ) ;
#8292=AXIS2_PLACEMENT_3D ( 'NONE', #10342, #43596, #28330 ) ;
#8303=EDGE_LOOP ( 'NONE', ( #42000, #25665 ) ) ;
#8310=( BOUNDED_CURVE ( )  B_SPLINE_CURVE ( 2, ( #41101, #18677, #12275, #37891, #717, #27056, #4650, #244, #38620 ),
 .UNSPECIFIED., .F., .F. ) 
 B_SPLINE_CURVE_WITH_KNOTS ( ( 3, 2, 2, 2, 3 ),
 ( 0.2916666666666666297, 0.3020833333333332593, 0.3124999999999999445, 0.3229166666666666297, 0.3333333333333332593 ),
 .UNSPECIFIED. ) 
 CURVE ( )  GEOMETRIC_REPRESENTATION_ITEM ( )  RATIONAL_B_SPLINE_CURVE ( ( 1.000000000000000444, 0.9238795325112862944, 1.000000000000000000, 0.9238795325112867385, 1.000000000000000000, 0.9238795325112867385, 1.000000000000000000, 0.9238795325112871826, 0.9999999999999995559 ) ) 
 REPRESENTATION_ITEM ( '' )  );
#8311=CARTESIAN_POINT ( 'NONE',  ( -14.76159385650551847, -9.295667164867525756, 49.30633214617472504 ) ) ;
#8329=ORIENTED_EDGE ( 'NONE', *, *, #23169, .F. ) ;
#8332=CARTESIAN_POINT ( 'NONE',  ( -36.42409385541304800, -8.109206544743658540, 50.50000000000030553 ) ) ;
#8344=CARTESIAN_POINT ( 'NONE',  ( -16.42409385759798823, -9.359200813967568422, 50.49621490985803263 ) ) ;
#8347=EDGE_LOOP ( 'NONE', ( #19416, #30454, #46569, #25315 ) ) ;
#8351=CARTESIAN_POINT ( 'NONE',  ( -21.06159385650551741, -9.295667164867525756, 49.30633214617472504 ) ) ;
#8366=DIRECTION ( 'NONE',  ( 1.000000000000000000, -4.164305804376849172E-17, 1.614929280266638808E-16 ) ) ;
#8379=ORIENTED_EDGE ( 'NONE', *, *, #19746, .F. ) ;
#8387=CARTESIAN_POINT ( 'NONE',  ( -19.12409385650551741, -6.426201560718813433, 50.50509628382439331 ) ) ;
#8390=EDGE_CURVE ( 'NONE', #40074, #17102, #4695, .T. ) ;
#8406=CARTESIAN_POINT ( 'NONE',  ( -20.64284385759799179, -7.587656875400192291, 49.25157356644813689 ) ) ;
#8422=CARTESIAN_POINT ( 'NONE',  ( -22.18659385650551741, -9.302874398569244363, 51.68646062012417985 ) ) ;
#8434=ORIENTED_EDGE ( 'NONE', *, *, #1616, .T. ) ;
#8453=EDGE_CURVE ( 'NONE', #26883, #19332, #14772, .T. ) ;
#8455=CARTESIAN_POINT ( 'NONE',  ( -17.29284385650551670, -7.406986770994972602, 48.81910596585309747 ) ) ;
#8456=ORIENTED_EDGE ( 'NONE', *, *, #681, .F. ) ;
#8473=FACE_OUTER_BOUND ( 'NONE', #45518, .T. ) ;
#8479=ORIENTED_EDGE ( 'NONE', *, *, #36552, .F. ) ;
#8480=CARTESIAN_POINT ( 'NONE',  ( -22.46784385541304374, -9.357632978295830739, 49.97845033065684106 ) ) ;
#8507=FACE_OUTER_BOUND ( 'NONE', #13457, .T. ) ;
#8515=CARTESIAN_POINT ( 'NONE',  ( 18.46573386768564973, 3.114729847419841047, 50.78398819077492732 ) ) ;
#8523=ORIENTED_EDGE ( 'NONE', *, *, #27126, .F. ) ;
#8541=CARTESIAN_POINT ( 'NONE',  ( -22.27409385650551243, -9.792211528768504536, 50.49490371617623197 ) ) ;
#8548=CARTESIAN_POINT ( 'NONE',  ( -21.54284385650551670, -8.811426318492348031, 52.18089403414751359 ) ) ;
#8549=ORIENTED_EDGE ( 'NONE', *, *, #44949, .T. ) ;
#8595=CARTESIAN_POINT ( 'NONE',  ( -22.41159385650551528, -6.922745924619793101, 51.69366785382590024 ) ) ;
#8600=( BOUNDED_CURVE ( )  B_SPLINE_CURVE ( 2, ( #4355, #42757, #20095, #19363, #1132, #9025, #45962, #24046, #34864 ),
 .UNSPECIFIED., .F., .F. ) 
 B_SPLINE_CURVE_WITH_KNOTS ( ( 3, 2, 2, 2, 3 ),
 ( 0.5833333333333332593, 0.5937499999999998890, 0.6041666666666665186, 0.6145833333333332593, 0.6249999999999998890 ),
 .UNSPECIFIED. ) 
 CURVE ( )  GEOMETRIC_REPRESENTATION_ITEM ( )  RATIONAL_B_SPLINE_CURVE ( ( 1.000000000000000888, 0.9238795325112859613, 1.000000000000000000, 0.9238795325112867385, 1.000000000000000000, 0.9238795325112867385, 1.000000000000000000, 0.9238795325112875156, 0.9999999999999992228 ) ) 
 REPRESENTATION_ITEM ( '' )  );
#8638=EDGE_CURVE ( 'NONE', #13744, #29820, #10095, .T. ) ;
#8639=CARTESIAN_POINT ( 'NONE',  ( -15.83034385541288991, -6.857644439847648599, 49.98602051094142951 ) ) ;
#8640=CARTESIAN_POINT ( 'NONE',  ( -17.66159385650551528, -9.295667164867525756, 49.30633214617472504 ) ) ;
#8658=CARTESIAN_POINT ( 'NONE',  ( -22.33034385759799179, -6.857644439848013640, 49.98602051094139398 ) ) ;
#8668=VECTOR ( 'NONE', #37663, 1000.000000000000114 ) ;
#8675=CARTESIAN_POINT ( 'NONE',  ( -22.74909385650551386, -8.104110260919577868, 48.81699501597546487 ) ) ;
#8687=CLOSED_SHELL ( 'NONE', ( #32829, #20110, #31688, #6131, #45936, #24247, #286, #5 ) ) ;
#8688=ORIENTED_EDGE ( 'NONE', *, *, #45753, .T. ) ;
#8703=DIRECTION ( 'NONE',  ( 1.000000000000000000, 1.669677910507523057E-21, 6.493791346278465266E-22 ) ) ;
#8704=DIRECTION ( 'NONE',  ( 0.000000000000000000, 1.000000000000000000, -3.469446951953614189E-15 ) ) ;
#8711=CARTESIAN_POINT ( 'NONE',  ( -14.48034385650551847, -6.424090610841176385, 49.80797279389978627 ) ) ;
#8716=CARTESIAN_POINT ( 'NONE',  ( -20.02409385759798965, -9.359200813967568422, 50.49621490985803263 ) ) ;
#8737=CARTESIAN_POINT ( 'NONE',  ( -22.74909385541304019, -8.112991634885936776, 51.74999426922421719 ) ) ;
#8762=CARTESIAN_POINT ( 'NONE',  ( -19.57409385759799036, -6.859212275519751323, 50.50378509014259265 ) ) ;
#8790=CARTESIAN_POINT ( 'NONE',  ( -21.84909385541302029, -8.112991634885936776, 51.74999426922424561 ) ) ;
#8797=CARTESIAN_POINT ( 'NONE',  ( -22.04909385650551457, -8.104110260919577868, 48.81699501597546487 ) ) ;
#8803=CARTESIAN_POINT ( 'NONE',  ( -22.55534385650551599, -7.417179338643134834, 52.18511593390279302 ) ) ;
#8816=ORIENTED_EDGE ( 'NONE', *, *, #5380, .T. ) ;
#8839=DIRECTION ( 'NONE',  ( 0.000000000000000000, -0.9999954153791273948, -0.003028072113819838245 ) ) ;
#8847=CARTESIAN_POINT ( 'NONE',  ( -12.72364782008763484, -9.064348897850818432, 49.69364828684970803 ) ) ;
#8875=CARTESIAN_POINT ( 'NONE',  ( -17.32409385759798681, -9.359200813967568422, 50.49621490985803263 ) ) ;
#8882=CARTESIAN_POINT ( 'NONE',  ( -15.80534385650551599, -8.801233750844183135, 48.81488406609782515 ) ) ;
#8891=CARTESIAN_POINT ( 'NONE',  ( -15.49284385541290376, -8.630756214087227818, 51.74842643355271576 ) ) ;
#8914=ORIENTED_EDGE ( 'NONE', *, *, #27126, .T. ) ;
#8915=CARTESIAN_POINT ( 'NONE',  ( -22.69284385650552238, -7.406986770994973490, 48.81910596585309747 ) ) ;
#8921=B_SPLINE_CURVE_WITH_KNOTS ( 'NONE', 1,
 ( #28399, #32559 ),
 .UNSPECIFIED., .F., .F.,
 ( 2, 2 ),
 ( 0.000000000000000000, 1.000000000000000000 ),
 .UNSPECIFIED. ) ;
#8935=CYLINDRICAL_SURFACE ( 'NONE', #24240, 1.249999999999998668 ) ;
#8951=CARTESIAN_POINT ( 'NONE',  ( -18.22409385759798894, -9.359200813967568422, 50.49621490985803263 ) ) ;
#8952=CARTESIAN_POINT ( 'NONE',  ( -17.40534385650551741, -8.801233750844183135, 48.81488406609782515 ) ) ;
#8962=CARTESIAN_POINT ( 'NONE',  ( 18.57590614458706924, 3.114729847420145248, 50.78398819077499127 ) ) ;
#8975=CARTESIAN_POINT ( 'NONE',  ( -21.00534385541304161, -7.595227055684746986, 51.75156210489594599 ) ) ;
#9003=DIRECTION ( 'NONE',  ( 1.000000000000000000, -4.164305804376849788E-17, 1.614929280266638808E-16 ) ) ;
#9025=CARTESIAN_POINT ( 'NONE',  ( -16.14284385759799179, -7.587656875400192291, 49.25157356644813689 ) ) ;
#9034=CARTESIAN_POINT ( 'NONE',  ( -21.20534385650551812, -8.801233750844183135, 48.81488406609782515 ) ) ;
#9040=CARTESIAN_POINT ( 'NONE',  ( -23.11784385650551954, -9.790100578890868377, 49.79778022625162492 ) ) ;
#9084=CARTESIAN_POINT ( 'NONE',  ( -18.02409385650551599, -6.426201560718813433, 50.50509628382439331 ) ) ;
#9094=CARTESIAN_POINT ( 'NONE',  ( -22.52409385541004383, -9.359200813967481380, 50.49621490983041383 ) ) ;
#9102=CARTESIAN_POINT ( 'NONE',  ( -13.52409385541304410, -9.359200813967568422, 50.49621490985803263 ) ) ;
#9119=CARTESIAN_POINT ( 'NONE',  ( -17.32409385650551314, -6.426201560718813433, 50.50509628382439331 ) ) ;
#9127=CIRCLE ( 'NONE', #11470, 1.049999999999998934 ) ;
#9140=CARTESIAN_POINT ( 'NONE',  ( -18.33659385759798965, -8.995762431863214559, 51.38120296130585274 ) ) ;
#9141=DIRECTION ( 'NONE',  ( 0.000000000000000000, 1.000000000000000000, -5.551115123125785858E-15 ) ) ;
#9159=VERTEX_POINT ( 'NONE', #28873 ) ;
#9190=CARTESIAN_POINT ( 'NONE',  ( -15.26784385650551989, -6.428312510596451368, 51.20221977374900035 ) ) ;
#9201=ORIENTED_EDGE ( 'NONE', *, *, #27020, .F. ) ;
#9215=CARTESIAN_POINT ( 'NONE',  ( -20.44284385541303806, -7.587656875400192291, 49.25157356644813689 ) ) ;
#9259=CARTESIAN_POINT ( 'NONE',  ( -33.42409385541304800, -7.059211358595575803, 50.50317947571981847 ) ) ;
#9268=CARTESIAN_POINT ( 'NONE',  ( -22.89284385650552522, -7.406986770994973490, 48.81910596585309747 ) ) ;
#9274=CARTESIAN_POINT ( 'NONE',  ( -13.63659385650551847, -6.915538690918075382, 49.31353937987644542 ) ) ;
#9276=EDGE_CURVE ( 'NONE', #501, #13279, #7454, .T. ) ;
#9282=EDGE_CURVE ( 'NONE', #4206, #12395, #47961, .T. ) ;
#9284=CARTESIAN_POINT ( 'NONE',  ( -21.00534385541298121, -7.595227055684706130, 51.75156210489605257 ) ) ;
#9310=VECTOR ( 'NONE', #14166, 1000.000000000000000 ) ;
#9318=VERTEX_POINT ( 'NONE', #6953 ) ;
#9320=CARTESIAN_POINT ( 'NONE',  ( -18.92409385541303024, -9.359200813967568422, 50.49621490985794026 ) ) ;
#9322=CARTESIAN_POINT ( 'NONE',  ( -17.57409385650551314, -9.792211528768504536, 50.49490371617623197 ) ) ;
#9345=CARTESIAN_POINT ( 'NONE',  ( -13.58034385541284195, -9.360768649639799932, 51.01397948905916735 ) ) ;
#9350=EDGE_CURVE ( 'NONE', #47438, #24678, #26393, .T. ) ;
#9363=CARTESIAN_POINT ( 'NONE',  ( -14.39909385650551776, -8.114302828567740988, 52.18300498402516041 ) ) ;
#9367=( GEOMETRIC_REPRESENTATION_CONTEXT ( 3 ) GLOBAL_UNCERTAINTY_ASSIGNED_CONTEXT ( ( #26814 ) ) GLOBAL_UNIT_ASSIGNED_CONTEXT ( ( #11559, #45075, #12052 ) ) REPRESENTATION_CONTEXT ( 'NONE', 'WORKASPACE' ) );
#9368=LINE ( 'NONE', #6633, #9464 ) ;
#9382=CARTESIAN_POINT ( 'NONE',  ( -17.54909385759799179, -8.112991634885936776, 51.74999426922421719 ) ) ;
#9415=DIRECTION ( 'NONE',  ( 1.000000000000000000, 1.669677910507523057E-21, 6.493791346278465266E-22 ) ) ;
#9436=CARTESIAN_POINT ( 'NONE',  ( -15.60534385650552025, -8.801233750844183135, 48.81488406609782515 ) ) ;
#9445=CARTESIAN_POINT ( 'NONE',  ( -18.47409385541327964, -6.859212275519742441, 50.50378509014038997 ) ) ;
#9462=CARTESIAN_POINT ( 'NONE',  ( -18.19284385541304161, -8.630756214087126565, 51.74842643355248129 ) ) ;
#9463=DIRECTION ( 'NONE',  ( 1.616182858256114592E-16, 0.003028072113811714535, -0.9999954153791273948 ) ) ;
#9464=VECTOR ( 'NONE', #29032, 1000.000000000000114 ) ;
#9468=( BOUNDED_CURVE ( )  B_SPLINE_CURVE ( 2, ( #43723, #22269, #7268, #21779, #44446, #36304, #10696, #18308, #6767 ),
 .UNSPECIFIED., .F., .F. ) 
 B_SPLINE_CURVE_WITH_KNOTS ( ( 3, 2, 2, 2, 3 ),
 ( 0.04720854346325247669, 0.04819199384251378337, 0.04917544422177509700, 0.05015889460103639674, 0.05114234498029770343 ),
 .UNSPECIFIED. ) 
 CURVE ( )  GEOMETRIC_REPRESENTATION_ITEM ( )  RATIONAL_B_SPLINE_CURVE ( ( 0.9999999999999715783, 0.9238795325113151602, 1.000000000000000000, 0.9238795325112867385, 1.000000000000000000, 0.9238795325112867385, 1.000000000000000000, 0.9238795325108096756, 1.000000000000476952 ) ) 
 REPRESENTATION_ITEM ( '' )  );
#9509=ORIENTED_EDGE ( 'NONE', *, *, #25084, .T. ) ;
#9515=CARTESIAN_POINT ( 'NONE',  ( 18.46573386768564973, 3.116243883476752963, 50.28399048308536123 ) ) ;
#9520=CARTESIAN_POINT ( 'NONE',  ( -19.01159385650551670, -6.922745924619793101, 51.69366785382590024 ) ) ;
#9526=CARTESIAN_POINT ( 'NONE',  ( -22.49909385650551741, -8.114302828567740988, 52.18300498402516041 ) ) ;
#9544=ORIENTED_EDGE ( 'NONE', *, *, #18392, .T. ) ;
#9568=ORIENTED_EDGE ( 'NONE', *, *, #20848, .T. ) ;
#9574=CARTESIAN_POINT ( 'NONE',  ( -19.43034385650552309, -9.794322478646142471, 51.19202720610083901 ) ) ;
#9610=ORIENTED_EDGE ( 'NONE', *, *, #33166, .F. ) ;
#9615=CARTESIAN_POINT ( 'NONE',  ( -15.01784385650551457, -9.790100578890868377, 49.79778022625163203 ) ) ;
#9621=DIRECTION ( 'NONE',  ( -1.000000000000000000, 4.164305804376849172E-17, -1.614929280266638808E-16 ) ) ;
#9634=CARTESIAN_POINT ( 'NONE',  ( -20.47409385759799250, -6.859212275519751323, 50.50378509014259265 ) ) ;
#9637=DIRECTION ( 'NONE',  ( -1.000000000000000000, -1.669677910507523057E-21, -6.493791346278465266E-22 ) ) ;
#9653=EDGE_LOOP ( 'NONE', ( #7892, #42599 ) ) ;
#9668=EDGE_LOOP ( 'NONE', ( #38320, #38627, #2626, #6480 ) ) ;
#9681=CARTESIAN_POINT ( 'NONE',  ( -13.29909385650551812, -8.114302828567740988, 52.18300498402516041 ) ) ;
#9690=CARTESIAN_POINT ( 'NONE',  ( -18.53034385541318230, -6.857644439848909812, 49.98602051094048448 ) ) ;
#9709=CARTESIAN_POINT ( 'NONE',  ( -16.89909385541304232, -8.105421454601382081, 49.25000573077640098 ) ) ;
#9744=( BOUNDED_CURVE ( )  B_SPLINE_CURVE ( 3, ( #10712, #40746, #3323, #36317 ),
 .UNSPECIFIED., .F., .F. ) 
 B_SPLINE_CURVE_WITH_KNOTS ( ( 4, 4 ),
 ( 3.703566858574705169E-15, 0.2013579207903336277 ),
 .UNSPECIFIED. ) 
 CURVE ( )  GEOMETRIC_REPRESENTATION_ITEM ( )  RATIONAL_B_SPLINE_CURVE ( ( 1.000000000000000000, 0.9966241020034161124, 0.9966241020034161124, 1.000000000000000000 ) ) 
 REPRESENTATION_ITEM ( '' )  );
#9760=CARTESIAN_POINT ( 'NONE',  ( -19.96784385650551741, -6.428312510596451368, 51.20221977374900035 ) ) ;
#9763=CARTESIAN_POINT ( 'NONE',  ( -19.46159385650551599, -9.295667164867525756, 49.30633214617472504 ) ) ;
#9770=EDGE_CURVE ( 'NONE', #43599, #3423, #3686, .T. ) ;
#9785=ORIENTED_EDGE ( 'NONE', *, *, #26585, .T. ) ;
#9800=VECTOR ( 'NONE', #39528, 1000.000000000000114 ) ;
#9808=CARTESIAN_POINT ( 'NONE',  ( -16.89909385650551599, -8.114302828567740988, 52.18300498402516041 ) ) ;
#9830=EDGE_CURVE ( 'NONE', #10899, #24601, #18475, .T. ) ;
#9839=ORIENTED_EDGE ( 'NONE', *, *, #26525, .F. ) ;
#9845=CARTESIAN_POINT ( 'NONE',  ( -14.28659385650551528, -9.302874398569244363, 51.68646062012417985 ) ) ;
#9862=CARTESIAN_POINT ( 'NONE',  ( -18.84284385759798752, -7.587656875400192291, 49.25157356644813689 ) ) ;
#9865=CARTESIAN_POINT ( 'NONE',  ( -36.42409385541304800, -9.359200813967566646, 50.49621490985803263 ) ) ;
#9917=CARTESIAN_POINT ( 'NONE',  ( 6.575906144586949331, -6.109215713985405749, 50.50605614422795497 ) ) ;
#9928=FACE_OUTER_BOUND ( 'NONE', #11344, .T. ) ;
#9932=EDGE_CURVE ( 'NONE', #4040, #34525, #45267, .T. ) ;
#9939=CARTESIAN_POINT ( 'NONE',  ( -19.76784385541304090, -9.357632978295830739, 49.97845033065684106 ) ) ;
#9988=CARTESIAN_POINT ( 'NONE',  ( -19.18034385650551599, -6.424090610841176385, 49.80797279389977916 ) ) ;
#9991=CARTESIAN_POINT ( 'NONE',  ( -19.79909385650551457, -8.114302828567740988, 52.18300498402516041 ) ) ;
#10056=CARTESIAN_POINT ( 'NONE',  ( -19.20534385650551457, -8.801233750844183135, 48.81488406609782515 ) ) ;
#10080=CARTESIAN_POINT ( 'NONE',  ( -13.27409385650551599, -9.792211528768504536, 50.49490371617623197 ) ) ;
#10091=EDGE_CURVE ( 'NONE', #28258, #45882, #28579, .T. ) ;
#10095=LINE ( 'NONE', #31536, #42458 ) ;
#10100=CARTESIAN_POINT ( 'NONE',  ( -20.41784385759799036, -6.860780111191487229, 51.02154966934377001 ) ) ;
#10141=AXIS2_PLACEMENT_3D ( 'NONE', #24450, #35509, #13087 ) ;
#10188=CARTESIAN_POINT ( 'NONE',  ( -17.06784385541304516, -9.357632978295830739, 49.97845033065684106 ) ) ;
#10219=CARTESIAN_POINT ( 'NONE',  ( -22.69284385650551883, -7.406986770994972602, 48.81910596585309747 ) ) ;
#10240=EDGE_LOOP ( 'NONE', ( #48353, #27571, #9568, #8456 ) ) ;
#10242=CARTESIAN_POINT ( 'NONE',  ( -18.95534385650551457, -7.417179338643134834, 52.18511593390279302 ) ) ;
#10247=CARTESIAN_POINT ( 'NONE',  ( -19.63034385650551883, -9.794322478646142471, 51.19202720610083901 ) ) ;
#10284=ORIENTED_EDGE ( 'NONE', *, *, #44681, .F. ) ;
#10305=CARTESIAN_POINT ( 'NONE',  ( -20.33034385650551812, -9.794322478646142471, 51.19202720610083901 ) ) ;
#10342=CARTESIAN_POINT ( 'NONE',  ( 6.575906144586949331, -8.109206544743660316, 50.50000000000031264 ) ) ;
#10350=CARTESIAN_POINT ( 'NONE',  ( -14.56784385759798894, -9.357632978295830739, 49.97845033065684106 ) ) ;
#10355=VERTEX_POINT ( 'NONE', #1085 ) ;
#10387=CARTESIAN_POINT ( 'NONE',  ( -18.61784385759798965, -6.860780111191480124, 51.02154966934376290 ) ) ;
#10392=CARTESIAN_POINT ( 'NONE',  ( -22.83659385650551954, -6.915538690918074494, 49.31353937987644542 ) ) ;
#10398=CARTESIAN_POINT ( 'NONE',  ( 18.82590614458706924, 1.876518846661452411, 52.53023010607846288 ) ) ;
#10430=CARTESIAN_POINT ( 'NONE',  ( -19.09284385541304019, -8.630756214087126565, 51.74842643355248129 ) ) ;
#10443=CARTESIAN_POINT ( 'NONE',  ( -20.33034385541270339, -6.857644439845836715, 49.98602051094355403 ) ) ;
#10470=( BOUNDED_CURVE ( )  B_SPLINE_CURVE ( 2, ( #26332, #33957, #4407, #7142, #23140, #3431, #14477, #38130, #4185 ),
 .UNSPECIFIED., .F., .F. ) 
 B_SPLINE_CURVE_WITH_KNOTS ( ( 3, 2, 2, 2, 3 ),
 ( 0.7500000000000000000, 0.7604166666666666297, 0.7708333333333334814, 0.7812500000000001110, 0.7916666666666667407 ),
 .UNSPECIFIED. ) 
 CURVE ( )  GEOMETRIC_REPRESENTATION_ITEM ( )  RATIONAL_B_SPLINE_CURVE ( ( 1.000000000000000000, 0.9238795325112867385, 1.000000000000000000, 0.9238795325112867385, 1.000000000000000000, 0.9238795325112867385, 1.000000000000000000, 0.9238795325112859613, 1.000000000000000888 ) ) 
 REPRESENTATION_ITEM ( '' )  );
#10482=CARTESIAN_POINT ( 'NONE',  ( -19.63034385650551883, -9.794322478646142471, 51.19202720610083901 ) ) ;
#10486=CARTESIAN_POINT ( 'NONE',  ( -18.28034385650551741, -6.424090610841176385, 49.80797279389977916 ) ) ;
#10500=EDGE_LOOP ( 'NONE', ( #37920, #45095 ) ) ;
#10509=ORIENTED_EDGE ( 'NONE', *, *, #28020, .F. ) ;
#10524=VERTEX_POINT ( 'NONE', #41666 ) ;
#10535=FACE_OUTER_BOUND ( 'NONE', #19597, .T. ) ;
#10542=EDGE_CURVE ( 'NONE', #20025, #45257, #43331, .T. ) ;
#10543=CARTESIAN_POINT ( 'NONE',  ( -18.36159385650551812, -9.295667164867525756, 49.30633214617472504 ) ) ;
#10577=ORIENTED_EDGE ( 'NONE', *, *, #19807, .T. ) ;
#10582=CARTESIAN_POINT ( 'NONE',  ( -15.74909385759799108, -8.112991634885936776, 51.74999426922421719 ) ) ;
#10632=CARTESIAN_POINT ( 'NONE',  ( -14.25534385650552238, -7.417179338643134834, 52.18511593390279302 ) ) ;
#10634=ORIENTED_EDGE ( 'NONE', *, *, #30701, .T. ) ;
#10655=CARTESIAN_POINT ( 'NONE',  ( -15.46784385759799285, -9.357632978295836068, 49.97845033065684106 ) ) ;
#10660=CARTESIAN_POINT ( 'NONE',  ( -15.88659385541304303, -7.222650657624104298, 49.61879703869476543 ) ) ;
#10668=ORIENTED_EDGE ( 'NONE', *, *, #45501, .F. ) ;
#10693=CARTESIAN_POINT ( 'NONE',  ( -21.43034385759798965, -6.857644439848012752, 49.98602051094139398 ) ) ;
#10696=CARTESIAN_POINT ( 'NONE',  ( -17.68659385541293716, -7.222650657623975512, 49.61879703869464464 ) ) ;
#10703=CARTESIAN_POINT ( 'NONE',  ( -19.48659385650551457, -9.302874398569244363, 51.68646062012417985 ) ) ;
#10711=CARTESIAN_POINT ( 'NONE',  ( -15.07409385650551670, -9.792211528768504536, 50.49490371617623197 ) ) ;
#10712=CARTESIAN_POINT ( 'NONE',  ( 18.54465614458695200, 0.6407533398237036382, 50.52649563099625851 ) ) ;
#10713=CARTESIAN_POINT ( 'NONE',  ( 18.57590614458706924, 1.890747609047893185, 50.53028072113869484 ) ) ;
#10714=CARTESIAN_POINT ( 'NONE',  ( -20.47409385650551528, -9.792211528768504536, 50.49490371617623197 ) ) ;
#10752=( BOUNDED_CURVE ( )  B_SPLINE_CURVE ( 2, ( #8951, #31831, #46853, #13336, #46373, #43653, #35994, #24697, #27892 ),
 .UNSPECIFIED., .F., .F. ) 
 B_SPLINE_CURVE_WITH_KNOTS ( ( 3, 2, 2, 2, 3 ),
 ( 0.4166666666666667407, 0.4270833333333333703, 0.4375000000000000000, 0.4479166666666666852, 0.4583333333333333148 ),
 .UNSPECIFIED. ) 
 CURVE ( )  GEOMETRIC_REPRESENTATION_ITEM ( )  RATIONAL_B_SPLINE_CURVE ( ( 0.9999999999999995559, 0.9238795325112871826, 1.000000000000000000, 0.9238795325112867385, 1.000000000000000000, 0.9238795325112867385, 1.000000000000000000, 0.9238795325112867385, 1.000000000000000000 ) ) 
 REPRESENTATION_ITEM ( '' )  );
#10777=CARTESIAN_POINT ( 'NONE',  ( -19.09284385650552096, -7.406986770994973490, 48.81910596585309747 ) ) ;
#10781=CARTESIAN_POINT ( 'NONE',  ( -13.19031587015885343, -9.064346445990929979, 49.69364538247001661 ) ) ;
#10816=CARTESIAN_POINT ( 'NONE',  ( -14.96159385759799143, -7.228003583438117552, 51.38655588711986155 ) ) ;
#10841=CARTESIAN_POINT ( 'NONE',  ( -22.97409385650551528, -9.792211528768504536, 50.49490371617623197 ) ) ;
#10854=CARTESIAN_POINT ( 'NONE',  ( -20.92409385650551812, -6.426201560718813433, 50.50509628382439331 ) ) ;
#10877=CARTESIAN_POINT ( 'NONE',  ( -13.72409385650551528, -6.426201560718813433, 50.50509628382439331 ) ) ;
#10892=CARTESIAN_POINT ( 'NONE',  ( -20.86784385759799321, -9.357632978295832515, 49.97845033065684106 ) ) ;
#10899=VERTEX_POINT ( 'NONE', #38082 ) ;
#10900=CARTESIAN_POINT ( 'NONE',  ( -13.91784385541304303, -6.860780111191487229, 51.02154966934377711 ) ) ;
#10932=DIRECTION ( 'NONE',  ( 2.231660450020913765E-16, 0.9999954153791275058, 0.003028072113822189229 ) ) ;
#10935=CARTESIAN_POINT ( 'NONE',  ( -20.27409385650551599, -9.792211528768504536, 50.49490371617623197 ) ) ;
#10939=CARTESIAN_POINT ( 'NONE',  ( -21.03659385759798894, -8.995762431863214559, 51.38120296130585274 ) ) ;
#10952=CARTESIAN_POINT ( 'NONE',  ( -15.66159385650551705, -9.295667164867525756, 49.30633214617472504 ) ) ;
#10960=CARTESIAN_POINT ( 'NONE',  ( -15.80534385650551421, -8.801233750844183135, 48.81488406609782515 ) ) ;
#10963=DIRECTION ( 'NONE',  ( 0.000000000000000000, -0.9999954153791273948, -0.003028072113819836944 ) ) ;
#10964=CARTESIAN_POINT ( 'NONE',  ( -16.81784385650551528, -9.790100578890868377, 49.79778022625163203 ) ) ;
#10975=CARTESIAN_POINT ( 'NONE',  ( -20.72409385541304161, -9.359200813967568422, 50.49621490985803263 ) ) ;
#11000=VERTEX_POINT ( 'NONE', #20353 ) ;
#11023=VECTOR ( 'NONE', #29854, 1000.000000000000114 ) ;
#11028=CARTESIAN_POINT ( 'NONE',  ( -14.64909385650551776, -8.104110260919579645, 48.81699501597546487 ) ) ;
#11061=ORIENTED_EDGE ( 'NONE', *, *, #19715, .F. ) ;
#11062=FACE_OUTER_BOUND ( 'NONE', #34869, .T. ) ;
#11071=CARTESIAN_POINT ( 'NONE',  ( -15.69284385759799427, -8.630756214087126565, 51.74842643355248129 ) ) ;
#11094=AXIS2_PLACEMENT_3D ( 'NONE', #24073, #30743, #1655 ) ;
#11108=CARTESIAN_POINT ( 'NONE',  ( -20.02409385650551599, -6.426201560718813433, 50.50509628382439331 ) ) ;
#11111=ADVANCED_FACE ( 'NONE', ( #22283 ), #47901, .F. ) ;
#11116=VECTOR ( 'NONE', #13787, 1000.000000000000000 ) ;
#11120=LINE ( 'NONE', #23178, #658 ) ;
#11143=CARTESIAN_POINT ( 'NONE',  ( -20.81159385759798752, -8.990409506049200417, 49.61344411288074951 ) ) ;
#11150=CARTESIAN_POINT ( 'NONE',  ( -14.31159385541304374, -8.990409506049202193, 49.61344411288074951 ) ) ;
#11159=VERTEX_POINT ( 'NONE', #21790 ) ;
#11172=EDGE_CURVE ( 'NONE', #24862, #7797, #9744, .T. ) ;
#11175=( BOUNDED_CURVE ( )  B_SPLINE_CURVE ( 2, ( #3861, #38054, #14899, #41036, #19349, #44995, #37819, #18363, #19112 ),
 .UNSPECIFIED., .F., .F. ) 
 B_SPLINE_CURVE_WITH_KNOTS ( ( 3, 2, 2, 2, 3 ),
 ( 0.07474742020699134959, 0.07573079478573833956, 0.07671416936448531565, 0.07769754394323229174, 0.07868091852197928171 ),
 .UNSPECIFIED. ) 
 CURVE ( )  GEOMETRIC_REPRESENTATION_ITEM ( )  RATIONAL_B_SPLINE_CURVE ( ( 0.9999999999988991028, 0.9238795325123876356, 1.000000000000000000, 0.9238795325112867385, 1.000000000000000000, 0.9238795325112867385, 1.000000000000000000, 0.9238795325112550971, 1.000000000000031530 ) ) 
 REPRESENTATION_ITEM ( '' )  );
#11185=CARTESIAN_POINT ( 'NONE',  ( -18.75534385650551528, -7.417179338643134834, 52.18511593390279302 ) ) ;
#11202=CARTESIAN_POINT ( 'NONE',  ( -14.81784385650551528, -9.790100578890868377, 49.79778022625163203 ) ) ;
#11204=CYLINDRICAL_SURFACE ( 'NONE', #7259, 1.249999999999998668 ) ;
#11211=CARTESIAN_POINT ( 'NONE',  ( -13.12522125891144853, -9.020171137055317701, 48.97007792487355005 ) ) ;
#11216=CARTESIAN_POINT ( 'NONE',  ( -14.56784385650551528, -6.428312510596451368, 51.20221977374900035 ) ) ;
#11262=CARTESIAN_POINT ( 'NONE',  ( -13.52409385541304410, -9.359200813967568422, 50.49621490985803263 ) ) ;
#11275=CARTESIAN_POINT ( 'NONE',  ( -16.28034385650551741, -6.424090610841176385, 49.80797279389977916 ) ) ;
#11315=CARTESIAN_POINT ( 'NONE',  ( -13.83659385759798965, -8.995762431863214559, 51.38120296130585274 ) ) ;
#11331=DIRECTION ( 'NONE',  ( -1.000000000000000000, 4.164305804376849172E-17, -1.614929280266638808E-16 ) ) ;
#11344=EDGE_LOOP ( 'NONE', ( #31185, #39297 ) ) ;
#11350=CARTESIAN_POINT ( 'NONE',  ( -21.14909385650551599, -8.104110260919577868, 48.81699501597546487 ) ) ;
#11384=CARTESIAN_POINT ( 'NONE',  ( -15.77409385541304232, -6.859212275519751323, 50.50378509014259265 ) ) ;
#11385=EDGE_CURVE ( 'NONE', #33983, #46443, #24958, .T. ) ;
#11397=CARTESIAN_POINT ( 'NONE',  ( -19.01159385759799036, -8.990409506049200417, 49.61344411288074951 ) ) ;
#11415=CARTESIAN_POINT ( 'NONE',  ( -18.69909385650551670, -8.114302828567740988, 52.18300498402516041 ) ) ;
#11423=ADVANCED_FACE ( 'NONE', ( #43933 ), #17554, .T. ) ;
#11428=CARTESIAN_POINT ( 'NONE',  ( -13.69284385650552061, -7.406986770994973490, 48.81910596585309747 ) ) ;
#11437=CARTESIAN_POINT ( 'NONE',  ( -14.96159385650551776, -9.295667164867525756, 49.30633214617472504 ) ) ;
#11443=CARTESIAN_POINT ( 'NONE',  ( -15.97409385650551705, -9.792211528768504536, 50.49490371617623197 ) ) ;
#11470=AXIS2_PLACEMENT_3D ( 'NONE', #3381, #25547, #21621 ) ;
#11490=EDGE_LOOP ( 'NONE', ( #46242, #11931, #27717, #15087, #25262 ) ) ;
#11498=CARTESIAN_POINT ( 'NONE',  ( -20.10534385541302882, -7.595227055684739881, 51.75156210489597441 ) ) ;
#11505=DIRECTION ( 'NONE',  ( 1.000000000000000000, -4.164305804376849172E-17, 1.614929280266638808E-16 ) ) ;
#11507=CARTESIAN_POINT ( 'NONE',  ( -16.89909385650551599, -8.114302828567740988, 52.18300498402516041 ) ) ;
#11548=CARTESIAN_POINT ( 'NONE',  ( -36.42409385541304800, -8.109206544743658540, 50.50000000000030553 ) ) ;
#11552=CARTESIAN_POINT ( 'NONE',  ( -21.73659385650551812, -6.915538690918074494, 49.31353937987644542 ) ) ;
#11559=( LENGTH_UNIT ( ) NAMED_UNIT ( * ) SI_UNIT ( .MILLI., .METRE. ) );
#11577=FACE_OUTER_BOUND ( 'NONE', #20392, .T. ) ;
#11590=CARTESIAN_POINT ( 'NONE',  ( -19.23659385650551457, -6.915538690918075382, 49.31353937987644542 ) ) ;
#11608=DIRECTION ( 'NONE',  ( -1.000000000000000000, 4.164305804376849172E-17, -1.614929280266638808E-16 ) ) ;
#11626=ORIENTED_EDGE ( 'NONE', *, *, #33440, .T. ) ;
#11629=CARTESIAN_POINT ( 'NONE',  ( -23.08659385541299969, -7.222650657624049231, 49.61879703869472280 ) ) ;
#11663=CARTESIAN_POINT ( 'NONE',  ( -18.47409385650551528, -9.792211528768504536, 50.49490371617623197 ) ) ;
#11671=LINE ( 'NONE', #15839, #34440 ) ;
#11678=CARTESIAN_POINT ( 'NONE',  ( -13.18659385650551918, -9.302874398569244363, 51.68646062012417985 ) ) ;
#11685=TOROIDAL_SURFACE ( 'NONE', #17948, 1.999999999999999112, 1.249999999999999334 ) ;
#11689=CARTESIAN_POINT ( 'NONE',  ( -15.63659385650551670, -6.915538690918075382, 49.31353937987644542 ) ) ;
#11693=CARTESIAN_POINT ( 'NONE',  ( -16.53659385650551528, -6.915538690918075382, 49.31353937987644542 ) ) ;
#11760=CARTESIAN_POINT ( 'NONE',  ( -16.84284385650551741, -8.811426318492348031, 52.18089403414752070 ) ) ;
#11789=AXIS2_PLACEMENT_3D ( 'NONE', #16349, #31384, #7239 ) ;
#11806=CARTESIAN_POINT ( 'NONE',  ( -20.94909385650551670, -8.104110260919577868, 48.81699501597546487 ) ) ;
#11824=CARTESIAN_POINT ( 'NONE',  ( -15.09909385541304516, -8.105421454601382081, 49.25000573077640809 ) ) ;
#11843=CARTESIAN_POINT ( 'NONE',  ( -16.03034385650551386, -9.794322478646142471, 51.19202720610083190 ) ) ;
#11851=CYLINDRICAL_SURFACE ( 'NONE', #36002, 1.249999999999999334 ) ;
#11863=CARTESIAN_POINT ( 'NONE',  ( -22.04909385759799179, -8.112991634885936776, 51.74999426922421719 ) ) ;
#11916=CARTESIAN_POINT ( 'NONE',  ( -20.72409385650551883, -6.426201560718812544, 50.50509628382439331 ) ) ;
#11931=ORIENTED_EDGE ( 'NONE', *, *, #38775, .T. ) ;
#11932=CARTESIAN_POINT ( 'NONE',  ( -14.59284385650551563, -7.406986770994973490, 48.81910596585309747 ) ) ;
#11940=CARTESIAN_POINT ( 'NONE',  ( -22.69284385541304161, -8.630756214087126565, 51.74842643355248129 ) ) ;
#11962=ADVANCED_FACE ( 'NONE', ( #35660 ), #1940, .T. ) ;
#11976=CARTESIAN_POINT ( 'NONE',  ( -14.42409385541304090, -9.359200813967568422, 50.49621490985801842 ) ) ;
#11998=ADVANCED_FACE ( 'NONE', ( #12537 ), #27563, .T. ) ;
#12003=CARTESIAN_POINT ( 'NONE',  ( -16.78659385650551883, -9.302874398569244363, 51.68646062012417985 ) ) ;
#12042=CARTESIAN_POINT ( 'NONE',  ( -12.82409385759799036, -9.359200813967568422, 50.49621490985803263 ) ) ;
#12052=( NAMED_UNIT ( * ) SI_UNIT ( $, .STERADIAN. ) SOLID_ANGLE_UNIT ( ) );
#12083=CARTESIAN_POINT ( 'NONE',  ( -17.77409385650551243, -9.792211528768504536, 50.49490371617623197 ) ) ;
#12100=CARTESIAN_POINT ( 'NONE',  ( -20.75534385759799250, -8.623186033802570094, 49.24843789510466507 ) ) ;
#12115=CARTESIAN_POINT ( 'NONE',  ( -22.86159385650551457, -9.295667164867525756, 49.30633214617472504 ) ) ;
#12118=AXIS2_PLACEMENT_3D ( 'NONE', #343, #35023, #34790 ) ;
#12121=CARTESIAN_POINT ( 'NONE',  ( -19.57409385759799036, -6.859212275519751323, 50.50378509014259265 ) ) ;
#12151=CARTESIAN_POINT ( 'NONE',  ( -16.16784385650552025, -6.428312510596451368, 51.20221977374900035 ) ) ;
#12169=PLANE ( 'NONE',  #40920 ) ;
#12173=CARTESIAN_POINT ( 'NONE',  ( -23.25534385541304161, -8.623186033802570094, 49.24843789510466507 ) ) ;
#12196=CARTESIAN_POINT ( 'NONE',  ( 22.62590614458706639, 0.6407533398237036382, 50.52649563099625851 ) ) ;
#12208=EDGE_LOOP ( 'NONE', ( #5495, #32035, #2033 ) ) ;
#12223=CARTESIAN_POINT ( 'NONE',  ( -22.07409385541323488, -6.859212275519745994, 50.50378509014079498 ) ) ;
#12230=CARTESIAN_POINT ( 'NONE',  ( -22.83659385650551954, -6.915538690918074494, 49.31353937987644542 ) ) ;
#12236=CARTESIAN_POINT ( 'NONE',  ( -20.69909385650551670, -8.114302828567740988, 52.18300498402516041 ) ) ;
#12275=CARTESIAN_POINT ( 'NONE',  ( -19.46159385759798965, -7.228003583438117552, 51.38655588711986155 ) ) ;
#12277=CARTESIAN_POINT ( 'NONE',  ( -20.44284385650551883, -8.811426318492348031, 52.18089403414751359 ) ) ;
#12316=CARTESIAN_POINT ( 'NONE',  ( -18.73034385650551670, -9.794322478646142471, 51.19202720610083190 ) ) ;
#12322=( BOUNDED_CURVE ( )  B_SPLINE_CURVE ( 3, ( #1755, #16748, #20215, #43118 ),
 .UNSPECIFIED., .F., .F. ) 
 B_SPLINE_CURVE_WITH_KNOTS ( ( 4, 4 ),
 ( 6.081827386389258017, 6.283185307179586232 ),
 .UNSPECIFIED. ) 
 CURVE ( )  GEOMETRIC_REPRESENTATION_ITEM ( )  RATIONAL_B_SPLINE_CURVE ( ( 1.000000000000000000, 0.9966241020034161124, 0.9966241020034161124, 1.000000000000000000 ) ) 
 REPRESENTATION_ITEM ( '' )  );
#12325=CARTESIAN_POINT ( 'NONE',  ( -15.43659385541290341, -8.995762431863383313, 51.38120296130602327 ) ) ;
#12352=ORIENTED_EDGE ( 'NONE', *, *, #22439, .T. ) ;
#12372=ORIENTED_EDGE ( 'NONE', *, *, #4638, .F. ) ;
#12384=CARTESIAN_POINT ( 'NONE',  ( -17.23659385650551812, -6.915538690918074494, 49.31353937987644542 ) ) ;
#12395=VERTEX_POINT ( 'NONE', #29377 ) ;
#12409=CARTESIAN_POINT ( 'NONE',  ( -20.27409385541304232, -6.859212275519751323, 50.50378509014259265 ) ) ;
#12457=EDGE_LOOP ( 'NONE', ( #21841, #41436, #31569, #40622, #45587, #20866, #6044, #29393, #43096, #19202, #5510, #38212, #6578, #5875, #6450, #23175, #6341, #23801, #187, #26177, #42029, #43396, #32480, #18383, #39046, #12372 ) ) ;
#12458=DIRECTION ( 'NONE',  ( -0.9524241471993248886, 0.0009228828802118167144, -0.3047743298226213704 ) ) ;
#12464=VERTEX_POINT ( 'NONE', #33282 ) ;
#12466=CARTESIAN_POINT ( 'NONE',  ( -22.16159385650551528, -9.295667164867525756, 49.30633214617472504 ) ) ;
#12471=CARTESIAN_POINT ( 'NONE',  ( -21.88034385650551883, -6.424090610841176385, 49.80797279389977916 ) ) ;
#12473=EDGE_CURVE ( 'NONE', #28707, #29774, #38042, .T. ) ;
#12495=LINE ( 'NONE', #24319, #25176 ) ;
#12518=CARTESIAN_POINT ( 'NONE',  ( -12.88034385759799250, -9.360768649639302552, 51.01397948905922419 ) ) ;
#12537=FACE_OUTER_BOUND ( 'NONE', #1128, .T. ) ;
#12541=EDGE_CURVE ( 'NONE', #46061, #43599, #24837, .T. ) ;
#12561=CARTESIAN_POINT ( 'NONE',  ( -18.56159385650551741, -9.295667164867525756, 49.30633214617472504 ) ) ;
#12596=CARTESIAN_POINT ( 'NONE',  ( 18.46573386768564973, 2.144455078683989768, 49.30629848276630156 ) ) ;
#12605=ADVANCED_FACE ( 'NONE', ( #43130 ), #5223, .T. ) ;
#12623=CARTESIAN_POINT ( 'NONE',  ( 23.52590614458706852, 1.890747609047893185, 50.53028072113869484 ) ) ;
#12624=CARTESIAN_POINT ( 'NONE',  ( -17.54909385759799179, -8.112991634885936776, 51.74999426922421719 ) ) ;
#12631=CARTESIAN_POINT ( 'NONE',  ( -17.68659385650551741, -9.302874398569244363, 51.68646062012417985 ) ) ;
#12656=CARTESIAN_POINT ( 'NONE',  ( -22.80534385541304232, -7.595227055684746986, 51.75156210489594599 ) ) ;
#12664=CARTESIAN_POINT ( 'NONE',  ( 8.575906144586950219, -6.109215713985405749, 50.50605614422795497 ) ) ;
#12676=AXIS2_PLACEMENT_3D ( 'NONE', #34656, #27031, #42298 ) ;
#12679=EDGE_CURVE ( 'NONE', #42061, #21742, #7165, .T. ) ;
#12684=CARTESIAN_POINT ( 'NONE',  ( 10.57590614458695377, 2.144455078683989768, 49.30629848276630156 ) ) ;
#12705=VERTEX_POINT ( 'NONE', #43623 ) ;
#12709=EDGE_CURVE ( 'NONE', #35477, #32441, #27696, .T. ) ;
#12715=CARTESIAN_POINT ( 'NONE',  ( -21.93659385650551741, -6.915538690918074494, 49.31353937987644542 ) ) ;
#12720=CARTESIAN_POINT ( 'NONE',  ( -22.61159385650551457, -6.922745924619793101, 51.69366785382590024 ) ) ;
#12743=FACE_OUTER_BOUND ( 'NONE', #16714, .T. ) ;
#12767=CARTESIAN_POINT ( 'NONE',  ( -16.61784385650551954, -9.790100578890868377, 49.79778022625163203 ) ) ;
#12776=CARTESIAN_POINT ( 'NONE',  ( -22.86159385541300182, -7.228003583438063373, 51.38655588711991840 ) ) ;
#12796=CARTESIAN_POINT ( 'NONE',  ( -16.11159385541290590, -8.990409506049370947, 49.61344411288057898 ) ) ;
#12797=CARTESIAN_POINT ( 'NONE',  ( -18.11159385650551457, -6.922745924619793101, 51.69366785382590024 ) ) ;
#12818=CARTESIAN_POINT ( 'NONE',  ( -18.22409385759798894, -9.359200813967568422, 50.49621490985803263 ) ) ;
#12865=CARTESIAN_POINT ( 'NONE',  ( -15.71784385650551741, -9.790100578890868377, 49.79778022625163203 ) ) ;
#12877=VERTEX_POINT ( 'NONE', #45576 ) ;
#12892=CARTESIAN_POINT ( 'NONE',  ( -23.14284385541304800, -7.587656875400192291, 49.25157356644813689 ) ) ;
#12904=( BOUNDED_CURVE ( )  B_SPLINE_CURVE ( 2, ( #849, #46874, #20540, #27913, #31124, #30896, #46396, #35541, #31854 ),
 .UNSPECIFIED., .F., .F. ) 
 B_SPLINE_CURVE_WITH_KNOTS ( ( 3, 2, 2, 2, 3 ),
 ( 0.5416666666666667407, 0.5520833333333334814, 0.5625000000000000000, 0.5729166666666665186, 0.5833333333333332593 ),
 .UNSPECIFIED. ) 
 CURVE ( )  GEOMETRIC_REPRESENTATION_ITEM ( )  RATIONAL_B_SPLINE_CURVE ( ( 0.9999999999999992228, 0.9238795325112875156, 1.000000000000000000, 0.9238795325112867385, 1.000000000000000000, 0.9238795325112867385, 1.000000000000000000, 0.9238795325112875156, 0.9999999999999992228 ) ) 
 REPRESENTATION_ITEM ( '' )  );
#12939=ORIENTED_EDGE ( 'NONE', *, *, #5380, .F. ) ;
#12943=CARTESIAN_POINT ( 'NONE',  ( -21.43034385650551954, -9.794322478646142471, 51.19202720610083901 ) ) ;
#12948=CARTESIAN_POINT ( 'NONE',  ( -21.76784385650551101, -6.428312510596451368, 51.20221977374900035 ) ) ;
#12953=ORIENTED_EDGE ( 'NONE', *, *, #30078, .F. ) ;
#12981=VERTEX_POINT ( 'NONE', #18745 ) ;
#12990=CARTESIAN_POINT ( 'NONE',  ( -18.41784385650552736, -9.790100578890868377, 49.79778022625163203 ) ) ;
#13008=DIRECTION ( 'NONE',  ( 1.000000000000000000, 0.000000000000000000, 0.000000000000000000 ) ) ;
#13020=CARTESIAN_POINT ( 'NONE',  ( -22.38659385759799036, -7.222650657624104298, 49.61879703869476543 ) ) ;
#13022=ORIENTED_EDGE ( 'NONE', *, *, #31358, .F. ) ;
#13029=CARTESIAN_POINT ( 'NONE',  ( -15.88659385541290447, -7.222650657623934656, 49.61879703869460201 ) ) ;
#13047=CARTESIAN_POINT ( 'NONE',  ( -18.89909385759798965, -8.105421454601382081, 49.25000573077640098 ) ) ;
#13077=EDGE_LOOP ( 'NONE', ( #46836, #30320, #6332, #2004, #45342, #47167, #10668, #15210, #3770, #13022, #45494, #46483 ) ) ;
#13078=DIRECTION ( 'NONE',  ( 0.000000000000000000, 1.000000000000000000, 0.000000000000000000 ) ) ;
#13084=CARTESIAN_POINT ( 'NONE',  ( -35.42409385541304800, -9.359200813967566646, 50.49621490985803263 ) ) ;
#13087=DIRECTION ( 'NONE',  ( 0.000000000000000000, 0.9999954153791273948, 0.003028072113819836077 ) ) ;
#13095=CARTESIAN_POINT ( 'NONE',  ( -16.44909385650551670, -8.104110260919579645, 48.81699501597546487 ) ) ;
#13119=CARTESIAN_POINT ( 'NONE',  ( -19.48659385541304090, -7.222650657624104298, 49.61879703869476543 ) ) ;
#13167=CARTESIAN_POINT ( 'NONE',  ( 18.54465614458695200, 3.140741878271521070, 50.53406581128081143 ) ) ;
#13172=CARTESIAN_POINT ( 'NONE',  ( -21.37409385650551741, -9.792211528768504536, 50.49490371617623197 ) ) ;
#13177=CARTESIAN_POINT ( 'NONE',  ( -21.59909385650551528, -8.114302828567740988, 52.18300498402516041 ) ) ;
#13220=DIRECTION ( 'NONE',  ( -1.000000000000000000, -1.669677910507523057E-21, -6.493791346278465266E-22 ) ) ;
#13221=CARTESIAN_POINT ( 'NONE',  ( -18.47409385650551528, -9.792211528768504536, 50.49490371617623197 ) ) ;
#13236=VECTOR ( 'NONE', #4469, 1000.000000000000000 ) ;
#13258=ADVANCED_FACE ( 'NONE', ( #44815 ), #26092, .T. ) ;
#13262=CARTESIAN_POINT ( 'NONE',  ( -13.83659385650551776, -6.915538690918075382, 49.31353937987644542 ) ) ;
#13263=VECTOR ( 'NONE', #22013, 1000.000000000000114 ) ;
#13266=ADVANCED_FACE ( 'NONE', ( #41103 ), #22898, .F. ) ;
#13279=VERTEX_POINT ( 'NONE', #22388 ) ;
#13283=CARTESIAN_POINT ( 'NONE',  ( -17.32409385759798681, -9.359200813967568422, 50.49621490985803263 ) ) ;
#13304=CIRCLE ( 'NONE', #30651, 1.249999999999999334 ) ;
#13320=PLANE ( 'NONE',  #33021 ) ;
#13336=CARTESIAN_POINT ( 'NONE',  ( -18.05534385759799321, -8.623186033802570094, 49.24843789510466507 ) ) ;
#13337=CARTESIAN_POINT ( 'NONE',  ( -13.91784385650551670, -9.790100578890868377, 49.79778022625163203 ) ) ;
#13367=CARTESIAN_POINT ( 'NONE',  ( -16.44909385541304303, -8.112991634885936776, 51.74999426922421719 ) ) ;
#13387=CARTESIAN_POINT ( 'NONE',  ( 10.57590614458695377, 3.140741878271521514, 50.53406581128081143 ) ) ;
#13388=EDGE_CURVE ( 'NONE', #47374, #27443, #4477, .T. ) ;
#13411=EDGE_CURVE ( 'NONE', #24967, #29446, #38262, .T. ) ;
#13424=CARTESIAN_POINT ( 'NONE',  ( -18.78659385650551528, -9.302874398569244363, 51.68646062012417985 ) ) ;
#13428=CARTESIAN_POINT ( 'NONE',  ( -20.02409385650551599, -6.426201560718813433, 50.50509628382439331 ) ) ;
#13433=AXIS2_PLACEMENT_3D ( 'NONE', #41822, #14948, #22361 ) ;
#13457=EDGE_LOOP ( 'NONE', ( #16756, #31938, #35524, #11626 ) ) ;
#13468=ORIENTED_EDGE ( 'NONE', *, *, #1349, .T. ) ;
#13473=CARTESIAN_POINT ( 'NONE',  ( -17.12409385650551741, -6.426201560718813433, 50.50509628382439331 ) ) ;
#13491=CARTESIAN_POINT ( 'NONE',  ( -21.84909385650551528, -8.104110260919577868, 48.81699501597546487 ) ) ;
#13500=CARTESIAN_POINT ( 'NONE',  ( -33.42409385541304800, -8.109206544743658540, 50.50000000000030553 ) ) ;
#13513=AXIS2_PLACEMENT_3D ( 'NONE', #40930, #48080, #44893 ) ;
#13523=ORIENTED_EDGE ( 'NONE', *, *, #16755, .T. ) ;
#13530=CARTESIAN_POINT ( 'NONE',  ( -19.51784385759799179, -6.860780111191487229, 51.02154966934377001 ) ) ;
#13551=CARTESIAN_POINT ( 'NONE',  ( 25.57590614458706568, 1.890747609047893185, 50.53028072113869484 ) ) ;
#13552=CARTESIAN_POINT ( 'NONE',  ( -36.42409385541304800, -6.859212275519750435, 50.50378509014258555 ) ) ;
#13564=PLANE ( 'NONE',  #14387 ) ;
#13576=CARTESIAN_POINT ( 'NONE',  ( -36.42409385541304800, -6.859212275519750435, 50.50378509014258555 ) ) ;
#13605=CARTESIAN_POINT ( 'NONE',  ( -18.53034385541304374, -6.857644439848013640, 49.98602051094139398 ) ) ;
#13631=DIRECTION ( 'NONE',  ( 1.000000000000000000, -4.164305804376849788E-17, 1.614929280266638808E-16 ) ) ;
#13656=CARTESIAN_POINT ( 'NONE',  ( -17.66159385650551528, -9.295667164867525756, 49.30633214617472504 ) ) ;
#13660=CARTESIAN_POINT ( 'NONE',  ( -18.11159385650551457, -6.922745924619793101, 51.69366785382590024 ) ) ;
#13679=DIRECTION ( 'NONE',  ( 0.000000000000000000, 0.9999954153791273948, 0.003028072113819836077 ) ) ;
#13686=EDGE_CURVE ( 'NONE', #32298, #3630, #45739, .T. ) ;
#13693=CYLINDRICAL_SURFACE ( 'NONE', #6098, 1.249999999999998668 ) ;
#13711=CARTESIAN_POINT ( 'NONE',  ( 18.46573386768564973, 3.114729847419841047, 50.78398819077492732 ) ) ;
#13722=CARTESIAN_POINT ( 'NONE',  ( -19.71159385650551599, -6.922745924619793101, 51.69366785382590024 ) ) ;
#13744=VERTEX_POINT ( 'NONE', #9259 ) ;
#13747=CARTESIAN_POINT ( 'NONE',  ( -14.68034385650551599, -6.424090610841176385, 49.80797279389978627 ) ) ;
#13756=CARTESIAN_POINT ( 'NONE',  ( 18.62590614458706995, 1.904976371434334181, 48.53033133619892681 ) ) ;
#13766=CARTESIAN_POINT ( 'NONE',  ( -19.96784385759798752, -9.357632978295830739, 49.97845033065684106 ) ) ;
#13787=DIRECTION ( 'NONE',  ( 1.000000000000000000, -4.164305804376849172E-17, 1.614929280266638808E-16 ) ) ;
#13801=CARTESIAN_POINT ( 'NONE',  ( -23.17409385650551457, -9.792211528768504536, 50.49490371617623197 ) ) ;
#13804=CARTESIAN_POINT ( 'NONE',  ( 18.07590614458695200, 0.7915096701590282890, 50.27695098796855433 ) ) ;
#13807=CARTESIAN_POINT ( 'NONE',  ( 25.57590614458706568, 1.876874565721113663, 52.48023137145496264 ) ) ;
#13814=CARTESIAN_POINT ( 'NONE',  ( -13.46784385650551741, -6.428312510596451368, 51.20221977374900035 ) ) ;
#13842=CARTESIAN_POINT ( 'NONE',  ( -19.03659385541304516, -8.995762431863214559, 51.38120296130585274 ) ) ;
#13873=CARTESIAN_POINT ( 'NONE',  ( -22.52409385650551954, -6.426201560718812544, 50.50509628382439331 ) ) ;
#13896=CARTESIAN_POINT ( 'NONE',  ( -19.51784385650551457, -9.790100578890868377, 49.79778022625163203 ) ) ;
#13900=CARTESIAN_POINT ( 'NONE',  ( -17.04284385650551670, -8.811426318492348031, 52.18089403414751359 ) ) ;
#13923=ADVANCED_FACE ( 'NONE', ( #4724 ), #8184, .T. ) ;
#13929=VERTEX_POINT ( 'NONE', #41407 ) ;
#13949=CYLINDRICAL_SURFACE ( 'NONE', #37524, 1.249999999999998668 ) ;
#13957=CARTESIAN_POINT ( 'NONE',  ( -18.47409385650551528, -9.792211528768504536, 50.49490371617623197 ) ) ;
#13960=FACE_OUTER_BOUND ( 'NONE', #9668, .T. ) ;
#13978=CARTESIAN_POINT ( 'NONE',  ( -14.84909385759799072, -8.112991634885936776, 51.74999426922421719 ) ) ;
#13981=CARTESIAN_POINT ( 'NONE',  ( -15.18659385650551386, -9.302874398569244363, 51.68646062012417985 ) ) ;
#13983=ORIENTED_EDGE ( 'NONE', *, *, #29935, .F. ) ;
#13991=ORIENTED_EDGE ( 'NONE', *, *, #18032, .F. ) ;
#13995=ORIENTED_EDGE ( 'NONE', *, *, #9932, .F. ) ;
#13996=CARTESIAN_POINT ( 'NONE',  ( -16.70534385759799179, -7.595227055684746986, 51.75156210489594599 ) ) ;
#14057=CARTESIAN_POINT ( 'NONE',  ( -36.42409385541304800, -8.109206544743658540, 50.50000000000030553 ) ) ;
#14078=CARTESIAN_POINT ( 'NONE',  ( -17.91159385541304161, -8.990409506049200417, 49.61344411288074951 ) ) ;
#14086=CARTESIAN_POINT ( 'NONE',  ( -20.02409385759798965, -9.359200813967568422, 50.49621490985803263 ) ) ;
#14097=CARTESIAN_POINT ( 'NONE',  ( -12.97364571557156232, -9.395203622806569399, 49.41430056510258595 ) ) ;
#14114=DIRECTION ( 'NONE',  ( 3.395021121731789346E-32, 0.9999954153791273948, 0.003028072113822188795 ) ) ;
#14128=CARTESIAN_POINT ( 'NONE',  ( -20.02409385650551599, -6.426201560718813433, 50.50509628382439331 ) ) ;
#14135=CARTESIAN_POINT ( 'NONE',  ( -18.33659385650551243, -6.915538690918075382, 49.31353937987644542 ) ) ;
#14166=DIRECTION ( 'NONE',  ( 1.000000000000000000, -4.164305804376849172E-17, 1.614929280266638808E-16 ) ) ;
#14190=ORIENTED_EDGE ( 'NONE', *, *, #31508, .F. ) ;
#14199=CARTESIAN_POINT ( 'NONE',  ( -21.06159385650551741, -9.295667164867525756, 49.30633214617472504 ) ) ;
#14244=CARTESIAN_POINT ( 'NONE',  ( -14.51159385759799214, -8.990409506049202193, 49.61344411288074951 ) ) ;
#14262=ORIENTED_EDGE ( 'NONE', *, *, #24021, .F. ) ;
#14321=CARTESIAN_POINT ( 'NONE',  ( -15.83034385541304623, -6.857644439848013640, 49.98602051094139398 ) ) ;
#14324=CARTESIAN_POINT ( 'NONE',  ( -20.36159385759798823, -7.228003583438117552, 51.38655588711986155 ) ) ;
#14338=FACE_OUTER_BOUND ( 'NONE', #26268, .T. ) ;
#14342=CARTESIAN_POINT ( 'NONE',  ( 18.57590614458695200, 3.149984814396855182, 50.78409494584673922 ) ) ;
#14346=CARTESIAN_POINT ( 'NONE',  ( -22.07409385650551670, -9.792211528768504536, 50.49490371617623197 ) ) ;
#14363=TOROIDAL_SURFACE ( 'NONE', #5772, 1.700000000000000178, 0.2500000000000000000 ) ;
#14364=CARTESIAN_POINT ( 'NONE',  ( -16.67409385650551812, -9.792211528768504536, 50.49490371617623197 ) ) ;
#14370=CARTESIAN_POINT ( 'NONE',  ( -16.64909385650551599, -8.104110260919579645, 48.81699501597546487 ) ) ;
#14372=CARTESIAN_POINT ( 'NONE',  ( -17.99909385650551741, -8.114302828567740988, 52.18300498402516041 ) ) ;
#14376=CYLINDRICAL_SURFACE ( 'NONE', #28384, 1.249999999999998668 ) ;
#14383=CARTESIAN_POINT ( 'NONE',  ( -19.48659385541296274, -7.222650657624008375, 49.61879703869468017 ) ) ;
#14387=AXIS2_PLACEMENT_3D ( 'NONE', #13084, #28118, #16292 ) ;
#14410=ADVANCED_FACE ( 'NONE', ( #10535 ), #13949, .T. ) ;
#14431=CARTESIAN_POINT ( 'NONE',  ( -17.91159385650551528, -6.922745924619793101, 51.69366785382590024 ) ) ;
#14474=CARTESIAN_POINT ( 'NONE',  ( -15.80534385759798965, -7.595227055684746986, 51.75156210489594599 ) ) ;
#14477=CARTESIAN_POINT ( 'NONE',  ( -14.28659385759798894, -7.222650657624104298, 49.61879703869476543 ) ) ;
#14509=CARTESIAN_POINT ( 'NONE',  ( -22.38659385650551670, -9.302874398569244363, 51.68646062012417985 ) ) ;
#14549=CARTESIAN_POINT ( 'NONE',  ( -14.19909385541304125, -8.105421454601382081, 49.25000573077640098 ) ) ;
#14559=ORIENTED_EDGE ( 'NONE', *, *, #3435, .F. ) ;
#14565=CARTESIAN_POINT ( 'NONE',  ( -20.27409385541325904, -6.859212275519745106, 50.50378509014061734 ) ) ;
#14569=CARTESIAN_POINT ( 'NONE',  ( -18.36159385541303735, -7.228003583438111335, 51.38655588711986866 ) ) ;
#14581=DIRECTION ( 'NONE',  ( 3.395021121731789346E-32, 0.9999954153791273948, 0.003028072113822188795 ) ) ;
#14589=CARTESIAN_POINT ( 'NONE',  ( -21.76784385759799179, -9.357632978295825410, 49.97845033065682685 ) ) ;
#14590=FACE_OUTER_BOUND ( 'NONE', #13077, .T. ) ;
#14599=CARTESIAN_POINT ( 'NONE',  ( -13.35534385650551492, -7.417179338643134834, 52.18511593390279302 ) ) ;
#14604=ORIENTED_EDGE ( 'NONE', *, *, #2274, .T. ) ;
#14606=CARTESIAN_POINT ( 'NONE',  ( -13.78034385650551563, -6.424090610841176385, 49.80797279389977916 ) ) ;
#14609=CARTESIAN_POINT ( 'NONE',  ( -14.90534385650551918, -8.801233750844183135, 48.81488406609782515 ) ) ;
#14627=ADVANCED_FACE ( 'NONE', ( #19620 ), #32719, .T. ) ;
#14636=FACE_OUTER_BOUND ( 'NONE', #36534, .T. ) ;
#14675=CARTESIAN_POINT ( 'NONE',  ( -21.11784385650551954, -9.790100578890868377, 49.79778022625163203 ) ) ;
#14678=ADVANCED_FACE ( 'NONE', ( #19755 ), #1950, .T. ) ;
#14692=ORIENTED_EDGE ( 'NONE', *, *, #38942, .T. ) ;
#14712=CARTESIAN_POINT ( 'NONE',  ( -14.17409385759798823, -6.859212275519751323, 50.50378509014259265 ) ) ;
#14754=CARTESIAN_POINT ( 'NONE',  ( -20.13659385650551670, -6.915538690918075382, 49.31353937987644542 ) ) ;
#14771=ORIENTED_EDGE ( 'NONE', *, *, #19715, .T. ) ;
#14772=LINE ( 'NONE', #44871, #31407 ) ;
#14791=FACE_OUTER_BOUND ( 'NONE', #10240, .T. ) ;
#14796=CARTESIAN_POINT ( 'NONE',  ( -14.59284385541304729, -8.630756214087126565, 51.74842643355248129 ) ) ;
#14801=TOROIDAL_SURFACE ( 'NONE', #42370, 1.899999999999999911, 0.1000000000000000056 ) ;
#14830=CARTESIAN_POINT ( 'NONE',  ( 10.57590614458695377, -0.1092432217106413528, 50.52422457691089619 ) ) ;
#14833=CARTESIAN_POINT ( 'NONE',  ( -20.44284385650551883, -8.811426318492348031, 52.18089403414751359 ) ) ;
#14850=CARTESIAN_POINT ( 'NONE',  ( -14.03034385650551563, -9.794322478646142471, 51.19202720610083901 ) ) ;
#14858=CARTESIAN_POINT ( 'NONE',  ( -13.55534385650551243, -7.417179338643134834, 52.18511593390279302 ) ) ;
#14864=CARTESIAN_POINT ( 'NONE',  ( -14.62409385650551386, -6.426201560718813433, 50.50509628382439331 ) ) ;
#14874=CIRCLE ( 'NONE', #38496, 1.049999999999998934 ) ;
#14899=CARTESIAN_POINT ( 'NONE',  ( -14.76159385541304658, -7.228003583438121993, 51.38655588711985445 ) ) ;
#14904=CYLINDRICAL_SURFACE ( 'NONE', #4660, 1.249999999999998668 ) ;
#14913=ORIENTED_EDGE ( 'NONE', *, *, #18392, .F. ) ;
#14923=CARTESIAN_POINT ( 'NONE',  ( -20.27409385541325904, -6.859212275519745106, 50.50378509014061734 ) ) ;
#14932=ORIENTED_EDGE ( 'NONE', *, *, #5805, .T. ) ;
#14933=CARTESIAN_POINT ( 'NONE',  ( -14.93034385650551599, -9.794322478646142471, 51.19202720610083901 ) ) ;
#14948=DIRECTION ( 'NONE',  ( 1.000000000000000000, 1.669677910507523057E-21, 6.493791346278465266E-22 ) ) ;
#14968=TOROIDAL_SURFACE ( 'NONE', #1643, 1.700000000000000178, 0.2500000000000000000 ) ;
#14977=CARTESIAN_POINT ( 'NONE',  ( -14.06159385759798930, -7.228003583438117552, 51.38655588711986155 ) ) ;
#14978=ADVANCED_FACE ( 'NONE', ( #26551 ), #3913, .T. ) ;
#14992=DIRECTION ( 'NONE',  ( 1.000000000000000000, -4.164305804376849172E-17, 1.614929280266638808E-16 ) ) ;
#15001=AXIS2_PLACEMENT_3D ( 'NONE', #22873, #3909, #18915 ) ;
#15004=CARTESIAN_POINT ( 'NONE',  ( -23.29909385595927773, -9.575706171368036479, 50.49555931301712519 ) ) ;
#15013=DIRECTION ( 'NONE',  ( -0.9524241471993249997, -0.0009228828802096092788, 0.3047743298226210373 ) ) ;
#15015=CARTESIAN_POINT ( 'NONE',  ( -22.21784385650551741, -9.790100578890868377, 49.79778022625163203 ) ) ;
#15020=CARTESIAN_POINT ( 'NONE',  ( -14.06159385759798930, -7.228003583438117552, 51.38655588711986155 ) ) ;
#15049=CIRCLE ( 'NONE', #40246, 2.000000000000001776 ) ;
#15053=CARTESIAN_POINT ( 'NONE',  ( -20.64284385759799534, -7.587656875400192291, 49.25157356644813689 ) ) ;
#15054=CARTESIAN_POINT ( 'NONE',  ( -21.23034385541294711, -6.857644439847737416, 49.98602051094152898 ) ) ;
#15060=CARTESIAN_POINT ( 'NONE',  ( -13.86159385541304090, -7.228003583438117552, 51.38655588711986155 ) ) ;
#15063=CARTESIAN_POINT ( 'NONE',  ( -15.91784385759799392, -6.860780111191481900, 51.02154966934377001 ) ) ;
#15064=VECTOR ( 'NONE', #5272, 1000.000000000000000 ) ;
#15066=CARTESIAN_POINT ( 'NONE',  ( -13.72409385759798894, -9.359200813967568422, 50.49621490985803263 ) ) ;
#15076=VERTEX_POINT ( 'NONE', #701 ) ;
#15087=ORIENTED_EDGE ( 'NONE', *, *, #21366, .F. ) ;
#15094=CARTESIAN_POINT ( 'NONE',  ( 25.57590614458706568, 1.890747609047893185, 50.53028072113869484 ) ) ;
#15095=CARTESIAN_POINT ( 'NONE',  ( -20.21784385650551386, -9.790100578890868377, 49.79778022625163203 ) ) ;
#15099=LINE ( 'NONE', #18550, #2195 ) ;
#15110=CARTESIAN_POINT ( 'NONE',  ( -14.48034385650551847, -6.424090610841176385, 49.80797279389977916 ) ) ;
#15118=CARTESIAN_POINT ( 'NONE',  ( -16.25534385650551528, -7.417179338643134834, 52.18511593390279302 ) ) ;
#15122=CARTESIAN_POINT ( 'NONE',  ( -14.28659385650551528, -9.302874398569244363, 51.68646062012417985 ) ) ;
#15126=ADVANCED_FACE ( 'NONE', ( #12743 ), #20131, .T. ) ;
#15148=DIRECTION ( 'NONE',  ( 0.000000000000000000, 0.007114381193220344589, -0.9999746924698832418 ) ) ;
#15181=CARTESIAN_POINT ( 'NONE',  ( -14.70534385650551989, -8.801233750844183135, 48.81488406609782515 ) ) ;
#15210=ORIENTED_EDGE ( 'NONE', *, *, #45495, .T. ) ;
#15220=EDGE_LOOP ( 'NONE', ( #39244, #9509, #22357, #9610 ) ) ;
#15225=CARTESIAN_POINT ( 'NONE',  ( -22.24284385650551954, -8.811426318492348031, 52.18089403414751359 ) ) ;
#15262=CARTESIAN_POINT ( 'NONE',  ( -20.53034385650551386, -9.794322478646142471, 51.19202720610083190 ) ) ;
#15264=( BOUNDED_CURVE ( )  B_SPLINE_CURVE ( 2, ( #38663, #46055, #12796, #20188, #27336, #27820, #13029, #8639, #5673 ),
 .UNSPECIFIED., .F., .F. ) 
 B_SPLINE_CURVE_WITH_KNOTS ( ( 3, 2, 2, 2, 3 ),
 ( 0.06294472996427230571, 0.06392819047740837257, 0.06491165099054443943, 0.06589511150368049242, 0.06687857201681655928 ),
 .UNSPECIFIED. ) 
 CURVE ( )  GEOMETRIC_REPRESENTATION_ITEM ( )  RATIONAL_B_SPLINE_CURVE ( ( 0.9999999999999537037, 0.9238795325113330348, 1.000000000000000000, 0.9238795325112867385, 1.000000000000000000, 0.9238795325112867385, 1.000000000000000000, 0.9238795325112624246, 1.000000000000024425 ) ) 
 REPRESENTATION_ITEM ( '' )  );
#15269=CARTESIAN_POINT ( 'NONE',  ( -22.07409385541323488, -6.859212275519745994, 50.50378509014079498 ) ) ;
#15297=CARTESIAN_POINT ( 'NONE',  ( -13.97409385541304161, -6.859212275519751323, 50.50378509014259265 ) ) ;
#15300=CARTESIAN_POINT ( 'NONE',  ( -23.19909385541299685, -8.105421454601382081, 49.25000573077632993 ) ) ;
#15314=ORIENTED_EDGE ( 'NONE', *, *, #47727, .F. ) ;
#15318=CARTESIAN_POINT ( 'NONE',  ( -18.02409385541303877, -9.359200813967568422, 50.49621490985803263 ) ) ;
#15333=DIRECTION ( 'NONE',  ( 4.115385489419890895E-17, 0.9999954153791273948, 0.003028072113818697231 ) ) ;
#15334=CARTESIAN_POINT ( 'NONE',  ( -18.08034385650551812, -6.424090610841176385, 49.80797279389978627 ) ) ;
#15340=CARTESIAN_POINT ( 'NONE',  ( -21.71159385759798965, -8.990409506049200417, 49.61344411288074951 ) ) ;
#15348=CARTESIAN_POINT ( 'NONE',  ( -13.58034385650551812, -6.424090610841176385, 49.80797279389977916 ) ) ;
#15357=CARTESIAN_POINT ( 'NONE',  ( -13.27409385650551599, -9.792211528768504536, 50.49490371617623197 ) ) ;
#15359=CARTESIAN_POINT ( 'NONE',  ( -16.14284385650552167, -8.811426318492348031, 52.18089403414751359 ) ) ;
#15383=CIRCLE ( 'NONE', #21693, 1.249999999999999334 ) ;
#15402=EDGE_LOOP ( 'NONE', ( #21374, #44757, #40732, #26712 ) ) ;
#15408=CARTESIAN_POINT ( 'NONE',  ( -19.14909385541296061, -8.112991634885936776, 51.74999426922435219 ) ) ;
#15415=DIRECTION ( 'NONE',  ( 0.000000000000000000, 1.000000000000000000, 0.000000000000000000 ) ) ;
#15419=CARTESIAN_POINT ( 'NONE',  ( -14.81784385650551528, -9.790100578890868377, 49.79778022625163203 ) ) ;
#15465=CARTESIAN_POINT ( 'NONE',  ( -22.69284385650552238, -7.406986770994973490, 48.81910596585309747 ) ) ;
#15477=VERTEX_POINT ( 'NONE', #24267 ) ;
#15484=CARTESIAN_POINT ( 'NONE',  ( -13.72409385759798894, -9.359200813967568422, 50.49621490985803263 ) ) ;
#15502=CARTESIAN_POINT ( 'NONE',  ( -20.30534385650551599, -8.801233750844183135, 48.81488406609782515 ) ) ;
#15557=VECTOR ( 'NONE', #16790, 1000.000000000000000 ) ;
#15566=VECTOR ( 'NONE', #45232, 1000.000000000000000 ) ;
#15567=ADVANCED_FACE ( 'NONE', ( #48595 ), #37566, .T. ) ;
#15576=CARTESIAN_POINT ( 'NONE',  ( -20.61159385650551812, -6.922745924619793101, 51.69366785382590024 ) ) ;
#15593=CARTESIAN_POINT ( 'NONE',  ( -16.16784385650552025, -6.428312510596451368, 51.20221977374900035 ) ) ;
#15606=CARTESIAN_POINT ( 'NONE',  ( -14.51159385650551492, -6.922745924619793101, 51.69366785382590024 ) ) ;
#15626=AXIS2_PLACEMENT_3D ( 'NONE', #17210, #24865, #16725 ) ;
#15641=CARTESIAN_POINT ( 'NONE',  ( -14.08659385541286468, -7.222650657623884918, 49.61879703869455227 ) ) ;
#15663=CARTESIAN_POINT ( 'NONE',  ( -20.04909385541303024, -8.112991634885936776, 51.74999426922423851 ) ) ;
#15672=ORIENTED_EDGE ( 'NONE', *, *, #18878, .F. ) ;
#15674=CARTESIAN_POINT ( 'NONE',  ( -14.42409385650551457, -6.426201560718813433, 50.50509628382439331 ) ) ;
#15676=AXIS2_PLACEMENT_3D ( 'NONE', #48482, #21190, #3429 ) ;
#15698=FACE_OUTER_BOUND ( 'NONE', #37868, .T. ) ;
#15700=ORIENTED_EDGE ( 'NONE', *, *, #27020, .T. ) ;
#15710=ORIENTED_EDGE ( 'NONE', *, *, #43023, .T. ) ;
#15715=CARTESIAN_POINT ( 'NONE',  ( -22.01784385650551812, -9.790100578890868377, 49.79778022625162492 ) ) ;
#15755=CARTESIAN_POINT ( 'NONE',  ( -18.39284385650552167, -7.406986770994972602, 48.81910596585309747 ) ) ;
#15762=CARTESIAN_POINT ( 'NONE',  ( -16.39284385541304800, -8.630756214087126565, 51.74842643355248129 ) ) ;
#15775=CARTESIAN_POINT ( 'NONE',  ( -20.92409385759799179, -9.359200813967568422, 50.49621490985803263 ) ) ;
#15783=DIRECTION ( 'NONE',  ( -1.616182858256117057E-16, -0.003028072113818697231, 0.9999954153791273948 ) ) ;
#15801=EDGE_CURVE ( 'NONE', #10524, #16810, #32072, .T. ) ;
#15816=DIRECTION ( 'NONE',  ( 2.231660450020913271E-16, 0.9999954153791273948, 0.003028072113822188795 ) ) ;
#15821=FACE_OUTER_BOUND ( 'NONE', #5035, .T. ) ;
#15828=CARTESIAN_POINT ( 'NONE',  ( -19.20534385650551457, -8.801233750844183135, 48.81488406609782515 ) ) ;
#15830=CIRCLE ( 'NONE', #12676, 1.249999999999999556 ) ;
#15836=CARTESIAN_POINT ( 'NONE',  ( -35.42409385541304800, -7.059211358595575803, 50.50317947571981847 ) ) ;
#15839=CARTESIAN_POINT ( 'NONE',  ( -36.42409385541304800, -9.359200813967566646, 50.49621490985803263 ) ) ;
#15847=CIRCLE ( 'NONE', #17430, 1.249999999999999556 ) ;
#15854=CARTESIAN_POINT ( 'NONE',  ( -21.62409385541304374, -9.359200813967568422, 50.49621490985803263 ) ) ;
#15873=ORIENTED_EDGE ( 'NONE', *, *, #45753, .F. ) ;
#15888=CARTESIAN_POINT ( 'NONE',  ( -14.19909385541286362, -8.105421454601380304, 49.25000573077609545 ) ) ;
#15917=CARTESIAN_POINT ( 'NONE',  ( -14.14284385650552167, -8.811426318492348031, 52.18089403414752070 ) ) ;
#15958=CARTESIAN_POINT ( 'NONE',  ( -13.21784385759799108, -6.860780111191488118, 51.02154966934377711 ) ) ;
#15966=AXIS2_PLACEMENT_3D ( 'NONE', #1594, #28435, #39510 ) ;
#15996=CARTESIAN_POINT ( 'NONE',  ( -18.22409385650551528, -6.426201560718813433, 50.50509628382439331 ) ) ;
#16014=CARTESIAN_POINT ( 'NONE',  ( -22.21784385759799108, -6.860780111191487229, 51.02154966934377001 ) ) ;
#16025=DIRECTION ( 'NONE',  ( 1.000000000000000000, -4.164305804376849788E-17, 1.614929280266638808E-16 ) ) ;
#16034=VECTOR ( 'NONE', #47635, 1000.000000000000000 ) ;
#16063=CARTESIAN_POINT ( 'NONE',  ( -14.59284385650551741, -7.406986770994972602, 48.81910596585309747 ) ) ;
#16088=CARTESIAN_POINT ( 'NONE',  ( -20.55534385541304232, -8.623186033802570094, 49.24843789510466507 ) ) ;
#16118=CARTESIAN_POINT ( 'NONE',  ( -36.42409385541304800, -9.359200813967566646, 50.49621490985803263 ) ) ;
#16141=VERTEX_POINT ( 'NONE', #36112 ) ;
#16144=CARTESIAN_POINT ( 'NONE',  ( -22.61159385650551457, -6.922745924619793101, 51.69366785382590024 ) ) ;
#16151=CARTESIAN_POINT ( 'NONE',  ( -22.94909385650551314, -8.104110260919577868, 48.81699501597546487 ) ) ;
#16167=ORIENTED_EDGE ( 'NONE', *, *, #5052, .T. ) ;
#16187=CARTESIAN_POINT ( 'NONE',  ( -33.42409385541304800, -8.109206544743658540, 50.50000000000030553 ) ) ;
#16194=CARTESIAN_POINT ( 'NONE',  ( -20.21784385650551386, -9.790100578890868377, 49.79778022625163203 ) ) ;
#16205=CARTESIAN_POINT ( 'NONE',  ( -22.74909385541299400, -8.112991634885936776, 51.74999426922429535 ) ) ;
#16217=PRODUCT_DEFINITION ( 'UNKNOWN', '', #46344, #38610 ) ;
#16231=CARTESIAN_POINT ( 'NONE',  ( -17.26784385650551457, -6.428312510596451368, 51.20221977374900035 ) ) ;
#16240=DIRECTION ( 'NONE',  ( 1.000000000000000000, 1.669677910507523057E-21, 6.493791346278465266E-22 ) ) ;
#16270=CARTESIAN_POINT ( 'NONE',  ( -23.36784385541299613, -9.357632978295908899, 49.97845033065679843 ) ) ;
#16292=DIRECTION ( 'NONE',  ( -4.115385489419834812E-17, -0.9999954153791273948, -0.003028072113822188795 ) ) ;
#16304=CARTESIAN_POINT ( 'NONE',  ( -15.99909385650551741, -8.114302828567740988, 52.18300498402516041 ) ) ;
#16311=AXIS2_PLACEMENT_3D ( 'NONE', #27040, #42066, #38606 ) ;
#16316=LINE ( 'NONE', #2042, #20790 ) ;
#16329=CARTESIAN_POINT ( 'NONE',  ( -22.97409385541304516, -6.859212275519751323, 50.50378509014259265 ) ) ;
#16349=CARTESIAN_POINT ( 'NONE',  ( -36.42409385541304800, -8.109206544743658540, 50.50000000000030553 ) ) ;
#16353=VERTEX_POINT ( 'NONE', #38547 ) ;
#16354=CARTESIAN_POINT ( 'NONE',  ( -13.97409385541301496, -6.859212275519754876, 50.50378509014287687 ) ) ;
#16379=CARTESIAN_POINT ( 'NONE',  ( 18.57590614458695200, 2.144561833755798563, 49.27104351578929453 ) ) ;
#16400=CARTESIAN_POINT ( 'NONE',  ( -23.00534385650551528, -8.801233750844183135, 48.81488406609782515 ) ) ;
#16408=CARTESIAN_POINT ( 'NONE',  ( -20.78034385541293716, -9.360768649639700456, 51.01397948905896840 ) ) ;
#16419=VERTEX_POINT ( 'NONE', #21776 ) ;
#16445=CARTESIAN_POINT ( 'NONE',  ( -19.88034385650552238, -6.424090610841174609, 49.80797279389977916 ) ) ;
#16463=VERTEX_POINT ( 'NONE', #47411 ) ;
#16468=AXIS2_PLACEMENT_3D ( 'NONE', #39446, #9415, #13078 ) ;
#16477=ADVANCED_FACE ( 'NONE', ( #6764 ), #11685, .T. ) ;
#16478=CARTESIAN_POINT ( 'NONE',  ( -16.87409385759798752, -6.859212275519751323, 50.50378509014259265 ) ) ;
#16485=CARTESIAN_POINT ( 'NONE',  ( -16.59284385650551741, -7.406986770994972602, 48.81910596585309747 ) ) ;
#16509=CARTESIAN_POINT ( 'NONE',  ( 18.57590614458706924, 1.890747609047612077, 50.53028072113853142 ) ) ;
#16554=DIRECTION ( 'NONE',  ( 1.000000000000000000, -4.164305804376849172E-17, 1.614929280266638808E-16 ) ) ;
#16555=CARTESIAN_POINT ( 'NONE',  ( -17.85534385650552025, -7.417179338643134834, 52.18511593390279302 ) ) ;
#16564=CARTESIAN_POINT ( 'NONE',  ( 22.62590614458706639, 1.876874565721113663, 52.48023137145496264 ) ) ;
#16580=CARTESIAN_POINT ( 'NONE',  ( -21.51159385541304303, -8.990409506049200417, 49.61344411288074951 ) ) ;
#16596=EDGE_CURVE ( 'NONE', #45882, #30416, #100, .T. ) ;
#16605=CARTESIAN_POINT ( 'NONE',  ( -19.74284385759798965, -7.587656875400192291, 49.25157356644813689 ) ) ;
#16608=ORIENTED_EDGE ( 'NONE', *, *, #6116, .T. ) ;
#16633=LINE ( 'NONE', #31180, #6691 ) ;
#16641=CARTESIAN_POINT ( 'NONE',  ( -20.30534385650551243, -8.801233750844183135, 48.81488406609782515 ) ) ;
#16647=CARTESIAN_POINT ( 'NONE',  ( -21.65534385650552096, -7.417179338643134834, 52.18511593390279302 ) ) ;
#16655=VERTEX_POINT ( 'NONE', #45898 ) ;
#16668=ORIENTED_EDGE ( 'NONE', *, *, #34090, .T. ) ;
#16670=CARTESIAN_POINT ( 'NONE',  ( 18.87590614458706995, 1.904620652374673151, 48.58033007082241994 ) ) ;
#16685=CARTESIAN_POINT ( 'NONE',  ( -18.64284385650551812, -8.811426318492348031, 52.18089403414751359 ) ) ;
#16697=DIRECTION ( 'NONE',  ( 1.000000000000000000, -4.164305804376849172E-17, 1.614929280266638808E-16 ) ) ;
#16714=EDGE_LOOP ( 'NONE', ( #32731, #5583, #8523, #5229 ) ) ;
#16721=CARTESIAN_POINT ( 'NONE',  ( -18.16784385650552025, -6.428312510596451368, 51.20221977374900035 ) ) ;
#16725=DIRECTION ( 'NONE',  ( 4.115385489419834812E-17, 0.9999954153791273948, 0.003028072113822188795 ) ) ;
#16740=CARTESIAN_POINT ( 'NONE',  ( -19.85534385759799036, -8.623186033802570094, 49.24843789510466507 ) ) ;
#16748=CARTESIAN_POINT ( 'NONE',  ( 18.51825960693461681, 0.6486925162843356629, 50.69417723405735643 ) ) ;
#16753=ORIENTED_EDGE ( 'NONE', *, *, #45488, .T. ) ;
#16755=EDGE_CURVE ( 'NONE', #3147, #35561, #38765, .T. ) ;
#16756=ORIENTED_EDGE ( 'NONE', *, *, #30482, .F. ) ;
#16783=CARTESIAN_POINT ( 'NONE',  ( -20.92409385759799179, -9.359200813967568422, 50.49621490985803263 ) ) ;
#16790=DIRECTION ( 'NONE',  ( 1.000000000000000000, -4.164305804376849172E-17, 1.614929280266638808E-16 ) ) ;
#16795=CARTESIAN_POINT ( 'NONE',  ( -16.05534385650551599, -7.417179338643134834, 52.18511593390279302 ) ) ;
#16810=VERTEX_POINT ( 'NONE', #33758 ) ;
#16818=CARTESIAN_POINT ( 'NONE',  ( -17.79909385541304445, -8.105421454601382081, 49.25000573077640098 ) ) ;
#16826=ORIENTED_EDGE ( 'NONE', *, *, #6275, .T. ) ;
#16848=CARTESIAN_POINT ( 'NONE',  ( -13.42364920204782841, -9.064338107659910548, 49.69363550579117117 ) ) ;
#16853=VERTEX_POINT ( 'NONE', #18251 ) ;
#16861=ORIENTED_EDGE ( 'NONE', *, *, #23169, .T. ) ;
#16872=CARTESIAN_POINT ( 'NONE',  ( -20.24909385650551386, -8.104110260919579645, 48.81699501597546487 ) ) ;
#16878=CARTESIAN_POINT ( 'NONE',  ( -21.14909385650551599, -8.104110260919577868, 48.81699501597546487 ) ) ;
#16904=ADVANCED_FACE ( 'NONE', ( #30588 ), #35309, .T. ) ;
#16924=CARTESIAN_POINT ( 'NONE',  ( -18.92409385650551812, -6.426201560718813433, 50.50509628382439331 ) ) ;
#16945=DIRECTION ( 'NONE',  ( -1.000000000000000000, 4.164305804376849172E-17, -1.614929280266638808E-16 ) ) ;
#16947=CYLINDRICAL_SURFACE ( 'NONE', #6861, 2.000000000000001776 ) ;
#16949=ORIENTED_EDGE ( 'NONE', *, *, #8390, .F. ) ;
#16960=CARTESIAN_POINT ( 'NONE',  ( -15.41159385650551705, -6.922745924619793101, 51.69366785382590024 ) ) ;
#16976=CARTESIAN_POINT ( 'NONE',  ( -19.91159385759799250, -8.990409506049200417, 49.61344411288074951 ) ) ;
#17008=CARTESIAN_POINT ( 'NONE',  ( -18.50534385759798894, -7.595227055684746986, 51.75156210489594599 ) ) ;
#17020=DIRECTION ( 'NONE',  ( 0.3047757271037812576, 0.9524197806957001022, 0.002884009000665203448 ) ) ;
#17027=CARTESIAN_POINT ( 'NONE',  ( -16.28034385650551741, -6.424090610841176385, 49.80797279389978627 ) ) ;
#17033=DIRECTION ( 'NONE',  ( 0.000000000000000000, 0.9999954153791273948, 0.003028072113819836077 ) ) ;
#17058=CARTESIAN_POINT ( 'NONE',  ( -17.34909385541304161, -8.112991634885936776, 51.74999426922421719 ) ) ;
#17075=DIRECTION ( 'NONE',  ( -1.000000000000000000, -1.669677910507523057E-21, -6.493791346278465266E-22 ) ) ;
#17102=VERTEX_POINT ( 'NONE', #21009 ) ;
#17107=CARTESIAN_POINT ( 'NONE',  ( -15.29909385759798823, -8.105421454601382081, 49.25000573077640098 ) ) ;
#17112=CARTESIAN_POINT ( 'NONE',  ( -19.23659385650551457, -6.915538690918075382, 49.31353937987644542 ) ) ;
#17115=CARTESIAN_POINT ( 'NONE',  ( -20.81159385650551386, -6.922745924619793101, 51.69366785382590024 ) ) ;
#17116=CIRCLE ( 'NONE', #47011, 1.949999999999999734 ) ;
#17122=CARTESIAN_POINT ( 'NONE',  ( 18.46573386768564973, 1.637040139411225059, 51.75426295951076838 ) ) ;
#17130=DIRECTION ( 'NONE',  ( 4.115385489419834196E-17, 0.9999954153791273948, 0.003028072113822188795 ) ) ;
#17142=ADVANCED_FACE ( 'NONE', ( #9928, #25429 ), #36011, .F. ) ;
#17159=CARTESIAN_POINT ( 'NONE',  ( -17.23659385650551812, -6.915538690918074494, 49.31353937987644542 ) ) ;
#17177=CARTESIAN_POINT ( 'NONE',  ( -21.34284385650552096, -8.811426318492348031, 52.18089403414751359 ) ) ;
#17190=CARTESIAN_POINT ( 'NONE',  ( 18.62590614458706995, 1.902842057076367777, 48.83032374393989272 ) ) ;
#17196=EDGE_LOOP ( 'NONE', ( #32873, #42572, #26582, #6626 ) ) ;
#17205=CARTESIAN_POINT ( 'NONE',  ( -14.17409385650551457, -9.792211528768504536, 50.49490371617623197 ) ) ;
#17206=CIRCLE ( 'NONE', #48685, 0.2499999999999976408 ) ;
#17210=CARTESIAN_POINT ( 'NONE',  ( 8.575906144586951996, 11.88994474481043184, 50.81056029612154390 ) ) ;
#17230=CARTESIAN_POINT ( 'NONE',  ( -18.67409385759799179, -6.859212275519751323, 50.50378509014259265 ) ) ;
#17236=DIRECTION ( 'NONE',  ( -1.669677910507523245E-21, 1.000000000000000000, -1.084253996632606407E-42 ) ) ;
#17280=CARTESIAN_POINT ( 'NONE',  ( -14.08659385650551776, -9.302874398569244363, 51.68646062012417985 ) ) ;
#17306=ORIENTED_EDGE ( 'NONE', *, *, #2242, .T. ) ;
#17307=CARTESIAN_POINT ( 'NONE',  ( -18.75534385541304516, -8.623186033802570094, 49.24843789510466507 ) ) ;
#17360=CARTESIAN_POINT ( 'NONE',  ( -22.27409385759798965, -6.859212275519751323, 50.50378509014259265 ) ) ;
#17365=CARTESIAN_POINT ( 'NONE',  ( -19.46159385650551599, -9.295667164867525756, 49.30633214617472504 ) ) ;
#17370=CARTESIAN_POINT ( 'NONE',  ( -17.38034385650551528, -6.424090610841176385, 49.80797279389977916 ) ) ;
#17380=CARTESIAN_POINT ( 'NONE',  ( -16.87409385759798752, -6.859212275519751323, 50.50378509014259265 ) ) ;
#17412=CIRCLE ( 'NONE', #4855, 2.000000000000000000 ) ;
#17418=CARTESIAN_POINT ( 'NONE',  ( -18.81159385650551741, -6.922745924619793101, 51.69366785382590024 ) ) ;
#17429=EDGE_CURVE ( 'NONE', #16141, #3147, #37939, .T. ) ;
#17430=AXIS2_PLACEMENT_3D ( 'NONE', #21488, #43662, #17033 ) ;
#17436=CARTESIAN_POINT ( 'NONE',  ( -20.66784385650552380, -6.428312510596450480, 51.20221977374900035 ) ) ;
#17459=CARTESIAN_POINT ( 'NONE',  ( -15.46784385650551918, -6.428312510596451368, 51.20221977374900035 ) ) ;
#17476=CARTESIAN_POINT ( 'NONE',  ( -17.21159385759798965, -8.990409506049200417, 49.61344411288074951 ) ) ;
#17478=ADVANCED_FACE ( 'NONE', ( #27591 ), #4956, .T. ) ;
#17495=DIRECTION ( 'NONE',  ( 1.000000000000000000, -4.164305804376849172E-17, 1.614929280266638808E-16 ) ) ;
#17501=ORIENTED_EDGE ( 'NONE', *, *, #15801, .F. ) ;
#17504=CARTESIAN_POINT ( 'NONE',  ( 7.325906144586951996, -6.109215713985405749, 50.50605614422795497 ) ) ;
#17529=PLANE ( 'NONE',  #40718 ) ;
#17535=CARTESIAN_POINT ( 'NONE',  ( -18.92409385541303024, -9.359200813967568422, 50.49621490985794026 ) ) ;
#17551=CARTESIAN_POINT ( 'NONE',  ( -18.36159385541304090, -7.228003583438117552, 51.38655588711986155 ) ) ;
#17554=CYLINDRICAL_SURFACE ( 'NONE', #24499, 1.249999999999998668 ) ;
#17558=EDGE_LOOP ( 'NONE', ( #34739, #6193, #35718, #21761 ) ) ;
#17581=CARTESIAN_POINT ( 'NONE',  ( -21.79284385650551670, -7.406986770994972602, 48.81910596585309747 ) ) ;
#17599=ORIENTED_EDGE ( 'NONE', *, *, #33455, .F. ) ;
#17600=CARTESIAN_POINT ( 'NONE',  ( -17.71784385650551741, -9.790100578890868377, 49.79778022625163203 ) ) ;
#17601=EDGE_CURVE ( 'NONE', #17102, #1741, #17935, .T. ) ;
#17604=CARTESIAN_POINT ( 'NONE',  ( -20.08034385650552167, -6.424090610841176385, 49.80797279389977916 ) ) ;
#17652=CARTESIAN_POINT ( 'NONE',  ( -14.87409385541153917, -6.859212275519794844, 50.50378509015643402 ) ) ;
#17668=CARTESIAN_POINT ( 'NONE',  ( -18.92409385650551812, -6.426201560718813433, 50.50509628382439331 ) ) ;
#17690=CARTESIAN_POINT ( 'NONE',  ( -13.22466687598806523, -9.790356633151166221, 49.88233999786937289 ) ) ;
#17695=VERTEX_POINT ( 'NONE', #8344 ) ;
#17707=CARTESIAN_POINT ( 'NONE',  ( -17.83034385759799179, -6.857644439848013640, 49.98602051094139398 ) ) ;
#17723=CARTESIAN_POINT ( 'NONE',  ( -15.21159385541304587, -8.990409506049200417, 49.61344411288074951 ) ) ;
#17742=CARTESIAN_POINT ( 'NONE',  ( -23.00534385650551172, -8.801233750844183135, 48.81488406609782515 ) ) ;
#17762=CARTESIAN_POINT ( 'NONE',  ( -18.64284385541303735, -7.587656875400188738, 49.25157356644812978 ) ) ;
#17765=( BOUNDED_CURVE ( )  B_SPLINE_CURVE ( 2, ( #20798, #27452, #23531, #20570, #4813, #16605, #31145, #42487, #8762 ),
 .UNSPECIFIED., .F., .F. ) 
 B_SPLINE_CURVE_WITH_KNOTS ( ( 3, 2, 2, 2, 3 ),
 ( 0.2500000000000001110, 0.2604166666666667407, 0.2708333333333333703, 0.2812500000000000000, 0.2916666666666666297 ),
 .UNSPECIFIED. ) 
 CURVE ( )  GEOMETRIC_REPRESENTATION_ITEM ( )  RATIONAL_B_SPLINE_CURVE ( ( 0.9999999999999992228, 0.9238795325112875156, 1.000000000000000000, 0.9238795325112867385, 1.000000000000000000, 0.9238795325112867385, 1.000000000000000000, 0.9238795325112871826, 0.9999999999999995559 ) ) 
 REPRESENTATION_ITEM ( '' )  );
#17785=CARTESIAN_POINT ( 'NONE',  ( -16.84284385541304729, -7.587656875400192291, 49.25157356644813689 ) ) ;
#17793=CARTESIAN_POINT ( 'NONE',  ( 18.62590614458706995, 1.878653161019418816, 52.23023769833749697 ) ) ;
#17813=CARTESIAN_POINT ( 'NONE',  ( -22.46784385650551741, -6.428312510596449592, 51.20221977374900035 ) ) ;
#17825=VERTEX_POINT ( 'NONE', #1677 ) ;
#17834=CARTESIAN_POINT ( 'NONE',  ( -17.60534385650551670, -8.801233750844183135, 48.81488406609782515 ) ) ;
#17837=CARTESIAN_POINT ( 'NONE',  ( -20.58659385650551599, -9.302874398569244363, 51.68646062012417985 ) ) ;
#17839=EDGE_CURVE ( 'NONE', #13744, #18062, #14874, .T. ) ;
#17857=CARTESIAN_POINT ( 'NONE',  ( -16.84284385541304374, -7.587656875400191403, 49.25157356644812978 ) ) ;
#17869=CARTESIAN_POINT ( 'NONE',  ( -36.42409385541304800, -9.359200813967566646, 50.49621490985803263 ) ) ;
#17899=CARTESIAN_POINT ( 'NONE',  ( -18.64284385650551812, -8.811426318492348031, 52.18089403414751359 ) ) ;
#17927=CARTESIAN_POINT ( 'NONE',  ( -14.84909385650551705, -8.104110260919579645, 48.81699501597546487 ) ) ;
#17930=DIRECTION ( 'NONE',  ( 1.000000000000000000, 1.669677910507523057E-21, 6.493791346278465266E-22 ) ) ;
#17935=LINE ( 'NONE', #13756, #29036 ) ;
#17943=CARTESIAN_POINT ( 'NONE',  ( -15.41159385759799072, -8.990409506049202193, 49.61344411288074951 ) ) ;
#17948=AXIS2_PLACEMENT_3D ( 'NONE', #47882, #36762, #14114 ) ;
#17962=CYLINDRICAL_SURFACE ( 'NONE', #37414, 1.249999999999998668 ) ;
#17964=CYLINDRICAL_SURFACE ( 'NONE', #43189, 1.949999999999999734 ) ;
#17990=VERTEX_POINT ( 'NONE', #8064 ) ;
#17996=CARTESIAN_POINT ( 'NONE',  ( -13.80534385650551776, -8.801233750844183135, 48.81488406609782515 ) ) ;
#17998=VERTEX_POINT ( 'NONE', #419 ) ;
#18003=CARTESIAN_POINT ( 'NONE',  ( -13.78034385650551563, -6.424090610841176385, 49.80797279389977916 ) ) ;
#18010=DIRECTION ( 'NONE',  ( 0.000000000000000000, 0.9999954153791273948, 0.003028072113821686159 ) ) ;
#18024=CARTESIAN_POINT ( 'NONE',  ( -16.05534385541304232, -8.623186033802570094, 49.24843789510467218 ) ) ;
#18032=EDGE_CURVE ( 'NONE', #17998, #21919, #26543, .T. ) ;
#18062=VERTEX_POINT ( 'NONE', #48421 ) ;
#18077=EDGE_LOOP ( 'NONE', ( #8075, #3965, #5721, #941 ) ) ;
#18078=CARTESIAN_POINT ( 'NONE',  ( -16.81784385650551528, -9.790100578890868377, 49.79778022625163203 ) ) ;
#18083=CARTESIAN_POINT ( 'NONE',  ( -17.09909385650551528, -8.114302828567740988, 52.18300498402516041 ) ) ;
#18085=AXIS2_PLACEMENT_3D ( 'NONE', #7465, #45136, #25662 ) ;
#18098=CARTESIAN_POINT ( 'NONE',  ( -17.51784385541255773, -6.860780111193798270, 51.02154966934632796 ) ) ;
#18150=CARTESIAN_POINT ( 'NONE',  ( -18.58659385650551599, -9.302874398569244363, 51.68646062012417985 ) ) ;
#18194=CARTESIAN_POINT ( 'NONE',  ( -14.28659385759798894, -7.222650657624104298, 49.61879703869476543 ) ) ;
#18230=CARTESIAN_POINT ( 'NONE',  ( -22.33034385650551812, -9.794322478646142471, 51.19202720610083190 ) ) ;
#18234=DIRECTION ( 'NONE',  ( 1.000000000000000000, 1.669677910507523057E-21, 6.493791346278465266E-22 ) ) ;
#18250=DIRECTION ( 'NONE',  ( 1.000000000000000000, -4.164305804376849172E-17, 1.614929280266638808E-16 ) ) ;
#18251=CARTESIAN_POINT ( 'NONE',  ( 18.46573386768564973, 0.6652513346184721899, 50.77657095919170871 ) ) ;
#18265=CARTESIAN_POINT ( 'NONE',  ( -20.58659385759798965, -7.222650657624104298, 49.61879703869476543 ) ) ;
#18271=CARTESIAN_POINT ( 'NONE',  ( -14.76159385541304303, -7.228003583438117552, 51.38655588711986155 ) ) ;
#18274=CARTESIAN_POINT ( 'NONE',  ( -15.69284385759799427, -8.630756214087126565, 51.74842643355248129 ) ) ;
#18282=CARTESIAN_POINT ( 'NONE',  ( -18.89909385759798965, -8.105421454601382081, 49.25000573077640098 ) ) ;
#18287=CARTESIAN_POINT ( 'NONE',  ( -18.47409385541327964, -6.859212275519742441, 50.50378509014038997 ) ) ;
#18308=CARTESIAN_POINT ( 'NONE',  ( -17.63034385541255489, -6.857644439845357986, 49.98602051094380982 ) ) ;
#18313=AXIS2_PLACEMENT_3D ( 'NONE', #27934, #17075, #32125 ) ;
#18314=CARTESIAN_POINT ( 'NONE',  ( -15.83034385650551634, -9.794322478646142471, 51.19202720610083901 ) ) ;
#18324=CARTESIAN_POINT ( 'NONE',  ( -13.72409385650551528, -6.426201560718813433, 50.50509628382439331 ) ) ;
#18329=CARTESIAN_POINT ( 'NONE',  ( -14.11784385650551954, -9.790100578890868377, 49.79778022625163203 ) ) ;
#18363=CARTESIAN_POINT ( 'NONE',  ( -14.48034385541302527, -9.360768649639460648, 51.01397948905905366 ) ) ;
#18369=ORIENTED_EDGE ( 'NONE', *, *, #45144, .F. ) ;
#18383=ORIENTED_EDGE ( 'NONE', *, *, #16596, .F. ) ;
#18392=EDGE_CURVE ( 'NONE', #12877, #47438, #13304, .T. ) ;
#18395=CARTESIAN_POINT ( 'NONE',  ( -17.63034385650551528, -9.794322478646142471, 51.19202720610083901 ) ) ;
#18432=CARTESIAN_POINT ( 'NONE',  ( -14.62409385759799108, -9.359200813967568422, 50.49621490985803263 ) ) ;
#18447=AXIS2_PLACEMENT_3D ( 'NONE', #7393, #37897, #22643 ) ;
#18451=FILL_AREA_STYLE_COLOUR ( '', #921 ) ;
#18456=EDGE_CURVE ( 'NONE', #29639, #31825, #22773, .T. ) ;
#18461=ADVANCED_FACE ( 'NONE', ( #32963 ), #40087, .T. ) ;
#18472=CARTESIAN_POINT ( 'NONE',  ( -20.24909385650551386, -8.104110260919579645, 48.81699501597546487 ) ) ;
#18475=( BOUNDED_CURVE ( )  B_SPLINE_CURVE ( 2, ( #14923, #26277, #45255, #11498, #15663, #911, #27004, #38072, #38305 ),
 .UNSPECIFIED., .F., .F. ) 
 B_SPLINE_CURVE_WITH_KNOTS ( ( 3, 2, 2, 2, 3 ),
 ( 0.02753876536673079828, 0.02852216368270100999, 0.02950556199867122517, 0.03048896031464144035, 0.03147235863061165206 ),
 .UNSPECIFIED. ) 
 CURVE ( )  GEOMETRIC_REPRESENTATION_ITEM ( )  RATIONAL_B_SPLINE_CURVE ( ( 0.9999999999995842215, 0.9238795325117025170, 1.000000000000000000, 0.9238795325112867385, 1.000000000000000000, 0.9238795325112867385, 1.000000000000000000, 0.9238795325112867385, 1.000000000000000000 ) ) 
 REPRESENTATION_ITEM ( '' )  );
#18515=CARTESIAN_POINT ( 'NONE',  ( -13.52409385541304410, -9.359200813967568422, 50.49621490985803263 ) ) ;
#18543=LINE ( 'NONE', #14342, #13263 ) ;
#18546=CARTESIAN_POINT ( 'NONE',  ( -18.98034385650551670, -6.424090610841176385, 49.80797279389978627 ) ) ;
#18550=CARTESIAN_POINT ( 'NONE',  ( 10.57590614458695377, 2.137037847100790255, 51.75577699556767897 ) ) ;
#18552=DIRECTION ( 'NONE',  ( -0.9524241471993248886, 0.0009228828802118167144, -0.3047743298226213704 ) ) ;
#18561=CARTESIAN_POINT ( 'NONE',  ( -15.99909385650551741, -8.114302828567740988, 52.18300498402516041 ) ) ;
#18563=DIRECTION ( 'NONE',  ( 1.000000000000000000, -4.164305804376849172E-17, 1.614929280266638808E-16 ) ) ;
#18568=CARTESIAN_POINT ( 'NONE',  ( -15.58034385650551634, -6.424090610841176385, 49.80797279389977916 ) ) ;
#18570=DIRECTION ( 'NONE',  ( 0.000000000000000000, 0.007114381193220381018, -0.9999746924698831307 ) ) ;
#18571=CARTESIAN_POINT ( 'NONE',  ( -15.41159385650551705, -6.922745924619793101, 51.69366785382590024 ) ) ;
#18623=CARTESIAN_POINT ( 'NONE',  ( -12.99284385759799143, -8.630756214087126565, 51.74842643355248129 ) ) ;
#18635=CARTESIAN_POINT ( 'NONE',  ( -14.87409385650551741, -9.792211528768504536, 50.49490371617623197 ) ) ;
#18644=( BOUNDED_CURVE ( )  B_SPLINE_CURVE ( 2, ( #24494, #2716, #17723, #26595, #11824, #34206, #41359, #45809, #41616 ),
 .UNSPECIFIED., .F., .F. ) 
 B_SPLINE_CURVE_WITH_KNOTS ( ( 3, 2, 2, 2, 3 ),
 ( 0.07081306277049698172, 0.07179665212962056675, 0.07278024148874416566, 0.07376383084786776456, 0.07474742020699134959 ),
 .UNSPECIFIED. ) 
 CURVE ( )  GEOMETRIC_REPRESENTATION_ITEM ( )  RATIONAL_B_SPLINE_CURVE ( ( 0.9999999999999642508, 0.9238795325113224877, 1.000000000000000000, 0.9238795325112867385, 1.000000000000000000, 0.9238795325112867385, 1.000000000000000000, 0.9238795325101858413, 1.000000000001100897 ) ) 
 REPRESENTATION_ITEM ( '' )  );
#18677=CARTESIAN_POINT ( 'NONE',  ( -19.51784385759798468, -6.860780111191484565, 51.02154966934377711 ) ) ;
#18680=CARTESIAN_POINT ( 'NONE',  ( -16.03034385759799108, -6.857644439848013640, 49.98602051094139398 ) ) ;
#18708=DIRECTION ( 'NONE',  ( -0.9524241471993249997, -0.3047743298226212039, -0.0009228828802129951337 ) ) ;
#18720=CARTESIAN_POINT ( 'NONE',  ( -20.75534385650551528, -7.417179338643134834, 52.18511593390279302 ) ) ;
#18728=CARTESIAN_POINT ( 'NONE',  ( -22.52409385541004383, -9.359200813967481380, 50.49621490983041383 ) ) ;
#18731=CARTESIAN_POINT ( 'NONE',  ( -22.46784385541121054, -9.357632978284044611, 49.97845033064507447 ) ) ;
#18745=CARTESIAN_POINT ( 'NONE',  ( -12.72364920584387349, -9.064356868646193277, 49.69365772853683438 ) ) ;
#18747=AXIS2_PLACEMENT_3D ( 'NONE', #25034, #5839, #13679 ) ;
#18784=CARTESIAN_POINT ( 'NONE',  ( -19.06784385759798894, -9.357632978295834292, 49.97845033065683396 ) ) ;
#18803=LINE ( 'NONE', #8226, #37785 ) ;
#18804=CARTESIAN_POINT ( 'NONE',  ( -19.14909385650551954, -8.104110260919579645, 48.81699501597546487 ) ) ;
#18823=CARTESIAN_POINT ( 'NONE',  ( -15.71784385650551741, -9.790100578890868377, 49.79778022625163203 ) ) ;
#18832=CARTESIAN_POINT ( 'NONE',  ( -16.03034385650551386, -9.794322478646142471, 51.19202720610083901 ) ) ;
#18835=CARTESIAN_POINT ( 'NONE',  ( -15.63659385650551670, -6.915538690918075382, 49.31353937987644542 ) ) ;
#18878=EDGE_CURVE ( 'NONE', #16655, #3147, #33136, .T. ) ;
#18880=ORIENTED_EDGE ( 'NONE', *, *, #7236, .F. ) ;
#18886=CARTESIAN_POINT ( 'NONE',  ( -18.92409385541303024, -9.359200813967568422, 50.49621490985794026 ) ) ;
#18902=CARTESIAN_POINT ( 'NONE',  ( -16.73034385650551670, -9.794322478646142471, 51.19202720610083901 ) ) ;
#18910=LINE ( 'NONE', #33175, #31965 ) ;
#18915=DIRECTION ( 'NONE',  ( 0.000000000000000000, -1.000000000000000000, 0.000000000000000000 ) ) ;
#18940=CARTESIAN_POINT ( 'NONE',  ( -15.63659385759799036, -8.995762431863214559, 51.38120296130585274 ) ) ;
#18943=FACE_OUTER_BOUND ( 'NONE', #15402, .T. ) ;
#18981=CARTESIAN_POINT ( 'NONE',  ( -19.96784385650551386, -6.428312510596451368, 51.20221977374900035 ) ) ;
#18990=CARTESIAN_POINT ( 'NONE',  ( -22.29909385541301958, -8.105421454601382081, 49.25000573077637256 ) ) ;
#19002=CARTESIAN_POINT ( 'NONE',  ( -33.42409385541304800, -8.109206544743658540, 50.50000000000030553 ) ) ;
#19015=CARTESIAN_POINT ( 'NONE',  ( -21.51159385541298263, -8.990409506049271471, 49.61344411288067846 ) ) ;
#19019=CARTESIAN_POINT ( 'NONE',  ( -15.38034385541304161, -9.360768649639302552, 51.01397948905922419 ) ) ;
#19052=CARTESIAN_POINT ( 'NONE',  ( -20.33034385650552167, -9.794322478646142471, 51.19202720610083190 ) ) ;
#19065=CARTESIAN_POINT ( 'NONE',  ( -15.21159385650551776, -6.922745924619793101, 51.69366785382590024 ) ) ;
#19072=CARTESIAN_POINT ( 'NONE',  ( -14.68034385650551599, -6.424090610841176385, 49.80797279389977916 ) ) ;
#19078=CARTESIAN_POINT ( 'NONE',  ( -16.87409385650551386, -9.792211528768504536, 50.49490371617623197 ) ) ;
#19105=SHAPE_DEFINITION_REPRESENTATION ( #29509, #34550 ) ;
#19112=CARTESIAN_POINT ( 'NONE',  ( -14.42409385541304090, -9.359200813967568422, 50.49621490985801842 ) ) ;
#19133=ORIENTED_EDGE ( 'NONE', *, *, #24085, .F. ) ;
#19140=CARTESIAN_POINT ( 'NONE',  ( -16.95534385650551812, -7.417179338643134834, 52.18511593390279302 ) ) ;
#19165=CARTESIAN_POINT ( 'NONE',  ( 18.57132275349405148, 1.802465958033905302, 51.78855248148219204 ) ) ;
#19171=CARTESIAN_POINT ( 'NONE',  ( -21.62409385541304374, -9.359200813967568422, 50.49621490985803263 ) ) ;
#19184=CARTESIAN_POINT ( 'NONE',  ( -21.68034385650551599, -6.424090610841174609, 49.80797279389977916 ) ) ;
#19202=ORIENTED_EDGE ( 'NONE', *, *, #38766, .F. ) ;
#19208=EDGE_LOOP ( 'NONE', ( #23404, #10577, #46346, #31721 ) ) ;
#19224=CARTESIAN_POINT ( 'NONE',  ( -22.72409385650551528, -6.426201560718813433, 50.50509628382439331 ) ) ;
#19230=( BOUNDED_CURVE ( )  B_SPLINE_CURVE ( 3, ( #9515, #44634, #39776, #13167 ),
 .UNSPECIFIED., .F., .F. ) 
 B_SPLINE_CURVE_WITH_KNOTS ( ( 4, 4 ),
 ( 6.081827386389250911, 6.283185307179578238 ),
 .UNSPECIFIED. ) 
 CURVE ( )  GEOMETRIC_REPRESENTATION_ITEM ( )  RATIONAL_B_SPLINE_CURVE ( ( 1.000000000000000000, 0.9966241020034157794, 0.9966241020034157794, 1.000000000000000000 ) ) 
 REPRESENTATION_ITEM ( '' )  );
#19243=CARTESIAN_POINT ( 'NONE',  ( -21.20534385759799179, -7.595227055684746986, 51.75156210489594599 ) ) ;
#19260=CARTESIAN_POINT ( 'NONE',  ( -22.80534385650551599, -8.801233750844183135, 48.81488406609782515 ) ) ;
#19261=EDGE_LOOP ( 'NONE', ( #22150, #26122, #26183, #14190 ) ) ;
#19292=CARTESIAN_POINT ( 'NONE',  ( -20.55534385650551599, -7.417179338643134834, 52.18511593390279302 ) ) ;
#19301=ORIENTED_EDGE ( 'NONE', *, *, #24021, .T. ) ;
#19307=CARTESIAN_POINT ( 'NONE',  ( -16.22409385650551883, -6.426201560718813433, 50.50509628382439331 ) ) ;
#19309=DIRECTION ( 'NONE',  ( 1.000000000000000000, 1.669677910507523057E-21, 6.493791346278465266E-22 ) ) ;
#19314=CARTESIAN_POINT ( 'NONE',  ( -14.62409385650551386, -6.426201560718813433, 50.50509628382439331 ) ) ;
#19319=CARTESIAN_POINT ( 'NONE',  ( -16.64909385650551599, -8.104110260919579645, 48.81699501597546487 ) ) ;
#19327=ORIENTED_EDGE ( 'NONE', *, *, #3435, .T. ) ;
#19332=VERTEX_POINT ( 'NONE', #27428 ) ;
#19346=CARTESIAN_POINT ( 'NONE',  ( -14.31159385541286433, -8.990409506049420685, 49.61344411288053635 ) ) ;
#19349=CARTESIAN_POINT ( 'NONE',  ( -14.64909385541304765, -8.112991634885936776, 51.74999426922421009 ) ) ;
#19363=CARTESIAN_POINT ( 'NONE',  ( -16.25534385759799250, -8.623186033802570094, 49.24843789510467218 ) ) ;
#19366=EDGE_CURVE ( 'NONE', #3652, #17695, #12904, .T. ) ;
#19375=ADVANCED_FACE ( 'NONE', ( #20043 ), #12169, .T. ) ;
#19380=CARTESIAN_POINT ( 'NONE',  ( -16.33659385650551599, -6.915538690918074494, 49.31353937987644542 ) ) ;
#19400=EDGE_LOOP ( 'NONE', ( #2248, #15710, #6857, #32991 ) ) ;
#19414=VECTOR ( 'NONE', #24500, 1000.000000000000000 ) ;
#19416=ORIENTED_EDGE ( 'NONE', *, *, #20252, .F. ) ;
#19422=CARTESIAN_POINT ( 'NONE',  ( -20.61159385650551812, -6.922745924619793101, 51.69366785382590024 ) ) ;
#19445=VECTOR ( 'NONE', #12458, 1000.000000000000227 ) ;
#19449=ORIENTED_EDGE ( 'NONE', *, *, #7236, .T. ) ;
#19461=CARTESIAN_POINT ( 'NONE',  ( -17.21159385650551599, -6.922745924619793101, 51.69366785382590024 ) ) ;
#19466=CARTESIAN_POINT ( 'NONE',  ( -16.56159385541304019, -7.228003583438115776, 51.38655588711986155 ) ) ;
#19470=ORIENTED_EDGE ( 'NONE', *, *, #11172, .T. ) ;
#19478=CARTESIAN_POINT ( 'NONE',  ( -22.10534385759799036, -7.595227055684746986, 51.75156210489594599 ) ) ;
#19528=CARTESIAN_POINT ( 'NONE',  ( -17.66159385759798894, -7.228003583438117552, 51.38655588711986155 ) ) ;
#19534=CARTESIAN_POINT ( 'NONE',  ( -20.78034385650551386, -6.424090610841176385, 49.80797279389978627 ) ) ;
#19552=DIRECTION ( 'NONE',  ( 1.000000000000000000, -4.164305804376849172E-17, 1.614929280266638808E-16 ) ) ;
#19561=CARTESIAN_POINT ( 'NONE',  ( -22.13034385541304161, -6.857644439848013640, 49.98602051094139398 ) ) ;
#19568=ADVANCED_FACE ( 'NONE', ( #33513 ), #23633, .T. ) ;
#19582=ORIENTED_EDGE ( 'NONE', *, *, #46518, .F. ) ;
#19589=DIRECTION ( 'NONE',  ( 1.000000000000000000, -4.164305804376849172E-17, 1.614929280266638808E-16 ) ) ;
#19597=EDGE_LOOP ( 'NONE', ( #6724, #20046, #1957, #29863 ) ) ;
#19620=FACE_OUTER_BOUND ( 'NONE', #35633, .T. ) ;
#19627=CARTESIAN_POINT ( 'NONE',  ( -15.77409385650551954, -9.792211528768504536, 50.49490371617623197 ) ) ;
#19662=AXIS2_PLACEMENT_3D ( 'NONE', #13500, #2434, #24847 ) ;
#19671=DIRECTION ( 'NONE',  ( 0.000000000000000000, 0.9999954153791273948, 0.003028072113820366902 ) ) ;
#19677=VECTOR ( 'NONE', #36966, 1000.000000000000114 ) ;
#19678=CARTESIAN_POINT ( 'NONE',  ( -22.86159385650551457, -9.295667164867525756, 49.30633214617472504 ) ) ;
#19715=EDGE_CURVE ( 'NONE', #16810, #1692, #44711, .T. ) ;
#19718=CARTESIAN_POINT ( 'NONE',  ( -16.53659385650551528, -6.915538690918075382, 49.31353937987644542 ) ) ;
#19724=CARTESIAN_POINT ( 'NONE',  ( -16.28034385541300111, -9.360768649639558348, 51.01397948905896840 ) ) ;
#19741=CIRCLE ( 'NONE', #44913, 1.249999999999999334 ) ;
#19746=EDGE_CURVE ( 'NONE', #30416, #28807, #5395, .T. ) ;
#19755=FACE_OUTER_BOUND ( 'NONE', #48494, .T. ) ;
#19762=( BOUNDED_CURVE ( )  B_SPLINE_CURVE ( 2, ( #41889, #4451, #19466, #34479, #767, #15762, #30817, #19724, #31048 ),
 .UNSPECIFIED., .F., .F. ) 
 B_SPLINE_CURVE_WITH_KNOTS ( ( 3, 2, 2, 2, 3 ),
 ( 0.05901120358171226682, 0.05999458517735227481, 0.06097796677299228973, 0.06196134836863229772, 0.06294472996427230571 ),
 .UNSPECIFIED. ) 
 CURVE ( )  GEOMETRIC_REPRESENTATION_ITEM ( )  RATIONAL_B_SPLINE_CURVE ( ( 0.9999999999998986366, 0.9238795325113881018, 1.000000000000000000, 0.9238795325112867385, 1.000000000000000000, 0.9238795325112867385, 1.000000000000000000, 0.9238795325112381107, 1.000000000000048628 ) ) 
 REPRESENTATION_ITEM ( '' )  );
#19791=CARTESIAN_POINT ( 'NONE',  ( -15.21159385650551776, -6.922745924619793101, 51.69366785382590024 ) ) ;
#19807=EDGE_CURVE ( 'NONE', #43020, #45257, #26044, .T. ) ;
#19818=CARTESIAN_POINT ( 'NONE',  ( -20.89284385541304445, -8.630756214087126565, 51.74842643355248129 ) ) ;
#19837=TOROIDAL_SURFACE ( 'NONE', #30853, 1.750000000000000000, 0.2500000000000000000 ) ;
#19873=CARTESIAN_POINT ( 'NONE',  ( -21.48659385650551457, -9.302874398569244363, 51.68646062012417985 ) ) ;
#19878=CARTESIAN_POINT ( 'NONE',  ( -13.07409385650551847, -9.792211528768506312, 50.49490371617623197 ) ) ;
#19879=VERTEX_POINT ( 'NONE', #44285 ) ;
#19918=CARTESIAN_POINT ( 'NONE',  ( -22.91784385650551670, -9.790100578890868377, 49.79778022625162492 ) ) ;
#19931=EDGE_CURVE ( 'NONE', #11159, #6741, #21283, .T. ) ;
#19956=CARTESIAN_POINT ( 'NONE',  ( -16.81784385650551528, -9.790100578890868377, 49.79778022625163203 ) ) ;
#19959=ORIENTED_EDGE ( 'NONE', *, *, #12679, .T. ) ;
#19975=CARTESIAN_POINT ( 'NONE',  ( -22.16159385759798894, -7.228003583438117552, 51.38655588711986155 ) ) ;
#19990=CARTESIAN_POINT ( 'NONE',  ( -22.58034385650552167, -6.424090610841174609, 49.80797279389977916 ) ) ;
#20024=CARTESIAN_POINT ( 'NONE',  ( -17.06784385650551528, -6.428312510596451368, 51.20221977374900035 ) ) ;
#20025=VERTEX_POINT ( 'NONE', #24297 ) ;
#20043=FACE_OUTER_BOUND ( 'NONE', #29659, .T. ) ;
#20046=ORIENTED_EDGE ( 'NONE', *, *, #9770, .T. ) ;
#20047=CARTESIAN_POINT ( 'NONE',  ( -21.28659385541304161, -7.222650657624104298, 49.61879703869476543 ) ) ;
#20062=DIRECTION ( 'NONE',  ( -1.000000000000000000, 0.000000000000000000, 0.000000000000000000 ) ) ;
#20074=DIRECTION ( 'NONE',  ( 0.000000000000000000, -0.9999954153791273948, -0.003028072113819838245 ) ) ;
#20080=CARTESIAN_POINT ( 'NONE',  ( 18.46573386768564973, 0.6667653706753842169, 50.27657325150214973 ) ) ;
#20081=ORIENTED_EDGE ( 'NONE', *, *, #5847, .T. ) ;
#20092=ORIENTED_EDGE ( 'NONE', *, *, #38850, .T. ) ;
#20095=CARTESIAN_POINT ( 'NONE',  ( -16.31159385759798752, -8.990409506049202193, 49.61344411288074951 ) ) ;
#20102=CARTESIAN_POINT ( 'NONE',  ( -22.49909385650551741, -8.114302828567740988, 52.18300498402516041 ) ) ;
#20108=CARTESIAN_POINT ( 'NONE',  ( -21.48659385650551457, -9.302874398569244363, 51.68646062012417985 ) ) ;
#20110=ADVANCED_FACE ( 'NONE', ( #30877 ), #826, .F. ) ;
#20116=EDGE_CURVE ( 'NONE', #32298, #43417, #18803, .T. ) ;
#20118=CARTESIAN_POINT ( 'NONE',  ( -20.94909385541298974, -8.112991634885936776, 51.74999426922432377 ) ) ;
#20131=CYLINDRICAL_SURFACE ( 'NONE', #2981, 1.249999999999998668 ) ;
#20151=CARTESIAN_POINT ( 'NONE',  ( -18.53034385650551386, -9.794322478646142471, 51.19202720610083901 ) ) ;
#20174=EDGE_CURVE ( 'NONE', #15076, #29468, #10752, .T. ) ;
#20188=CARTESIAN_POINT ( 'NONE',  ( -16.05534385541290376, -8.623186033802667794, 49.24843789510443059 ) ) ;
#20189=CARTESIAN_POINT ( 'NONE',  ( -17.60534385650551670, -8.801233750844183135, 48.81488406609782515 ) ) ;
#20195=ORIENTED_EDGE ( 'NONE', *, *, #38766, .T. ) ;
#20199=DIRECTION ( 'NONE',  ( 0.000000000000000000, -0.007114381193220334181, 0.9999746924698833528 ) ) ;
#20208=CARTESIAN_POINT ( 'NONE',  ( -21.59909385759798894, -8.105421454601382081, 49.25000573077640098 ) ) ;
#20215=CARTESIAN_POINT ( 'NONE',  ( 18.54465614458695910, 0.6404988570616596544, 50.61053642849761758 ) ) ;
#20233=DIRECTION ( 'NONE',  ( 0.000000000000000000, -0.9999954153791273948, -0.003028072113819838245 ) ) ;
#20252=EDGE_CURVE ( 'NONE', #3652, #16353, #20748, .T. ) ;
#20268=CARTESIAN_POINT ( 'NONE',  ( -17.63034385650551528, -9.794322478646142471, 51.19202720610083190 ) ) ;
#20292=CARTESIAN_POINT ( 'NONE',  ( -19.99284385541304232, -8.630756214087126565, 51.74842643355248129 ) ) ;
#20335=VERTEX_POINT ( 'NONE', #39853 ) ;
#20350=CARTESIAN_POINT ( 'NONE',  ( -20.47409385650551528, -9.792211528768504536, 50.49490371617623197 ) ) ;
#20353=CARTESIAN_POINT ( 'NONE',  ( -18.02409385541303877, -9.359200813967568422, 50.49621490985803263 ) ) ;
#20355=CARTESIAN_POINT ( 'NONE',  ( -22.83659385650551954, -6.915538690918074494, 49.31353937987644542 ) ) ;
#20362=CARTESIAN_POINT ( 'NONE',  ( -36.42409385541304800, -9.359200813967566646, 50.49621490985803263 ) ) ;
#20364=CARTESIAN_POINT ( 'NONE',  ( -21.17409385541299116, -6.859212275519752211, 50.50378509014304029 ) ) ;
#20392=EDGE_LOOP ( 'NONE', ( #37754, #36752, #31764, #45563 ) ) ;
#20405=CARTESIAN_POINT ( 'NONE',  ( -19.20534385650551457, -8.801233750844183135, 48.81488406609782515 ) ) ;
#20434=CARTESIAN_POINT ( 'NONE',  ( -22.49909385759799108, -8.105421454601382081, 49.25000573077640098 ) ) ;
#20446=CARTESIAN_POINT ( 'NONE',  ( -17.71784385650551741, -9.790100578890868377, 49.79778022625163203 ) ) ;
#20450=EDGE_LOOP ( 'NONE', ( #10509, #6604, #1032, #19582 ) ) ;
#20466=CARTESIAN_POINT ( 'NONE',  ( -18.39284385759798823, -8.630756214087126565, 51.74842643355248129 ) ) ;
#20511=DIRECTION ( 'NONE',  ( 1.000000000000000000, -4.164305804376849172E-17, 1.614929280266638808E-16 ) ) ;
#20516=CARTESIAN_POINT ( 'NONE',  ( -14.93034385650551599, -9.794322478646142471, 51.19202720610083190 ) ) ;
#20540=CARTESIAN_POINT ( 'NONE',  ( -16.76159385759799036, -7.228003583438117552, 51.38655588711986155 ) ) ;
#20545=CARTESIAN_POINT ( 'NONE',  ( -21.79284385541304658, -8.630756214087126565, 51.74842643355248129 ) ) ;
#20552=( BOUNDED_CURVE ( )  B_SPLINE_CURVE ( 2, ( #26684, #46120, #19528, #34536, #12624, #27401, #820, #30632, #45658 ),
 .UNSPECIFIED., .F., .F. ) 
 B_SPLINE_CURVE_WITH_KNOTS ( ( 3, 2, 2, 2, 3 ),
 ( 0.4583333333333333148, 0.4687500000000000555, 0.4791666666666667962, 0.4895833333333334814, 0.5000000000000002220 ),
 .UNSPECIFIED. ) 
 CURVE ( )  GEOMETRIC_REPRESENTATION_ITEM ( )  RATIONAL_B_SPLINE_CURVE ( ( 1.000000000000000000, 0.9238795325112867385, 1.000000000000000000, 0.9238795325112867385, 1.000000000000000000, 0.9238795325112867385, 1.000000000000000000, 0.9238795325112850731, 1.000000000000001554 ) ) 
 REPRESENTATION_ITEM ( '' )  );
#20557=VERTEX_POINT ( 'NONE', #20362 ) ;
#20570=CARTESIAN_POINT ( 'NONE',  ( -19.85534385759799392, -8.623186033802570094, 49.24843789510466507 ) ) ;
#20598=CARTESIAN_POINT ( 'NONE',  ( -21.99284385650551243, -7.406986770994973490, 48.81910596585309747 ) ) ;
#20599=VECTOR ( 'NONE', #33482, 1000.000000000000114 ) ;
#20603=CARTESIAN_POINT ( 'NONE',  ( -22.38659385650551670, -9.302874398569244363, 51.68646062012417985 ) ) ;
#20626=DIRECTION ( 'NONE',  ( 1.000000000000000000, -4.164305804376849172E-17, 1.614929280266638808E-16 ) ) ;
#20647=CARTESIAN_POINT ( 'NONE',  ( -18.86784385650551954, -6.428312510596451368, 51.20221977374900035 ) ) ;
#20704=CARTESIAN_POINT ( 'NONE',  ( -19.12409385759799108, -9.359200813967568422, 50.49621490985803263 ) ) ;
#20709=CARTESIAN_POINT ( 'NONE',  ( 23.52590614458706852, 1.890747609047893185, 50.53028072113869484 ) ) ;
#20748=LINE ( 'NONE', #13576, #39374 ) ;
#20749=CARTESIAN_POINT ( 'NONE',  ( -15.04284385650551670, -8.811426318492348031, 52.18089403414752070 ) ) ;
#20753=CARTESIAN_POINT ( 'NONE',  ( -15.07409385759798859, -6.859212275519751323, 50.50378509014259265 ) ) ;
#20758=CARTESIAN_POINT ( 'NONE',  ( -18.75534385541303806, -8.623186033802571870, 49.24843789510465797 ) ) ;
#20777=CARTESIAN_POINT ( 'NONE',  ( -18.08034385541304445, -9.360768649639302552, 51.01397948905922419 ) ) ;
#20783=ADVANCED_FACE ( 'NONE', ( #37790 ), #14376, .T. ) ;
#20790=VECTOR ( 'NONE', #43428, 1000.000000000000000 ) ;
#20798=CARTESIAN_POINT ( 'NONE',  ( -20.02409385759798965, -9.359200813967568422, 50.49621490985803263 ) ) ;
#20833=CARTESIAN_POINT ( 'NONE',  ( -17.38034385650551528, -6.424090610841176385, 49.80797279389977916 ) ) ;
#20837=CARTESIAN_POINT ( 'NONE',  ( -21.03659385650551528, -6.915538690918074494, 49.31353937987644542 ) ) ;
#20848=EDGE_CURVE ( 'NONE', #9159, #501, #19741, .T. ) ;
#20866=ORIENTED_EDGE ( 'NONE', *, *, #12541, .F. ) ;
#20883=CARTESIAN_POINT ( 'NONE',  ( -17.40534385650551741, -8.801233750844183135, 48.81488406609782515 ) ) ;
#20884=CARTESIAN_POINT ( 'NONE',  ( 18.57590614458706924, 0.6299963676414210845, 50.77646420411990391 ) ) ;
#20896=CARTESIAN_POINT ( 'NONE',  ( 8.575906144586953772, -0.1092432217106413528, 50.52422457691089619 ) ) ;
#20918=CARTESIAN_POINT ( 'NONE',  ( -14.73659385759798823, -8.995762431863214559, 51.38120296130585274 ) ) ;
#20921=CARTESIAN_POINT ( 'NONE',  ( -13.61159385650551457, -6.922745924619793101, 51.69366785382590024 ) ) ;
#20942=CARTESIAN_POINT ( 'NONE',  ( -17.49284385759798965, -8.630756214087126565, 51.74842643355248129 ) ) ;
#20943=LINE ( 'NONE', #35943, #33654 ) ;
#20955=VERTEX_POINT ( 'NONE', #24734 ) ;
#20962=DIRECTION ( 'NONE',  ( 0.000000000000000000, -0.007114381193220324640, 0.9999746924698832418 ) ) ;
#20968=ORIENTED_EDGE ( 'NONE', *, *, #44949, .F. ) ;
#20975=CARTESIAN_POINT ( 'NONE',  ( 22.62590614458706639, 1.890747609047893185, 50.53028072113869484 ) ) ;
#20990=CARTESIAN_POINT ( 'NONE',  ( -13.74909385650551563, -8.104110260919579645, 48.81699501597546487 ) ) ;
#21009=CARTESIAN_POINT ( 'NONE',  ( 23.52590614458706852, 1.904976371434334181, 48.53033133619892681 ) ) ;
#21020=CARTESIAN_POINT ( 'NONE',  ( -16.61784385541304587, -6.860780111191487229, 51.02154966934377711 ) ) ;
#21042=DIRECTION ( 'NONE',  ( 1.000000000000000000, -4.164305804376849788E-17, 1.614929280266638808E-16 ) ) ;
#21049=CARTESIAN_POINT ( 'NONE',  ( -22.97409385650551528, -9.792211528768504536, 50.49490371617623197 ) ) ;
#21075=CARTESIAN_POINT ( 'NONE',  ( -19.12409385650551741, -6.426201560718813433, 50.50509628382439331 ) ) ;
#21078=AXIS2_PLACEMENT_3D ( 'NONE', #33614, #47935, #22076 ) ;
#21081=CARTESIAN_POINT ( 'NONE',  ( -17.49284385650551599, -7.406986770994973490, 48.81910596585309747 ) ) ;
#21102=( BOUNDED_CURVE ( )  B_SPLINE_CURVE ( 2, ( #21049, #21302, #47638, #25704, #6996, #10219, #24988, #22017, #13873, #17813, #36297, #3045, #29162, #6758, #48115, #40006, #14346, #44438, #3299, #33307, #2579, #17581, #28917, #25232, #7994, #34057, #38229, #582, #22501, #48596, #22259, #23242, #4514, #26440, #26201, #45663, #40973, #23012, #37250, #19534, #11916, #41708, #15576, #19292, #110, #14833, #29901, #19052, #10935, #15095, #33553, #34542, #4282, #30393, #30151, #37996, #34296, #30638, #26934, #7256, #3794, #3537, #33814, #827, #4050, #45176, #45407, #15828, #18804, #7500, #44932, #18546, #22761, #41952, #8227, #11185, #11415, #41212, #41452, #7748, #11663, #30878, #37499, #37753, #25955, #349, #26689, #15334, #27652, #35748, #39218, #16555, #5014, #35520, #12631, #20268, #1295, #1795, #31594, #8952, #5248, #8455, #12384, #42191, #27407, #20024, #31832, #28136, #31343, #2031, #46854, #35027, #42685, #42441, #42918, #23969, #13095, #4766, #43161, #17027, #35272, #12151, #24460, #16795, #16304, #23485, #23736, #46622, #39463, #12865, #5501, #9436, #38972, #46374, #27170, #1545, #27893, #9190, #19791, #5747, #24208, #20749, #45892, #20516, #38481, #38730, #46125, #34794, #1065, #16063, #31106, #8711, #36470, #48054, #32551, #10632, #21482, #6935, #17280, #5968, #43416, #13337, #24926, #17996, #20990, #39943, #43899, #36949, #36237, #13814, #28855, #47579, #9681, #25411, #21710, #28622, #6215, #44377, #2519 ),
 .UNSPECIFIED., .F., .F. ) 
 B_SPLINE_CURVE_WITH_KNOTS ( ( 3, 2, 2, 2, 2, 2, 2, 2, 2, 2, 2, 2, 2, 2, 2, 2, 2, 2, 2, 2, 2, 2, 2, 2, 2, 2, 2, 2, 2, 2, 2, 2, 2, 2, 2, 2, 2, 2, 2, 2, 2, 2, 2, 2, 2, 2, 2, 2, 2, 2, 2, 2, 2, 2, 2, 2, 2, 2, 2, 2, 2, 2, 2, 2, 2, 2, 2, 2, 2, 2, 2, 2, 2, 2, 2, 2, 2, 2, 2, 2, 2, 2, 2, 2, 2, 2, 2, 2, 2, 3 ),
 ( 0.000000000000000000, 0.01125025777839750753, 0.02250051555679501505, 0.03375077333519252432, 0.04500103111359003011, 0.05625128889198754284, 0.06750154667038504863, 0.07875180444878256136, 0.09000206222718006022, 0.1012523200055775729, 0.1125025777839750857, 0.1237528355623725845, 0.1350030933407700973, 0.1462533511191675961, 0.1575036088975651227, 0.1687538666759626216, 0.1800041244543601204, 0.1912543822327576470, 0.2025046400111551459, 0.2137548977895526447, 0.2250051555679501714, 0.2362554133463476702, 0.2475056711247451691, 0.2587559289031426957, 0.2700061866815401945, 0.2812564444599377489, 0.2925067022383351922, 0.3037569600167327466, 0.3150072177951302455, 0.3262574755735277443, 0.3375077333519252432, 0.3487579911303227975, 0.3600082489087202409, 0.3712585066871177952, 0.3825087644655152941, 0.3937590222439127929, 0.4050092800223102918, 0.4162595378007078462, 0.4275097955791052895, 0.4387600533575028439, 0.4500103111359003427, 0.4612605689142978416, 0.4725108266926953404, 0.4837610844710928948, 0.4950113422494903381, 0.5062616000278878925, 0.5175118578062853913, 0.5287621155846828902, 0.5400123733630803891, 0.5512626311414778879, 0.5625128889198754978, 0.5737631466982728856, 0.5850134044766703845, 0.5962636622550679943, 0.6075139200334654932, 0.6187641778118628810, 0.6300144355902604909, 0.6412646933686579898, 0.6525149511470554886, 0.6637652089254529875, 0.6750154667038504863, 0.6862657244822479852, 0.6975159822606455950, 0.7087662400390429829, 0.7200164978174404817, 0.7312667555958380916, 0.7425170133742355905, 0.7537672711526329783, 0.7650175289310305882, 0.7762677867094280870, 0.7875180444878255859, 0.7987683022662230847, 0.8100185600446205836, 0.8212688178230180824, 0.8325190756014156923, 0.8437693333798130801, 0.8550195911582105790, 0.8662698489366081889, 0.8775201067150056877, 0.8887703644934030756, 0.9000206222718006854, 0.9112708800501981843, 0.9225211378285956831, 0.9337713956069931820, 0.9450216533853906808, 0.9562719111637881797, 0.9675221689421857896, 0.9787724267205831774, 0.9900226844989806763, 1.000000000000000000 ),
 .UNSPECIFIED. ) 
 CURVE ( )  GEOMETRIC_REPRESENTATION_ITEM ( )  RATIONAL_B_SPLINE_CURVE ( ( 1.000000000000000000, 0.9238795325112867385, 1.000000000000000000, 0.9238795325112867385, 1.000000000000000000, 0.9238795325112867385, 1.000000000000000000, 0.9238795325112867385, 1.000000000000000000, 0.9238795325112867385, 1.000000000000000000, 0.9238795325112867385, 1.000000000000000000, 0.9238795325112867385, 1.000000000000000000, 0.9238795325112867385, 1.000000000000000000, 0.9238795325112867385, 1.000000000000000000, 0.9238795325112867385, 1.000000000000000000, 0.9238795325112867385, 1.000000000000000000, 0.9238795325112867385, 1.000000000000000000, 0.9238795325112867385, 1.000000000000000000, 0.9238795325112867385, 1.000000000000000000, 0.9238795325112867385, 1.000000000000000000, 0.9238795325112867385, 1.000000000000000000, 0.9238795325112867385, 1.000000000000000000, 0.9238795325112867385, 1.000000000000000000, 0.9238795325112867385, 1.000000000000000000, 0.9238795325112867385, 1.000000000000000000, 0.9238795325112867385, 1.000000000000000000, 0.9238795325112867385, 1.000000000000000000, 0.9238795325112867385, 1.000000000000000000, 0.9238795325112867385, 1.000000000000000000, 0.9238795325112867385, 1.000000000000000000, 0.9238795325112867385, 1.000000000000000000, 0.9238795325112867385, 1.000000000000000000, 0.9238795325112867385, 1.000000000000000000, 0.9238795325112867385, 1.000000000000000000, 0.9238795325112867385, 1.000000000000000000, 0.9238795325112867385, 1.000000000000000000, 0.9238795325112867385, 1.000000000000000000, 0.9238795325112867385, 1.000000000000000000, 0.9238795325112867385, 1.000000000000000000, 0.9238795325112867385, 1.000000000000000000, 0.9238795325112867385, 1.000000000000000000, 0.9238795325112867385, 1.000000000000000000, 0.9238795325112867385, 1.000000000000000000, 0.9238795325112867385, 1.000000000000000000, 0.9238795325112867385, 1.000000000000000000, 0.9238795325112867385, 1.000000000000000000, 0.9238795325112867385, 1.000000000000000000, 0.9238795325112867385, 1.000000000000000000, 0.9238795325112867385, 1.000000000000000000, 0.9238795325112867385, 1.000000000000000000, 0.9238795325112867385, 1.000000000000000000, 0.9238795325112867385, 1.000000000000000000, 0.9238795325112867385, 1.000000000000000000, 0.9238795325112867385, 1.000000000000000000, 0.9238795325112867385, 1.000000000000000000, 0.9238795325112867385, 1.000000000000000000, 0.9238795325112867385, 1.000000000000000000, 0.9238795325112867385, 1.000000000000000000, 0.9238795325112867385, 1.000000000000000000, 0.9238795325112867385, 1.000000000000000000, 0.9238795325112867385, 1.000000000000000000, 0.9238795325112867385, 1.000000000000000000, 0.9238795325112867385, 1.000000000000000000, 0.9238795325112867385, 1.000000000000000000, 0.9238795325112867385, 1.000000000000000000, 0.9238795325112867385, 1.000000000000000000, 0.9238795325112867385, 1.000000000000000000, 0.9238795325112867385, 1.000000000000000000, 0.9238795325112867385, 1.000000000000000000, 0.9238795325112867385, 1.000000000000000000, 0.9238795325112867385, 1.000000000000000000, 0.9238795325112867385, 1.000000000000000000, 0.9238795325112867385, 1.000000000000000000, 0.9238795325112867385, 1.000000000000000000, 0.9238795325112867385, 1.000000000000000000, 0.9238795325112867385, 1.000000000000000000, 0.9238795325112867385, 1.000000000000000000, 0.9238795325112867385, 1.000000000000000000, 0.9238795325112867385, 1.000000000000000000, 0.9238795325112867385, 1.000000000000000000, 0.9238795325112867385, 1.000000000000000000, 0.9238795325112867385, 1.000000000000000000, 0.9238795325112867385, 1.000000000000000000, 0.9238795325112867385, 1.000000000000000000, 0.9238795325112867385, 1.000000000000000000, 0.9238795325112867385, 1.000000000000000000, 0.9238795325112867385, 1.000000000000000000, 0.9238795325112867385, 1.000000000000000000, 0.9238795325112867385, 1.000000000000000000, 0.9238795325112867385, 1.000000000000000000, 0.9238795325112867385, 1.000000000000000000, 0.9238795325112867385, 1.000000000000000000, 0.9238795325112867385, 1.000000000000000000, 0.9324923983805685213, 0.9847233224627454096 ) ) 
 REPRESENTATION_ITEM ( '' )  );
#21127=CARTESIAN_POINT ( 'NONE',  ( -19.82409385650551670, -6.426201560718813433, 50.50509628382439331 ) ) ;
#21143=CARTESIAN_POINT ( 'NONE',  ( -19.99284385650551243, -7.406986770994973490, 48.81910596585309747 ) ) ;
#21148=DIRECTION ( 'NONE',  ( 0.3047757271037813687, 0.002884009000661817267, -0.9524197806957001022 ) ) ;
#21188=CARTESIAN_POINT ( 'NONE',  ( -18.28034385759799108, -9.360768649639302552, 51.01397948905922419 ) ) ;
#21190=DIRECTION ( 'NONE',  ( -1.000000000000000000, -1.669677910507523057E-21, -6.493791346278465266E-22 ) ) ;
#21218=CARTESIAN_POINT ( 'NONE',  ( 6.575906144586949331, -9.359200813967568422, 50.49621490985803263 ) ) ;
#21223=EDGE_LOOP ( 'NONE', ( #24914, #9785, #7860, #40489, #44803 ) ) ;
#21269=CARTESIAN_POINT ( 'NONE',  ( -17.51784385541304090, -6.860780111191487229, 51.02154966934377001 ) ) ;
#21272=DIRECTION ( 'NONE',  ( -1.000000000000000000, -1.669677910507523057E-21, -6.493791346278465266E-22 ) ) ;
#21274=EDGE_CURVE ( 'NONE', #10355, #35561, #32529, .T. ) ;
#21283=CIRCLE ( 'NONE', #31502, 1.249999999999999334 ) ;
#21284=CARTESIAN_POINT ( 'NONE',  ( -20.72409385541304161, -9.359200813967568422, 50.49621490985803263 ) ) ;
#21291=EDGE_CURVE ( 'NONE', #29446, #32298, #32759, .T. ) ;
#21302=CARTESIAN_POINT ( 'NONE',  ( -22.91784385650551670, -9.790100578890868377, 49.79778022625162492 ) ) ;
#21318=VERTEX_POINT ( 'NONE', #7169 ) ;
#21327=CARTESIAN_POINT ( 'NONE',  ( -17.49284385650551599, -7.406986770994973490, 48.81910596585309747 ) ) ;
#21331=CARTESIAN_POINT ( 'NONE',  ( -19.18034385650551599, -6.424090610841176385, 49.80797279389977916 ) ) ;
#21366=EDGE_CURVE ( 'NONE', #24678, #39727, #29075, .T. ) ;
#21374=ORIENTED_EDGE ( 'NONE', *, *, #43145, .F. ) ;
#21394=CARTESIAN_POINT ( 'NONE',  ( -18.98034385650551670, -6.424090610841176385, 49.80797279389977916 ) ) ;
#21413=CARTESIAN_POINT ( 'NONE',  ( -14.68034385759798965, -9.360768649639304329, 51.01397948905922419 ) ) ;
#21417=CARTESIAN_POINT ( 'NONE',  ( -14.56784385650551705, -6.428312510596451368, 51.20221977374900035 ) ) ;
#21436=CARTESIAN_POINT ( 'NONE',  ( -19.74284385759798965, -7.587656875400192291, 49.25157356644813689 ) ) ;
#21451=DIRECTION ( 'NONE',  ( 1.000000000000000000, -4.164305804376849172E-17, 1.614929280266638808E-16 ) ) ;
#21459=EDGE_LOOP ( 'NONE', ( #42986, #44122, #29689, #2520 ) ) ;
#21474=CARTESIAN_POINT ( 'NONE',  ( -14.11784385759799143, -6.860780111191492558, 51.02154966934379132 ) ) ;
#21482=CARTESIAN_POINT ( 'NONE',  ( -14.19909385650551847, -8.114302828567740988, 52.18300498402516041 ) ) ;
#21484=ORIENTED_EDGE ( 'NONE', *, *, #32280, .F. ) ;
#21488=CARTESIAN_POINT ( 'NONE',  ( -36.42409385541304800, -8.109206544743658540, 50.50000000000030553 ) ) ;
#21490=CARTESIAN_POINT ( 'NONE',  ( -13.61159385650551457, -6.922745924619793101, 51.69366785382590024 ) ) ;
#21501=EDGE_CURVE ( 'NONE', #24601, #16655, #35903, .T. ) ;
#21504=CARTESIAN_POINT ( 'NONE',  ( 18.57590614458706924, 1.890747609047893185, 50.53028072113869484 ) ) ;
#21512=CARTESIAN_POINT ( 'NONE',  ( -16.95534385541304445, -8.623186033802570094, 49.24843789510466507 ) ) ;
#21527=CARTESIAN_POINT ( 'NONE',  ( -20.49909385541303308, -8.105421454601382081, 49.25000573077638677 ) ) ;
#21528=ORIENTED_EDGE ( 'NONE', *, *, #9830, .T. ) ;
#21532=ORIENTED_EDGE ( 'NONE', *, *, #8453, .F. ) ;
#21535=( BOUNDED_CURVE ( )  B_SPLINE_CURVE ( 2, ( #20364, #43007, #1156, #9284, #20118, #42291, #1391, #16408, #38584 ),
 .UNSPECIFIED., .F., .F. ) 
 B_SPLINE_CURVE_WITH_KNOTS ( ( 3, 2, 2, 2, 3 ),
 ( 0.01966989284433012450, 0.02065350756516602312, 0.02163712228600192522, 0.02262073700683782732, 0.02360435172767372594 ),
 .UNSPECIFIED. ) 
 CURVE ( )  GEOMETRIC_REPRESENTATION_ITEM ( )  RATIONAL_B_SPLINE_CURVE ( ( 0.9999999999999663602, 0.9238795325113203782, 1.000000000000000000, 0.9238795325112867385, 1.000000000000000000, 0.9238795325112867385, 1.000000000000000000, 0.9238795325112295620, 1.000000000000057288 ) ) 
 REPRESENTATION_ITEM ( '' )  );
#21550=CARTESIAN_POINT ( 'NONE',  ( 18.82590614458706924, 1.890747609047893185, 50.53028072113869484 ) ) ;
#21565=CARTESIAN_POINT ( 'NONE',  ( -18.61784385650552309, -9.790100578890868377, 49.79778022625163203 ) ) ;
#21569=CARTESIAN_POINT ( 'NONE',  ( -18.44909385650551670, -8.104110260919579645, 48.81699501597546487 ) ) ;
#21598=ORIENTED_EDGE ( 'NONE', *, *, #865, .T. ) ;
#21621=DIRECTION ( 'NONE',  ( 0.000000000000000000, 0.9999954153791273948, 0.003028072113820366902 ) ) ;
#21626=CARTESIAN_POINT ( 'NONE',  ( -18.08034385650551812, -6.424090610841176385, 49.80797279389977916 ) ) ;
#21638=ORIENTED_EDGE ( 'NONE', *, *, #13411, .F. ) ;
#21655=VERTEX_POINT ( 'NONE', #10975 ) ;
#21661=CARTESIAN_POINT ( 'NONE',  ( -14.73659385759798823, -8.995762431863214559, 51.38120296130585274 ) ) ;
#21693=AXIS2_PLACEMENT_3D ( 'NONE', #25926, #22231, #4013 ) ;
#21702=CARTESIAN_POINT ( 'NONE',  ( -13.83659385759798965, -8.995762431863214559, 51.38120296130585274 ) ) ;
#21710=CARTESIAN_POINT ( 'NONE',  ( -13.18659385650551918, -9.302874398569244363, 51.68646062012417985 ) ) ;
#21717=CARTESIAN_POINT ( 'NONE',  ( -13.66784385650551670, -6.428312510596451368, 51.20221977374900035 ) ) ;
#21718=FACE_OUTER_BOUND ( 'NONE', #41475, .T. ) ;
#21739=CARTESIAN_POINT ( 'NONE',  ( -17.23659385541304445, -8.995762431863214559, 51.38120296130585274 ) ) ;
#21742=VERTEX_POINT ( 'NONE', #16354 ) ;
#21761=ORIENTED_EDGE ( 'NONE', *, *, #8638, .F. ) ;
#21776=CARTESIAN_POINT ( 'NONE',  ( -15.52409385759799143, -9.359200813967568422, 50.49621490985803263 ) ) ;
#21779=CARTESIAN_POINT ( 'NONE',  ( -17.85534385541293645, -8.623186033802644701, 49.24843789510448033 ) ) ;
#21788=CARTESIAN_POINT ( 'NONE',  ( -17.21159385650551599, -6.922745924619793101, 51.69366785382590024 ) ) ;
#21790=CARTESIAN_POINT ( 'NONE',  ( 22.62590614458706639, 3.140741878271520626, 50.53406581128081143 ) ) ;
#21793=CARTESIAN_POINT ( 'NONE',  ( -17.66159385650551528, -9.295667164867525756, 49.30633214617472504 ) ) ;
#21795=AXIS2_PLACEMENT_3D ( 'NONE', #15004, #30554, #22416 ) ;
#21841=ORIENTED_EDGE ( 'NONE', *, *, #35914, .T. ) ;
#21849=AXIS2_PLACEMENT_3D ( 'NONE', #46020, #45302, #26826 ) ;
#21858=CARTESIAN_POINT ( 'NONE',  ( -20.49909385650551741, -8.114302828567740988, 52.18300498402516041 ) ) ;
#21896=AXIS2_PLACEMENT_3D ( 'NONE', #22255, #10932, #6752 ) ;
#21899=CARTESIAN_POINT ( 'NONE',  ( -14.39909385759799143, -8.105421454601382081, 49.25000573077640098 ) ) ;
#21905=DIRECTION ( 'NONE',  ( 1.616182858256118783E-16, 0.003028072113822189229, -0.9999954153791275058 ) ) ;
#21915=B_SPLINE_CURVE_WITH_KNOTS ( 'NONE', 1,
 ( #33695, #22160 ),
 .UNSPECIFIED., .F., .F.,
 ( 2, 2 ),
 ( 0.000000000000000000, 1.000000000000000000 ),
 .UNSPECIFIED. ) ;
#21919=VERTEX_POINT ( 'NONE', #43949 ) ;
#21937=DIRECTION ( 'NONE',  ( 1.000000000000000000, -4.164305804376849172E-17, 1.614929280266638808E-16 ) ) ;
#21939=CARTESIAN_POINT ( 'NONE',  ( -22.49909385650551741, -8.114302828567740988, 52.18300498402516041 ) ) ;
#21942=EDGE_CURVE ( 'NONE', #21919, #12981, #41544, .T. ) ;
#21950=DIRECTION ( 'NONE',  ( -1.000000000000000000, 4.164305804376849172E-17, -1.614929280266638808E-16 ) ) ;
#21960=CARTESIAN_POINT ( 'NONE',  ( -13.89284385650552167, -7.406986770994973490, 48.81910596585309747 ) ) ;
#21964=EDGE_CURVE ( 'NONE', #12705, #6741, #33293, .T. ) ;
#21984=CARTESIAN_POINT ( 'NONE',  ( -14.98659385541304268, -7.222650657624104298, 49.61879703869476543 ) ) ;
#21988=CARTESIAN_POINT ( 'NONE',  ( 18.62590614458706995, 1.876518846661452411, 52.53023010607846288 ) ) ;
#22013=DIRECTION ( 'NONE',  ( 1.616182858256118536E-16, 0.003028072113822188795, -0.9999954153791273948 ) ) ;
#22017=CARTESIAN_POINT ( 'NONE',  ( -22.58034385650552167, -6.424090610841176385, 49.80797279389978627 ) ) ;
#22020=CARTESIAN_POINT ( 'NONE',  ( -20.98034385759799036, -9.360768649639304329, 51.01397948905922419 ) ) ;
#22033=CARTESIAN_POINT ( 'NONE',  ( -13.97409385650551528, -9.792211528768506312, 50.49490371617623197 ) ) ;
#22043=CARTESIAN_POINT ( 'NONE',  ( -14.11784385650551954, -9.790100578890868377, 49.79778022625163203 ) ) ;
#22048=CARTESIAN_POINT ( 'NONE',  ( -18.84284385650551386, -8.811426318492348031, 52.18089403414751359 ) ) ;
#22076=DIRECTION ( 'NONE',  ( 0.000000000000000000, 0.007114381193220190198, -0.9999746924698832418 ) ) ;
#22102=ORIENTED_EDGE ( 'NONE', *, *, #12679, .F. ) ;
#22111=LINE ( 'NONE', #22592, #200 ) ;
#22114=CARTESIAN_POINT ( 'NONE',  ( -18.69909385650551670, -8.114302828567740988, 52.18300498402516041 ) ) ;
#22150=ORIENTED_EDGE ( 'NONE', *, *, #4784, .T. ) ;
#22152=CIRCLE ( 'NONE', #924, 3.250000000000002220 ) ;
#22156=CARTESIAN_POINT ( 'NONE',  ( -14.34284385759799108, -7.587656875400194068, 49.25157356644813689 ) ) ;
#22160=CARTESIAN_POINT ( 'NONE',  ( -23.42409385541304090, -9.359200813967568422, 50.49621490985803263 ) ) ;
#22179=EDGE_CURVE ( 'NONE', #10355, #15076, #25560, .T. ) ;
#22192=CARTESIAN_POINT ( 'NONE',  ( -21.43034385650551599, -9.794322478646142471, 51.19202720610083190 ) ) ;
#22228=CARTESIAN_POINT ( 'NONE',  ( -14.48034385541304125, -9.360768649639302552, 51.01397948905922419 ) ) ;
#22231=DIRECTION ( 'NONE',  ( -4.115385489419834812E-17, -0.9999954153791275058, -0.003028072113822189229 ) ) ;
#22232=ADVANCED_FACE ( 'NONE', ( #28608 ), #13320, .T. ) ;
#22235=CARTESIAN_POINT ( 'NONE',  ( -20.47409385759799250, -6.859212275519751323, 50.50378509014259265 ) ) ;
#22255=CARTESIAN_POINT ( 'NONE',  ( 8.575906144586951996, -6.109215713985405749, 50.50605614422795497 ) ) ;
#22259=CARTESIAN_POINT ( 'NONE',  ( -21.28659385650551528, -9.302874398569244363, 51.68646062012417985 ) ) ;
#22266=DIRECTION ( 'NONE',  ( 0.000000000000000000, -0.9999954153791273948, -0.003028072113819836944 ) ) ;
#22269=CARTESIAN_POINT ( 'NONE',  ( -17.96784385541291940, -9.357632978295868043, 49.97845033065662790 ) ) ;
#22274=CARTESIAN_POINT ( 'NONE',  ( -15.04284385650551670, -8.811426318492348031, 52.18089403414752070 ) ) ;
#22281=CARTESIAN_POINT ( 'NONE',  ( -14.17409385650551457, -9.792211528768504536, 50.49490371617623197 ) ) ;
#22283=FACE_OUTER_BOUND ( 'NONE', #11490, .T. ) ;
#22286=CARTESIAN_POINT ( 'NONE',  ( -16.48034385650551670, -6.424090610841176385, 49.80797279389977916 ) ) ;
#22344=CARTESIAN_POINT ( 'NONE',  ( -16.22409385541304871, -9.359200813967568422, 50.49621490985801842 ) ) ;
#22346=CARTESIAN_POINT ( 'NONE',  ( -15.26784385650551989, -6.428312510596451368, 51.20221977374900035 ) ) ;
#22357=ORIENTED_EDGE ( 'NONE', *, *, #43794, .T. ) ;
#22361=DIRECTION ( 'NONE',  ( 0.000000000000000000, 1.000000000000000000, 0.000000000000000000 ) ) ;
#22388=CARTESIAN_POINT ( 'NONE',  ( 7.325906144586953772, -0.1092432217106413528, 50.52422457691088908 ) ) ;
#22389=DIRECTION ( 'NONE',  ( 1.000000000000000000, 1.669677910507523057E-21, 6.493791346278465266E-22 ) ) ;
#22390=CARTESIAN_POINT ( 'NONE',  ( -15.18659385759799108, -7.222650657624104298, 49.61879703869476543 ) ) ;
#22416=DIRECTION ( 'NONE',  ( 4.115385489419721413E-17, 0.9999954153791273948, 0.003028072113829171491 ) ) ;
#22429=CARTESIAN_POINT ( 'NONE',  ( -21.71159385650551599, -6.922745924619793101, 51.69366785382590024 ) ) ;
#22439=EDGE_CURVE ( 'NONE', #19879, #3652, #35346, .T. ) ;
#22464=CARTESIAN_POINT ( 'NONE',  ( -20.47409385759799250, -6.859212275519751323, 50.50378509014259265 ) ) ;
#22500=EDGE_CURVE ( 'NONE', #2504, #27510, #1702, .T. ) ;
#22501=CARTESIAN_POINT ( 'NONE',  ( -21.39909385650551599, -8.114302828567740988, 52.18300498402516041 ) ) ;
#22505=CARTESIAN_POINT ( 'NONE',  ( -21.26159385759799036, -7.228003583438117552, 51.38655588711986155 ) ) ;
#22518=CARTESIAN_POINT ( 'NONE',  ( -13.02466918351365877, -9.790356719747981273, 49.88236859574131898 ) ) ;
#22525=CARTESIAN_POINT ( 'NONE',  ( -14.90534385650551918, -8.801233750844183135, 48.81488406609782515 ) ) ;
#22529=CARTESIAN_POINT ( 'NONE',  ( -15.24284385650551776, -8.811426318492348031, 52.18089403414752070 ) ) ;
#22544=CARTESIAN_POINT ( 'NONE',  ( -17.18034385541238507, -9.360768649643061323, 51.01397948905569990 ) ) ;
#22560=CARTESIAN_POINT ( 'NONE',  ( -36.42409385541304800, -6.859212275519750435, 50.50378509014258555 ) ) ;
#22592=CARTESIAN_POINT ( 'NONE',  ( 10.57590614458695377, 0.6667653706753807752, 50.27657325150214973 ) ) ;
#22593=ORIENTED_EDGE ( 'NONE', *, *, #18456, .F. ) ;
#22594=CARTESIAN_POINT ( 'NONE',  ( -15.43659385650551741, -6.915538690918075382, 49.31353937987644542 ) ) ;
#22602=CARTESIAN_POINT ( 'NONE',  ( 23.62590614458706639, 1.890747609047893185, 50.53028072113869484 ) ) ;
#22640=CARTESIAN_POINT ( 'NONE',  ( -13.66784385759799392, -9.357632978295830739, 49.97845033065684106 ) ) ;
#22643=DIRECTION ( 'NONE',  ( 0.000000000000000000, -0.9999954153791273948, -0.003028072113819838245 ) ) ;
#22678=CARTESIAN_POINT ( 'NONE',  ( -19.46159385650551599, -9.295667164867525756, 49.30633214617472504 ) ) ;
#22729=CARTESIAN_POINT ( 'NONE',  ( -15.63659385759799036, -8.995762431863214559, 51.38120296130585274 ) ) ;
#22761=CARTESIAN_POINT ( 'NONE',  ( -18.92409385650551812, -6.426201560718813433, 50.50509628382439331 ) ) ;
#22773=CIRCLE ( 'NONE', #15676, 1.749999999999997558 ) ;
#22778=CARTESIAN_POINT ( 'NONE',  ( -14.42409385650551457, -6.426201560718813433, 50.50509628382439331 ) ) ;
#22786=CARTESIAN_POINT ( 'NONE',  ( -14.06159385650551741, -9.295667164867525756, 49.30633214617472504 ) ) ;
#22791=CARTESIAN_POINT ( 'NONE',  ( -15.80534385650551421, -8.801233750844183135, 48.81488406609782515 ) ) ;
#22855=CARTESIAN_POINT ( 'NONE',  ( -16.61784385650551954, -9.790100578890868377, 49.79778022625163203 ) ) ;
#22873=CARTESIAN_POINT ( 'NONE',  ( 23.52590614458706852, -0.009252390952106800612, 50.53028072113869484 ) ) ;
#22878=DIRECTION ( 'NONE',  ( 1.000000000000000000, -4.164305804376849172E-17, 1.614929280266638808E-16 ) ) ;
#22896=DIRECTION ( 'NONE',  ( -1.000000000000000000, -1.669677910507523057E-21, -6.493791346278465266E-22 ) ) ;
#22898=PLANE ( 'NONE',  #37461 ) ;
#22900=CARTESIAN_POINT ( 'NONE',  ( -21.96159385650551599, -9.295667164867525756, 49.30633214617472504 ) ) ;
#22939=DIRECTION ( 'NONE',  ( -4.115385489419834812E-17, -0.9999954153791273948, -0.003028072113822188795 ) ) ;
#22940=CARTESIAN_POINT ( 'NONE',  ( -21.82409385650551670, -6.426201560718813433, 50.50509628382439331 ) ) ;
#22953=ORIENTED_EDGE ( 'NONE', *, *, #6734, .F. ) ;
#22971=ADVANCED_FACE ( 'NONE', ( #2950 ), #17962, .T. ) ;
#22974=CARTESIAN_POINT ( 'NONE',  ( -14.14284385541304800, -7.587656875400194068, 49.25157356644813689 ) ) ;
#22982=CARTESIAN_POINT ( 'NONE',  ( -13.61159385759799001, -8.990409506049202193, 49.61344411288074951 ) ) ;
#23010=EDGE_CURVE ( 'NONE', #42266, #3256, #18644, .T. ) ;
#23012=CARTESIAN_POINT ( 'NONE',  ( -20.89284385650552522, -7.406986770994972602, 48.81910596585309747 ) ) ;
#23018=CARTESIAN_POINT ( 'NONE',  ( -21.48659385759799179, -7.222650657624104298, 49.61879703869476543 ) ) ;
#23025=CARTESIAN_POINT ( 'NONE',  ( -14.25534385650552238, -7.417179338643134834, 52.18511593390279302 ) ) ;
#23032=CARTESIAN_POINT ( 'NONE',  ( -14.84909385650551705, -8.104110260919579645, 48.81699501597546487 ) ) ;
#23037=CARTESIAN_POINT ( 'NONE',  ( -14.17409385650551457, -9.792211528768504536, 50.49490371617623197 ) ) ;
#23063=CIRCLE ( 'NONE', #15966, 1.249999999999999556 ) ;
#23093=CARTESIAN_POINT ( 'NONE',  ( -15.21159385650551776, -6.922745924619793101, 51.69366785382590024 ) ) ;
#23136=CARTESIAN_POINT ( 'NONE',  ( -13.27409385759798965, -6.859212275519751323, 50.50378509014259265 ) ) ;
#23140=CARTESIAN_POINT ( 'NONE',  ( -14.39909385759799143, -8.105421454601382081, 49.25000573077640098 ) ) ;
#23167=ORIENTED_EDGE ( 'NONE', *, *, #33440, .F. ) ;
#23169=EDGE_CURVE ( 'NONE', #21742, #4040, #47574, .T. ) ;
#23171=CARTESIAN_POINT ( 'NONE',  ( -16.08659385650551599, -9.302874398569244363, 51.68646062012417985 ) ) ;
#23175=ORIENTED_EDGE ( 'NONE', *, *, #20174, .F. ) ;
#23178=CARTESIAN_POINT ( 'NONE',  ( 18.07590614458695200, 2.144077342217588722, 49.43104278224995340 ) ) ;
#23190=CARTESIAN_POINT ( 'NONE',  ( -21.43034385759799321, -6.857644439848013640, 49.98602051094139398 ) ) ;
#23200=AXIS2_PLACEMENT_3D ( 'NONE', #14057, #18250, #48064 ) ;
#23218=EDGE_LOOP ( 'NONE', ( #26089, #17599, #32054, #26849, #46257, #31267, #21598, #35727, #39695, #14913, #30859, #48629, #39983, #21638, #41818, #34568 ) ) ;
#23242=CARTESIAN_POINT ( 'NONE',  ( -21.23034385650551670, -9.794322478646142471, 51.19202720610083190 ) ) ;
#23253=EDGE_CURVE ( 'NONE', #20557, #23343, #18910, .T. ) ;
#23266=CARTESIAN_POINT ( 'NONE',  ( -22.18659385541304374, -7.222650657624104298, 49.61879703869476543 ) ) ;
#23297=CARTESIAN_POINT ( 'NONE',  ( -14.03034385541274531, -6.857644439846917628, 49.98602051094207610 ) ) ;
#23318=CARTESIAN_POINT ( 'NONE',  ( -21.71159385650551599, -6.922745924619793101, 51.69366785382590024 ) ) ;
#23323=CARTESIAN_POINT ( 'NONE',  ( -16.16784385650552025, -6.428312510596451368, 51.20221977374900035 ) ) ;
#23331=DIRECTION ( 'NONE',  ( 1.000000000000000000, -4.164305804376849788E-17, 1.614929280266638808E-16 ) ) ;
#23343=VERTEX_POINT ( 'NONE', #48703 ) ;
#23368=CARTESIAN_POINT ( 'NONE',  ( -21.00534385650551883, -8.801233750844183135, 48.81488406609782515 ) ) ;
#23404=ORIENTED_EDGE ( 'NONE', *, *, #559, .T. ) ;
#23411=CARTESIAN_POINT ( 'NONE',  ( -19.01159385650551670, -6.922745924619793101, 51.69366785382590024 ) ) ;
#23414=DIRECTION ( 'NONE',  ( -1.000000000000000000, 4.164305804376849172E-17, -1.614929280266638808E-16 ) ) ;
#23415=ORIENTED_EDGE ( 'NONE', *, *, #11385, .F. ) ;
#23419=CARTESIAN_POINT ( 'NONE',  ( 18.62590614458706995, 1.890747609047893185, 50.53028072113869484 ) ) ;
#23448=CARTESIAN_POINT ( 'NONE',  ( -22.13034385650552238, -9.794322478646142471, 51.19202720610083901 ) ) ;
#23476=CIRCLE ( 'NONE', #28178, 1.250000000000001998 ) ;
#23485=CARTESIAN_POINT ( 'NONE',  ( -15.94284385650551883, -8.811426318492348031, 52.18089403414752070 ) ) ;
#23502=CARTESIAN_POINT ( 'NONE',  ( -36.42409385541304800, -8.109206544743658540, 50.50000000000030553 ) ) ;
#23510=CARTESIAN_POINT ( 'NONE',  ( -21.23034385541303948, -6.857644439848013640, 49.98602051094139398 ) ) ;
#23531=CARTESIAN_POINT ( 'NONE',  ( -19.91159385759799250, -8.990409506049200417, 49.61344411288074951 ) ) ;
#23545=CARTESIAN_POINT ( 'NONE',  ( -14.14284385541286859, -7.587656875400065282, 49.25157356644783135 ) ) ;
#23575=CARTESIAN_POINT ( 'NONE',  ( -20.64284385650552167, -8.811426318492348031, 52.18089403414751359 ) ) ;
#23576=AXIS2_PLACEMENT_3D ( 'NONE', #32507, #28812, #43849 ) ;
#23579=CARTESIAN_POINT ( 'NONE',  ( 10.57590614458695377, 3.140741878271517962, 50.53406581128081143 ) ) ;
#23625=CARTESIAN_POINT ( 'NONE',  ( -21.45534385650551812, -7.417179338643134834, 52.18511593390279302 ) ) ;
#23633=CYLINDRICAL_SURFACE ( 'NONE', #18085, 1.249999999999998668 ) ;
#23637=ORIENTED_EDGE ( 'NONE', *, *, #17429, .T. ) ;
#23656=EDGE_LOOP ( 'NONE', ( #20195, #34890, #36865, #6823 ) ) ;
#23662=CARTESIAN_POINT ( 'NONE',  ( -18.61784385650552309, -9.790100578890868377, 49.79778022625163203 ) ) ;
#23668=CARTESIAN_POINT ( 'NONE',  ( -33.42409385541304800, -9.359200813967566646, 50.49621490985803263 ) ) ;
#23670=CARTESIAN_POINT ( 'NONE',  ( -15.54909385541290590, -8.112991634885938552, 51.74999426922445878 ) ) ;
#23672=AXIS2_PLACEMENT_3D ( 'NONE', #10713, #3566, #18570 ) ;
#23684=CARTESIAN_POINT ( 'NONE',  ( -21.76784385759799179, -9.357632978295830739, 49.97845033065684106 ) ) ;
#23704=CARTESIAN_POINT ( 'NONE',  ( -21.90534385650552096, -8.801233750844183135, 48.81488406609782515 ) ) ;
#23707=CARTESIAN_POINT ( 'NONE',  ( -23.42409385541304090, -9.359200813967568422, 50.49621490985803263 ) ) ;
#23713=AXIS2_PLACEMENT_3D ( 'NONE', #32637, #29672, #10963 ) ;
#23731=DIRECTION ( 'NONE',  ( 6.374839753205896285E-22, 0.007114381193220334181, -0.9999746924698833528 ) ) ;
#23736=CARTESIAN_POINT ( 'NONE',  ( -15.88659385650551670, -9.302874398569244363, 51.68646062012417985 ) ) ;
#23764=CARTESIAN_POINT ( 'NONE',  ( -20.83659385541304232, -8.995762431863214559, 51.38120296130585274 ) ) ;
#23801=ORIENTED_EDGE ( 'NONE', *, *, #4122, .F. ) ;
#23805=CARTESIAN_POINT ( 'NONE',  ( 18.07590614458695200, 1.637417875877629436, 51.62951866002712364 ) ) ;
#23806=CARTESIAN_POINT ( 'NONE',  ( -21.68034385541343312, -9.360768649636696637, 51.01397948906189583 ) ) ;
#23815=CARTESIAN_POINT ( 'NONE',  ( -22.10534385650551670, -8.801233750844183135, 48.81488406609782515 ) ) ;
#23821=CARTESIAN_POINT ( 'NONE',  ( -22.44284385650551528, -8.811426318492348031, 52.18089403414751359 ) ) ;
#23833=( BOUNDED_CURVE ( )  B_SPLINE_CURVE ( 3, ( #5565, #35576, #890, #8515 ),
 .UNSPECIFIED., .F., .F. ) 
 B_SPLINE_CURVE_WITH_KNOTS ( ( 4, 4 ),
 ( -7.993605777301127091E-15, 0.2013579207903272439 ),
 .UNSPECIFIED. ) 
 CURVE ( )  GEOMETRIC_REPRESENTATION_ITEM ( )  RATIONAL_B_SPLINE_CURVE ( ( 1.000000000000000000, 0.9966241020034157794, 0.9966241020034157794, 1.000000000000000000 ) ) 
 REPRESENTATION_ITEM ( '' )  );
#23863=CARTESIAN_POINT ( 'NONE',  ( -21.62409385650551741, -6.426201560718812544, 50.50509628382439331 ) ) ;
#23881=DIRECTION ( 'NONE',  ( 1.000000000000000000, -4.164305804376849172E-17, 1.614929280266638808E-16 ) ) ;
#23887=DIRECTION ( 'NONE',  ( -1.000000000000000000, -1.669677910507523057E-21, -6.493791346278465266E-22 ) ) ;
#23896=CARTESIAN_POINT ( 'NONE',  ( -17.09909385759799250, -8.105421454601382081, 49.25000573077640098 ) ) ;
#23902=CARTESIAN_POINT ( 'NONE',  ( -15.69284385650551350, -7.406986770994972602, 48.81910596585309747 ) ) ;
#23910=CARTESIAN_POINT ( 'NONE',  ( -15.38034385541287463, -9.360768649639723549, 51.01397948905911761 ) ) ;
#23921=CARTESIAN_POINT ( 'NONE',  ( -21.99284385759798965, -8.630756214087126565, 51.74842643355248129 ) ) ;
#23969=CARTESIAN_POINT ( 'NONE',  ( -16.50534385650551883, -8.801233750844183135, 48.81488406609782515 ) ) ;
#23990=LINE ( 'NONE', #46641, #15064 ) ;
#23996=CARTESIAN_POINT ( 'NONE',  ( -20.04909385541304445, -8.112991634885936776, 51.74999426922421719 ) ) ;
#24021=EDGE_CURVE ( 'NONE', #35561, #11000, #35619, .T. ) ;
#24046=CARTESIAN_POINT ( 'NONE',  ( -16.03034385759799463, -6.857644439848019857, 49.98602051094139398 ) ) ;
#24052=CARTESIAN_POINT ( 'NONE',  ( -21.76784385650551101, -6.428312510596451368, 51.20221977374900035 ) ) ;
#24057=CARTESIAN_POINT ( 'NONE',  ( -13.91784385650551670, -9.790100578890868377, 49.79778022625163203 ) ) ;
#24073=CARTESIAN_POINT ( 'NONE',  ( 6.575906144586949331, -6.109215713985405749, 50.50605614422795497 ) ) ;
#24085=EDGE_CURVE ( 'NONE', #9159, #4206, #45390, .T. ) ;
#24096=CARTESIAN_POINT ( 'NONE',  ( -19.31784385650551528, -9.790100578890868377, 49.79778022625163203 ) ) ;
#24107=CARTESIAN_POINT ( 'NONE',  ( -22.69284385541299542, -8.630756214087158540, 51.74842643355255944 ) ) ;
#24137=CARTESIAN_POINT ( 'NONE',  ( -17.09909385650551528, -8.114302828567740988, 52.18300498402516041 ) ) ;
#24141=VECTOR ( 'NONE', #39830, 1000.000000000000114 ) ;
#24153=ORIENTED_EDGE ( 'NONE', *, *, #7401, .F. ) ;
#24156=CARTESIAN_POINT ( 'NONE',  ( -20.53034385759798752, -6.857644439848013640, 49.98602051094139398 ) ) ;
#24158=ADVANCED_FACE ( 'NONE', ( #47081 ), #8935, .T. ) ;
#24166=FACE_OUTER_BOUND ( 'NONE', #41048, .T. ) ;
#24179=CARTESIAN_POINT ( 'NONE',  ( -21.82409385759798681, -9.359200813967568422, 50.49621490985803263 ) ) ;
#24180=CARTESIAN_POINT ( 'NONE',  ( -36.42409385541304800, -8.109206544743658540, 50.50000000000030553 ) ) ;
#24184=EDGE_LOOP ( 'NONE', ( #22102, #8434, #471, #8329 ) ) ;
#24194=FACE_BOUND ( 'NONE', #29268, .T. ) ;
#24208=CARTESIAN_POINT ( 'NONE',  ( -15.09909385650551705, -8.114302828567740988, 52.18300498402516041 ) ) ;
#24217=VECTOR ( 'NONE', #13631, 1000.000000000000000 ) ;
#24238=CARTESIAN_POINT ( 'NONE',  ( -20.16159385541304161, -7.228003583438117552, 51.38655588711986155 ) ) ;
#24240=AXIS2_PLACEMENT_3D ( 'NONE', #46835, #24913, #31576 ) ;
#24247=ADVANCED_FACE ( 'NONE', ( #2015, #32059 ), #43399, .F. ) ;
#24251=ORIENTED_EDGE ( 'NONE', *, *, #24780, .T. ) ;
#24267=CARTESIAN_POINT ( 'NONE',  ( 18.54465614458695200, 3.140741878271521070, 50.53406581128081143 ) ) ;
#24295=CARTESIAN_POINT ( 'NONE',  ( -22.21784385650551741, -9.790100578890868377, 49.79778022625163203 ) ) ;
#24297=CARTESIAN_POINT ( 'NONE',  ( 18.87590614458706995, 1.876874565721113663, 52.48023137145496264 ) ) ;
#24301=CARTESIAN_POINT ( 'NONE',  ( -13.74909385650551563, -8.104110260919579645, 48.81699501597546487 ) ) ;
#24306=CIRCLE ( 'NONE', #1470, 1.249999999999999556 ) ;
#24319=CARTESIAN_POINT ( 'NONE',  ( -36.42409385541304800, -9.159201730891741278, 50.49682052428079970 ) ) ;
#24341=CARTESIAN_POINT ( 'NONE',  ( -19.54284385650551670, -8.811426318492348031, 52.18089403414751359 ) ) ;
#24363=CARTESIAN_POINT ( 'NONE',  ( -13.91784385541274460, -6.860780111191973063, 51.02154966934469371 ) ) ;
#24369=DIRECTION ( 'NONE',  ( 0.000000000000000000, 0.007114381193220190198, -0.9999746924698832418 ) ) ;
#24390=PLANE ( 'NONE',  #42804 ) ;
#24402=CARTESIAN_POINT ( 'NONE',  ( -19.40534385759799463, -7.595227055684746986, 51.75156210489594599 ) ) ;
#24436=VERTEX_POINT ( 'NONE', #30804 ) ;
#24450=CARTESIAN_POINT ( 'NONE',  ( 10.57590614458695377, 1.890747609047609190, 50.53028072113853142 ) ) ;
#24460=CARTESIAN_POINT ( 'NONE',  ( -16.11159385650551457, -6.922745924619793101, 51.69366785382590024 ) ) ;
#24486=CARTESIAN_POINT ( 'NONE',  ( -18.02409385541303877, -9.359200813967568422, 50.49621490985803263 ) ) ;
#24494=CARTESIAN_POINT ( 'NONE',  ( -15.32409385541304481, -9.359200813967568422, 50.49621490985804684 ) ) ;
#24499=AXIS2_PLACEMENT_3D ( 'NONE', #36728, #48319, #3017 ) ;
#24500=DIRECTION ( 'NONE',  ( 1.000000000000000000, -4.164305804376849172E-17, 1.614929280266638808E-16 ) ) ;
#24545=CARTESIAN_POINT ( 'NONE',  ( -19.79909385650551457, -8.114302828567740988, 52.18300498402516041 ) ) ;
#24549=CARTESIAN_POINT ( 'NONE',  ( -13.86159385650551812, -9.295667164867525756, 49.30633214617472504 ) ) ;
#24589=EDGE_LOOP ( 'NONE', ( #13468, #5486, #32396, #7519, #23415 ) ) ;
#24594=CARTESIAN_POINT ( 'NONE',  ( -20.04909385650551457, -8.104110260919579645, 48.81699501597546487 ) ) ;
#24595=DIRECTION ( 'NONE',  ( 1.000000000000000000, -4.164305804376849788E-17, 1.614929280266638808E-16 ) ) ;
#24601=VERTEX_POINT ( 'NONE', #45225 ) ;
#24603=CARTESIAN_POINT ( 'NONE',  ( -22.80534385541300324, -7.595227055684715900, 51.75156210489603126 ) ) ;
#24607=CARTESIAN_POINT ( 'NONE',  ( -21.39909385650551599, -8.114302828567740988, 52.18300498402516041 ) ) ;
#24617=CARTESIAN_POINT ( 'NONE',  ( -36.42409385541304800, -9.359200813967566646, 50.49621490985803263 ) ) ;
#24629=CARTESIAN_POINT ( 'NONE',  ( -13.78034385650551563, -6.424090610841176385, 49.80797279389978627 ) ) ;
#24635=PLANE ( 'NONE',  #15626 ) ;
#24650=CARTESIAN_POINT ( 'NONE',  ( -19.57409385759799036, -6.859212275519751323, 50.50378509014259265 ) ) ;
#24678=VERTEX_POINT ( 'NONE', #3349 ) ;
#24680=DIRECTION ( 'NONE',  ( -4.115385489420004910E-17, -0.9999954153791273948, -0.003028072113811714535 ) ) ;
#24697=CARTESIAN_POINT ( 'NONE',  ( -17.83034385759799179, -6.857644439848014528, 49.98602051094139398 ) ) ;
#24699=ORIENTED_EDGE ( 'NONE', *, *, #41674, .F. ) ;
#24726=CARTESIAN_POINT ( 'NONE',  ( -18.24909385541304374, -8.112991634885936776, 51.74999426922421719 ) ) ;
#24734=CARTESIAN_POINT ( 'NONE',  ( -14.42409385541304090, -9.359200813967568422, 50.49621490985801842 ) ) ;
#24749=CARTESIAN_POINT ( 'NONE',  ( 10.57590614458695377, 0.6407533398237040823, 50.52649563099625851 ) ) ;
#24755=CARTESIAN_POINT ( 'NONE',  ( -13.42364920204782841, -9.064338107659910548, 49.69363550579117117 ) ) ;
#24761=ADVANCED_FACE ( 'NONE', ( #8507 ), #30929, .T. ) ;
#24779=CARTESIAN_POINT ( 'NONE',  ( -17.88659385650551670, -9.302874398569244363, 51.68646062012417985 ) ) ;
#24780=EDGE_CURVE ( 'NONE', #41647, #13929, #46429, .T. ) ;
#24783=CARTESIAN_POINT ( 'NONE',  ( -19.51784385650551457, -9.790100578890868377, 49.79778022625163203 ) ) ;
#24820=CARTESIAN_POINT ( 'NONE',  ( -16.84284385650551741, -8.811426318492348031, 52.18089403414752070 ) ) ;
#24828=ORIENTED_EDGE ( 'NONE', *, *, #35181, .T. ) ;
#24830=CARTESIAN_POINT ( 'NONE',  ( -36.42409385541304800, -8.109206544743658540, 50.50000000000030553 ) ) ;
#24837=( BOUNDED_CURVE ( )  B_SPLINE_CURVE ( 2, ( #15066, #26910, #22982, #26414, #38455, #4741, #801, #3764, #4487 ),
 .UNSPECIFIED., .F., .F. ) 
 B_SPLINE_CURVE_WITH_KNOTS ( ( 3, 2, 2, 2, 3 ),
 ( 0.8333333333333334814, 0.8437500000000001110, 0.8541666666666667407, 0.8645833333333333703, 0.8750000000000000000 ),
 .UNSPECIFIED. ) 
 CURVE ( )  GEOMETRIC_REPRESENTATION_ITEM ( )  RATIONAL_B_SPLINE_CURVE ( ( 0.9999999999999992228, 0.9238795325112875156, 1.000000000000000000, 0.9238795325112867385, 1.000000000000000000, 0.9238795325112867385, 1.000000000000000000, 0.9238795325112867385, 1.000000000000000000 ) ) 
 REPRESENTATION_ITEM ( '' )  );
#24838=CARTESIAN_POINT ( 'NONE',  ( -20.21784385650551386, -9.790100578890868377, 49.79778022625163203 ) ) ;
#24847=DIRECTION ( 'NONE',  ( 0.000000000000000000, 0.9999954153791273948, 0.003028072113820366902 ) ) ;
#24857=CARTESIAN_POINT ( 'NONE',  ( -14.90534385759799463, -7.595227055684746986, 51.75156210489594599 ) ) ;
#24860=CARTESIAN_POINT ( 'NONE',  ( -13.17364477763805652, -9.395196358873663556, 49.41429196092195042 ) ) ;
#24862=VERTEX_POINT ( 'NONE', #32133 ) ;
#24865=DIRECTION ( 'NONE',  ( 1.616182858256118536E-16, 0.003028072113822188795, -0.9999954153791273948 ) ) ;
#24868=DIRECTION ( 'NONE',  ( 1.000000000000000000, -4.164305804376849172E-17, 1.614929280266638808E-16 ) ) ;
#24877=CARTESIAN_POINT ( 'NONE',  ( -20.30534385759798965, -7.595227055684746986, 51.75156210489594599 ) ) ;
#24895=EDGE_CURVE ( 'NONE', #13929, #1563, #41557, .T. ) ;
#24912=DIRECTION ( 'NONE',  ( 1.616182858256114592E-16, 0.003028072113811714535, -0.9999954153791273948 ) ) ;
#24913=DIRECTION ( 'NONE',  ( 1.000000000000000000, -4.164305804376849172E-17, 1.614929280266638808E-16 ) ) ;
#24914=ORIENTED_EDGE ( 'NONE', *, *, #17601, .F. ) ;
#24926=CARTESIAN_POINT ( 'NONE',  ( -13.86159385650551812, -9.295667164867525756, 49.30633214617472504 ) ) ;
#24955=CARTESIAN_POINT ( 'NONE',  ( -19.37409385541304374, -6.859212275519751323, 50.50378509014259265 ) ) ;
#24958=LINE ( 'NONE', #21988, #41787 ) ;
#24967=VERTEX_POINT ( 'NONE', #41444 ) ;
#24979=( BOUNDED_CURVE ( )  B_SPLINE_CURVE ( 2, ( #7238, #18784, #11397, #37731, #18282, #7973, #30375, #48579, #25683 ),
 .UNSPECIFIED., .F., .F. ) 
 B_SPLINE_CURVE_WITH_KNOTS ( ( 3, 2, 2, 2, 3 ),
 ( 0.3333333333333332593, 0.3437499999999998890, 0.3541666666666665741, 0.3645833333333331483, 0.3749999999999998335 ),
 .UNSPECIFIED. ) 
 CURVE ( )  GEOMETRIC_REPRESENTATION_ITEM ( )  RATIONAL_B_SPLINE_CURVE ( ( 1.000000000000000444, 0.9238795325112862944, 1.000000000000000000, 0.9238795325112867385, 1.000000000000000000, 0.9238795325112867385, 1.000000000000000000, 0.9238795325112879597, 0.9999999999999987788 ) ) 
 REPRESENTATION_ITEM ( '' )  );
#24988=CARTESIAN_POINT ( 'NONE',  ( -22.63659385650551670, -6.915538690918074494, 49.31353937987644542 ) ) ;
#25011=CARTESIAN_POINT ( 'NONE',  ( -18.50534385650551883, -8.801233750844183135, 48.81488406609782515 ) ) ;
#25016=ADVANCED_FACE ( 'NONE', ( #40474 ), #2804, .T. ) ;
#25017=CARTESIAN_POINT ( 'NONE',  ( -18.22409385650551528, -6.426201560718813433, 50.50509628382439331 ) ) ;
#25034=CARTESIAN_POINT ( 'NONE',  ( -33.42409385541304800, -8.109206544743658540, 50.50000000000030553 ) ) ;
#25067=EDGE_CURVE ( 'NONE', #24678, #42690, #18543, .T. ) ;
#25072=CARTESIAN_POINT ( 'NONE',  ( 25.57590614458706568, 1.904620652374673151, 48.58033007082241994 ) ) ;
#25078=CARTESIAN_POINT ( 'NONE',  ( -19.14909385650551954, -8.104110260919579645, 48.81699501597546487 ) ) ;
#25084=EDGE_CURVE ( 'NONE', #29468, #19879, #20552, .T. ) ;
#25123=CARTESIAN_POINT ( 'NONE',  ( -20.02409385759798965, -9.359200813967568422, 50.49621490985803263 ) ) ;
#25127=LINE ( 'NONE', #9865, #33337 ) ;
#25166=DIRECTION ( 'NONE',  ( -1.000000000000000000, -1.669677910507523057E-21, -6.493791346278465266E-22 ) ) ;
#25176=VECTOR ( 'NONE', #45772, 1000.000000000000000 ) ;
#25203=CARTESIAN_POINT ( 'NONE',  ( -18.98034385541303948, -9.360768649639302552, 51.01397948905922419 ) ) ;
#25232=CARTESIAN_POINT ( 'NONE',  ( -21.68034385650551599, -6.424090610841176385, 49.80797279389978627 ) ) ;
#25245=VECTOR ( 'NONE', #11505, 1000.000000000000000 ) ;
#25251=CARTESIAN_POINT ( 'NONE',  ( -36.42409385541304800, -9.359200813967566646, 50.49621490985803263 ) ) ;
#25257=CARTESIAN_POINT ( 'NONE',  ( -17.32409385650551314, -6.426201560718813433, 50.50509628382439331 ) ) ;
#25261=CARTESIAN_POINT ( 'NONE',  ( -19.29284385650551670, -7.406986770994973490, 48.81910596585309747 ) ) ;
#25262=ORIENTED_EDGE ( 'NONE', *, *, #25067, .T. ) ;
#25313=CARTESIAN_POINT ( 'NONE',  ( -13.10534385759798681, -7.595227055684746986, 51.75156210489594599 ) ) ;
#25315=ORIENTED_EDGE ( 'NONE', *, *, #46649, .F. ) ;
#25322=CARTESIAN_POINT ( 'NONE',  ( -18.53034385650551386, -9.794322478646142471, 51.19202720610083901 ) ) ;
#25363=CARTESIAN_POINT ( 'NONE',  ( -16.76159385759799036, -7.228003583438117552, 51.38655588711986155 ) ) ;
#25367=DIRECTION ( 'NONE',  ( 0.000000000000000000, 0.9999954153791273948, 0.003028072113822398263 ) ) ;
#25393=CARTESIAN_POINT ( 'NONE',  ( -18.44909385759799036, -8.112991634885936776, 51.74999426922421719 ) ) ;
#25411=CARTESIAN_POINT ( 'NONE',  ( -13.24284385650551599, -8.811426318492348031, 52.18089403414752070 ) ) ;
#25429=FACE_BOUND ( 'NONE', #23218, .T. ) ;
#25431=CARTESIAN_POINT ( 'NONE',  ( -20.92409385759799179, -9.359200813967568422, 50.49621490985803263 ) ) ;
#25439=CARTESIAN_POINT ( 'NONE',  ( -18.92409385541304090, -9.359200813967568422, 50.49621490985803263 ) ) ;
#25476=ORIENTED_EDGE ( 'NONE', *, *, #27331, .T. ) ;
#25484=CARTESIAN_POINT ( 'NONE',  ( -16.93034385650552309, -9.794322478646142471, 51.19202720610083901 ) ) ;
#25487=DIRECTION ( 'NONE',  ( 1.000000000000000000, -4.164305804376849172E-17, 1.614929280266638808E-16 ) ) ;
#25488=CARTESIAN_POINT ( 'NONE',  ( -19.01159385650551670, -6.922745924619793101, 51.69366785382590024 ) ) ;
#25502=CARTESIAN_POINT ( 'NONE',  ( -19.59909385541296345, -8.105421454601382081, 49.25000573077626598 ) ) ;
#25540=CARTESIAN_POINT ( 'NONE',  ( -13.16159385759798894, -7.228003583438117552, 51.38655588711986155 ) ) ;
#25543=DIRECTION ( 'NONE',  ( 1.000000000000000000, -4.164305804376849172E-17, 1.614929280266638808E-16 ) ) ;
#25547=DIRECTION ( 'NONE',  ( -1.000000000000000000, 4.164305804376849172E-17, -1.614929280266638808E-16 ) ) ;
#25550=CARTESIAN_POINT ( 'NONE',  ( -20.16159385650551883, -9.295667164867525756, 49.30633214617472504 ) ) ;
#25555=EDGE_CURVE ( 'NONE', #21318, #23343, #24306, .T. ) ;
#25560=( BOUNDED_CURVE ( )  B_SPLINE_CURVE ( 2, ( #6448, #10387, #2014, #17008, #25393, #36218, #2256, #28372, #43398 ),
 .UNSPECIFIED., .F., .F. ) 
 B_SPLINE_CURVE_WITH_KNOTS ( ( 3, 2, 2, 2, 3 ),
 ( 0.3749999999999998335, 0.3854166666666665741, 0.3958333333333332593, 0.4062500000000000000, 0.4166666666666667407 ),
 .UNSPECIFIED. ) 
 CURVE ( )  GEOMETRIC_REPRESENTATION_ITEM ( )  RATIONAL_B_SPLINE_CURVE ( ( 1.000000000000001110, 0.9238795325112855172, 1.000000000000000000, 0.9238795325112867385, 1.000000000000000000, 0.9238795325112867385, 1.000000000000000000, 0.9238795325112862944, 1.000000000000000444 ) ) 
 REPRESENTATION_ITEM ( '' )  );
#25591=CARTESIAN_POINT ( 'NONE',  ( -16.25534385759799250, -8.623186033802570094, 49.24843789510467218 ) ) ;
#25628=CARTESIAN_POINT ( 'NONE',  ( -20.81159385650551386, -6.922745924619793101, 51.69366785382590024 ) ) ;
#25647=CARTESIAN_POINT ( 'NONE',  ( -13.83659385650551776, -6.915538690918075382, 49.31353937987644542 ) ) ;
#25662=DIRECTION ( 'NONE',  ( 0.000000000000000000, -0.9999954153791273948, -0.003028072113819838245 ) ) ;
#25665=ORIENTED_EDGE ( 'NONE', *, *, #6542, .T. ) ;
#25669=CARTESIAN_POINT ( 'NONE',  ( -15.49284385541304232, -8.630756214087126565, 51.74842643355248129 ) ) ;
#25678=ADVANCED_FACE ( 'NONE', ( #35681 ), #24635, .F. ) ;
#25683=CARTESIAN_POINT ( 'NONE',  ( -18.67409385759799179, -6.859212275519751323, 50.50378509014259265 ) ) ;
#25686=FACE_OUTER_BOUND ( 'NONE', #5523, .T. ) ;
#25704=CARTESIAN_POINT ( 'NONE',  ( -22.80534385650551954, -8.801233750844183135, 48.81488406609782515 ) ) ;
#25714=ORIENTED_EDGE ( 'NONE', *, *, #32363, .T. ) ;
#25719=CARTESIAN_POINT ( 'NONE',  ( -19.26159385650551670, -9.295667164867525756, 49.30633214617472504 ) ) ;
#25726=CARTESIAN_POINT ( 'NONE',  ( -14.39909385650551776, -8.114302828567740988, 52.18300498402516041 ) ) ;
#25730=CARTESIAN_POINT ( 'NONE',  ( -20.41784385650551314, -9.790100578890868377, 49.79778022625163203 ) ) ;
#25742=CARTESIAN_POINT ( 'NONE',  ( -19.65534385541296203, -8.623186033802625161, 49.24843789510452297 ) ) ;
#25776=ORIENTED_EDGE ( 'NONE', *, *, #27963, .T. ) ;
#25786=CARTESIAN_POINT ( 'NONE',  ( -12.88034385759799250, -9.360768649639304329, 51.01397948905922419 ) ) ;
#25797=CARTESIAN_POINT ( 'NONE',  ( -19.26159385650551670, -9.295667164867525756, 49.30633214617472504 ) ) ;
#25837=CARTESIAN_POINT ( 'NONE',  ( -15.52409385759799143, -9.359200813967568422, 50.49621490985803263 ) ) ;
#25855=CYLINDRICAL_SURFACE ( 'NONE', #31195, 1.249999999999998668 ) ;
#25879=CARTESIAN_POINT ( 'NONE',  ( -20.86784385650551954, -6.428312510596451368, 51.20221977374900035 ) ) ;
#25881=AXIS2_PLACEMENT_3D ( 'NONE', #5851, #47213, #32436 ) ;
#25888=CARTESIAN_POINT ( 'NONE',  ( -35.42409385541304800, -8.109206544743658540, 50.50000000000030553 ) ) ;
#25899=CARTESIAN_POINT ( 'NONE',  ( -13.94909385650551492, -8.104110260919579645, 48.81699501597546487 ) ) ;
#25924=CARTESIAN_POINT ( 'NONE',  ( -13.74909385541304374, -8.112991634885936776, 51.74999426922421719 ) ) ;
#25926=CARTESIAN_POINT ( 'NONE',  ( 8.575906144586950219, -6.109215713985405749, 50.50605614422795497 ) ) ;
#25955=CARTESIAN_POINT ( 'NONE',  ( -18.24909385650551741, -8.104110260919579645, 48.81699501597546487 ) ) ;
#25970=CARTESIAN_POINT ( 'NONE',  ( -15.60534385650551847, -8.801233750844183135, 48.81488406609782515 ) ) ;
#25978=CARTESIAN_POINT ( 'NONE',  ( -15.13034385650551528, -9.794322478646142471, 51.19202720610083901 ) ) ;
#25981=FACE_OUTER_BOUND ( 'NONE', #48611, .T. ) ;
#25984=CARTESIAN_POINT ( 'NONE',  ( -16.98659385650551812, -9.302874398569244363, 51.68646062012417985 ) ) ;
#25988=ORIENTED_EDGE ( 'NONE', *, *, #6542, .F. ) ;
#26044=LINE ( 'NONE', #25072, #35399 ) ;
#26048=CARTESIAN_POINT ( 'NONE',  ( -16.22409385650551883, -6.426201560718813433, 50.50509628382439331 ) ) ;
#26084=CYLINDRICAL_SURFACE ( 'NONE', #39667, 1.249999999999998668 ) ;
#26089=ORIENTED_EDGE ( 'NONE', *, *, #5052, .F. ) ;
#26090=AXIS2_PLACEMENT_3D ( 'NONE', #29054, #21905, #25367 ) ;
#26092=CYLINDRICAL_SURFACE ( 'NONE', #47708, 1.249999999999998668 ) ;
#26093=CARTESIAN_POINT ( 'NONE',  ( -15.35534385759798859, -8.623186033802571870, 49.24843789510467218 ) ) ;
#26106=CARTESIAN_POINT ( 'NONE',  ( -36.42409385541304800, -8.109206544743658540, 50.50000000000030553 ) ) ;
#26122=ORIENTED_EDGE ( 'NONE', *, *, #47727, .T. ) ;
#26131=CARTESIAN_POINT ( 'NONE',  ( -19.85534385650552025, -7.417179338643134834, 52.18511593390279302 ) ) ;
#26141=DIRECTION ( 'NONE',  ( -0.9524241471993249997, -0.0009228828802096092788, 0.3047743298226210373 ) ) ;
#26177=ORIENTED_EDGE ( 'NONE', *, *, #4784, .F. ) ;
#26183=ORIENTED_EDGE ( 'NONE', *, *, #21501, .F. ) ;
#26193=DIRECTION ( 'NONE',  ( -4.115385489419834196E-17, -0.9999954153791273948, -0.003028072113822188795 ) ) ;
#26201=CARTESIAN_POINT ( 'NONE',  ( -21.06159385650551741, -9.295667164867525756, 49.30633214617472504 ) ) ;
#26214=CARTESIAN_POINT ( 'NONE',  ( -13.24284385650551599, -8.811426318492348031, 52.18089403414752070 ) ) ;
#26222=CARTESIAN_POINT ( 'NONE',  ( -13.07679657469475032, -8.645136888763005345, 48.52585319722742696 ) ) ;
#26224=DIRECTION ( 'NONE',  ( 0.000000000000000000, -0.9999954153791273948, -0.003028072113819838245 ) ) ;
#26225=CARTESIAN_POINT ( 'NONE',  ( -14.39909385650551776, -8.114302828567740988, 52.18300498402516041 ) ) ;
#26248=CARTESIAN_POINT ( 'NONE',  ( -36.42409385541304800, -8.109206544743658540, 50.50000000000030553 ) ) ;
#26252=CARTESIAN_POINT ( 'NONE',  ( -13.97409385541301496, -6.859212275519754876, 50.50378509014287687 ) ) ;
#26259=CARTESIAN_POINT ( 'NONE',  ( -36.42409385541304800, -8.109206544743658540, 50.50000000000030553 ) ) ;
#26268=EDGE_LOOP ( 'NONE', ( #13983, #29091, #41604, #3872 ) ) ;
#26277=CARTESIAN_POINT ( 'NONE',  ( -20.21784385541269558, -6.860780111193637509, 51.02154966934593006 ) ) ;
#26287=CARTESIAN_POINT ( 'NONE',  ( -14.08659385650551776, -9.302874398569244363, 51.68646062012417985 ) ) ;
#26291=CARTESIAN_POINT ( 'NONE',  ( -12.72364920584387349, -9.064356868646193277, 49.69365772853683438 ) ) ;
#26329=CARTESIAN_POINT ( 'NONE',  ( -15.46784385759799285, -9.357632978295830739, 49.97845033065684106 ) ) ;
#26332=CARTESIAN_POINT ( 'NONE',  ( -14.62409385759799108, -9.359200813967568422, 50.49621490985803263 ) ) ;
#26342=DIRECTION ( 'NONE',  ( 0.000000000000000000, 0.9999954153791273948, 0.003028072113820366902 ) ) ;
#26344=( LENGTH_UNIT ( ) NAMED_UNIT ( * ) SI_UNIT ( .MILLI., .METRE. ) );
#26365=CARTESIAN_POINT ( 'NONE',  ( -21.65534385650552096, -7.417179338643134834, 52.18511593390279302 ) ) ;
#26383=ORIENTED_EDGE ( 'NONE', *, *, #37359, .T. ) ;
#26393=LINE ( 'NONE', #48550, #11023 ) ;
#26402=CARTESIAN_POINT ( 'NONE',  ( -21.45534385541298406, -8.623186033802610950, 49.24843789510456560 ) ) ;
#26407=CARTESIAN_POINT ( 'NONE',  ( -15.54909385541304268, -8.112991634885936776, 51.74999426922421719 ) ) ;
#26414=CARTESIAN_POINT ( 'NONE',  ( -13.55534385759798965, -8.623186033802571870, 49.24843789510467218 ) ) ;
#26430=EDGE_CURVE ( 'NONE', #32426, #12395, #4652, .T. ) ;
#26440=CARTESIAN_POINT ( 'NONE',  ( -21.11784385650551954, -9.790100578890868377, 49.79778022625163203 ) ) ;
#26444=VERTEX_POINT ( 'NONE', #17190 ) ;
#26455=CARTESIAN_POINT ( 'NONE',  ( -14.70534385650551989, -8.801233750844183135, 48.81488406609782515 ) ) ;
#26465=CARTESIAN_POINT ( 'NONE',  ( -16.59284385650551741, -7.406986770994973490, 48.81910596585309747 ) ) ;
#26469=CARTESIAN_POINT ( 'NONE',  ( -15.69284385650551172, -7.406986770994973490, 48.81910596585309747 ) ) ;
#26525=EDGE_CURVE ( 'NONE', #29639, #1741, #17206, .T. ) ;
#26532=CARTESIAN_POINT ( 'NONE',  ( -17.51784385650551812, -9.790100578890868377, 49.79778022625163203 ) ) ;
#26543=( BOUNDED_CURVE ( )  B_SPLINE_CURVE ( 1, ( #30464, #30707 ),
 .UNSPECIFIED., .F., .F. ) 
 B_SPLINE_CURVE_WITH_KNOTS ( ( 2, 2 ),
 ( 0.000000000000000000, 1.000000000000000000 ),
 .UNSPECIFIED. ) 
 CURVE ( )  GEOMETRIC_REPRESENTATION_ITEM ( )  RATIONAL_B_SPLINE_CURVE ( ( 0.9847278705211290895, 0.9847278705211290895 ) ) 
 REPRESENTATION_ITEM ( '' )  );
#26551=FACE_OUTER_BOUND ( 'NONE', #83, .T. ) ;
#26576=CARTESIAN_POINT ( 'NONE',  ( -21.56784385650551528, -6.428312510596450480, 51.20221977374900035 ) ) ;
#26582=ORIENTED_EDGE ( 'NONE', *, *, #24085, .T. ) ;
#26585=EDGE_CURVE ( 'NONE', #17102, #8229, #47179, .T. ) ;
#26595=CARTESIAN_POINT ( 'NONE',  ( -15.15534385541304729, -8.623186033802571870, 49.24843789510467928 ) ) ;
#26616=CARTESIAN_POINT ( 'NONE',  ( -19.18034385650551599, -6.424090610841176385, 49.80797279389978627 ) ) ;
#26624=CARTESIAN_POINT ( 'NONE',  ( -22.13034385541265792, -6.857644439845596906, 49.98602051094377430 ) ) ;
#26626=AXIS2_PLACEMENT_3D ( 'NONE', #7552, #172, #15148 ) ;
#26638=DIRECTION ( 'NONE',  ( 0.000000000000000000, 0.9999954153791273948, 0.003028072113819836077 ) ) ;
#26639=AXIS2_PLACEMENT_3D ( 'NONE', #42434, #8703, #23731 ) ;
#26653=CARTESIAN_POINT ( 'NONE',  ( -15.60534385541304836, -7.595227055684746986, 51.75156210489594599 ) ) ;
#26655=CARTESIAN_POINT ( 'NONE',  ( -23.03034385541303308, -6.857644439848129991, 49.98602051094116661 ) ) ;
#26674=EDGE_CURVE ( 'NONE', #18062, #13744, #29066, .T. ) ;
#26684=CARTESIAN_POINT ( 'NONE',  ( -17.77409385759798965, -6.859212275519751323, 50.50378509014259265 ) ) ;
#26689=CARTESIAN_POINT ( 'NONE',  ( -18.13659385650551670, -6.915538690918074494, 49.31353937987644542 ) ) ;
#26703=CARTESIAN_POINT ( 'NONE',  ( -16.50534385650551883, -8.801233750844183135, 48.81488406609782515 ) ) ;
#26712=ORIENTED_EDGE ( 'NONE', *, *, #48332, .F. ) ;
#26714=CARTESIAN_POINT ( 'NONE',  ( -16.19909385650551670, -8.114302828567740988, 52.18300498402516041 ) ) ;
#26718=CARTESIAN_POINT ( 'NONE',  ( -15.01784385650551457, -9.790100578890868377, 49.79778022625163203 ) ) ;
#26784=CARTESIAN_POINT ( 'NONE',  ( -17.29284385650551670, -7.406986770994973490, 48.81910596585309747 ) ) ;
#26814=UNCERTAINTY_MEASURE_WITH_UNIT (LENGTH_MEASURE( 1.000000000000000082E-05 ), #11559, 'distance_accuracy_value', 'NONE');
#26826=DIRECTION ( 'NONE',  ( -1.000000000000000000, 2.276824562219560297E-16, 0.000000000000000000 ) ) ;
#26828=CARTESIAN_POINT ( 'NONE',  ( -20.89284385650552167, -7.406986770994973490, 48.81910596585309747 ) ) ;
#26834=AXIS2_PLACEMENT_3D ( 'NONE', #20896, #31977, #35891 ) ;
#26843=CARTESIAN_POINT ( 'NONE',  ( -36.42409385541304800, -6.859212275519750435, 50.50378509014258555 ) ) ;
#26849=ORIENTED_EDGE ( 'NONE', *, *, #37359, .F. ) ;
#26870=CARTESIAN_POINT ( 'NONE',  ( -15.74909385650551386, -8.104110260919579645, 48.81699501597546487 ) ) ;
#26883=VERTEX_POINT ( 'NONE', #42479 ) ;
#26889=CARTESIAN_POINT ( 'NONE',  ( -22.72409385759798894, -9.359200813967568422, 50.49621490985803263 ) ) ;
#26908=AXIS2_PLACEMENT_3D ( 'NONE', #43120, #39425, #46814 ) ;
#26910=CARTESIAN_POINT ( 'NONE',  ( -13.66784385759799036, -9.357632978295827186, 49.97845033065683396 ) ) ;
#26934=CARTESIAN_POINT ( 'NONE',  ( -19.71159385650551599, -6.922745924619793101, 51.69366785382590024 ) ) ;
#26949=CARTESIAN_POINT ( 'NONE',  ( -14.98659385650551457, -9.302874398569244363, 51.68646062012417985 ) ) ;
#26957=CARTESIAN_POINT ( 'NONE',  ( -22.52409385541304232, -9.359200813967568422, 50.49621490985803263 ) ) ;
#26982=PRODUCT_CONTEXT ( 'NONE', #34083, 'mechanical' ) ;
#27004=CARTESIAN_POINT ( 'NONE',  ( -19.93659385541302953, -8.995762431863228770, 51.38120296130586695 ) ) ;
#27017=CARTESIAN_POINT ( 'NONE',  ( -17.12409385650551741, -6.426201560718813433, 50.50509628382439331 ) ) ;
#27020=EDGE_CURVE ( 'NONE', #40074, #35620, #44035, .T. ) ;
#27021=LINE ( 'NONE', #4867, #6436 ) ;
#27031=DIRECTION ( 'NONE',  ( -1.000000000000000000, 4.164305804376849172E-17, -1.614929280266638808E-16 ) ) ;
#27040=CARTESIAN_POINT ( 'NONE',  ( 8.575906144586950219, 1.610468034064642007, 60.52947785690135163 ) ) ;
#27056=CARTESIAN_POINT ( 'NONE',  ( -19.29284385759799036, -8.630756214087126565, 51.74842643355248129 ) ) ;
#27058=CARTESIAN_POINT ( 'NONE',  ( -13.04909385759799001, -8.112991634885936776, 51.74999426922421719 ) ) ;
#27066=ADVANCED_FACE ( 'NONE', ( #6008 ), #5048, .T. ) ;
#27081=DIRECTION ( 'NONE',  ( 0.000000000000000000, 1.000000000000000000, 0.000000000000000000 ) ) ;
#27090=CARTESIAN_POINT ( 'NONE',  ( -17.04284385759799036, -7.587656875400192291, 49.25157356644813689 ) ) ;
#27095=CARTESIAN_POINT ( 'NONE',  ( -16.42409385650551812, -6.426201560718813433, 50.50509628382439331 ) ) ;
#27101=FACE_OUTER_BOUND ( 'NONE', #8303, .T. ) ;
#27112=CARTESIAN_POINT ( 'NONE',  ( -22.55534385759799321, -8.623186033802570094, 49.24843789510466507 ) ) ;
#27126=EDGE_CURVE ( 'NONE', #21655, #10899, #38200, .T. ) ;
#27148=LINE ( 'NONE', #8205, #39101 ) ;
#27157=CARTESIAN_POINT ( 'NONE',  ( -18.13659385541303948, -8.995762431863221664, 51.38120296130585984 ) ) ;
#27170=CARTESIAN_POINT ( 'NONE',  ( -15.43659385650551741, -6.915538690918075382, 49.31353937987644542 ) ) ;
#27192=CARTESIAN_POINT ( 'NONE',  ( -21.39909385541304232, -8.105421454601382081, 49.25000573077640098 ) ) ;
#27217=CARTESIAN_POINT ( 'NONE',  ( 23.52590614458706852, 1.890747609047893185, 50.53028072113869484 ) ) ;
#27250=CARTESIAN_POINT ( 'NONE',  ( -22.44284385650551528, -8.811426318492348031, 52.18089403414751359 ) ) ;
#27256=CARTESIAN_POINT ( 'NONE',  ( -22.72409385650551528, -6.426201560718813433, 50.50509628382439331 ) ) ;
#27299=CARTESIAN_POINT ( 'NONE',  ( 6.575906144586949331, -8.109206544743660316, 50.50000000000031264 ) ) ;
#27301=CARTESIAN_POINT ( 'NONE',  ( -20.33034385650551812, -9.794322478646142471, 51.19202720610083901 ) ) ;
#27328=ORIENTED_EDGE ( 'NONE', *, *, #22179, .T. ) ;
#27331=EDGE_CURVE ( 'NONE', #43020, #47460, #31426, .T. ) ;
#27332=CARTESIAN_POINT ( 'NONE',  ( -16.93034385759798965, -6.857644439848010087, 49.98602051094140108 ) ) ;
#27336=CARTESIAN_POINT ( 'NONE',  ( -15.99909385541290341, -8.105421454601380304, 49.25000573077616650 ) ) ;
#27338=CARTESIAN_POINT ( 'NONE',  ( -19.06784385650551528, -6.428312510596451368, 51.20221977374900035 ) ) ;
#27342=ORIENTED_EDGE ( 'NONE', *, *, #18032, .T. ) ;
#27356=CARTESIAN_POINT ( 'NONE',  ( -22.49909385759799108, -8.105421454601382081, 49.25000573077640098 ) ) ;
#27373=CARTESIAN_POINT ( 'NONE',  ( -22.97409385650551528, -9.792211528768504536, 50.49490371617623197 ) ) ;
#27401=CARTESIAN_POINT ( 'NONE',  ( -17.49284385759798965, -8.630756214087126565, 51.74842643355248129 ) ) ;
#27407=CARTESIAN_POINT ( 'NONE',  ( -17.12409385650551741, -6.426201560718813433, 50.50509628382439331 ) ) ;
#27428=CARTESIAN_POINT ( 'NONE',  ( -23.42409385541304090, -9.359200813967568422, 50.49621490985803263 ) ) ;
#27433=CARTESIAN_POINT ( 'NONE',  ( -23.19909385541303948, -8.105421454601382081, 49.25000573077640098 ) ) ;
#27443=VERTEX_POINT ( 'NONE', #21218 ) ;
#27452=CARTESIAN_POINT ( 'NONE',  ( -19.96784385759798752, -9.357632978295827186, 49.97845033065683396 ) ) ;
#27457=ORIENTED_EDGE ( 'NONE', *, *, #5822, .T. ) ;
#27491=CARTESIAN_POINT ( 'NONE',  ( -20.81159385650551386, -6.922745924619793101, 51.69366785382590024 ) ) ;
#27499=CARTESIAN_POINT ( 'NONE',  ( -13.46784385650551741, -6.428312510596451368, 51.20221977374900035 ) ) ;
#27503=CARTESIAN_POINT ( 'NONE',  ( -23.17409385650551457, -9.792211528768504536, 50.49490371617623197 ) ) ;
#27510=VERTEX_POINT ( 'NONE', #2726 ) ;
#27543=CARTESIAN_POINT ( 'NONE',  ( -22.13034385650552238, -9.794322478646142471, 51.19202720610083901 ) ) ;
#27563=CYLINDRICAL_SURFACE ( 'NONE', #5656, 1.249999999999998668 ) ;
#27564=CARTESIAN_POINT ( 'NONE',  ( -13.74909385541286788, -8.112991634885936776, 51.74999426922452272 ) ) ;
#27569=CARTESIAN_POINT ( 'NONE',  ( 23.52590614458706852, 1.890747609047893185, 50.53028072113869484 ) ) ;
#27571=ORIENTED_EDGE ( 'NONE', *, *, #29940, .T. ) ;
#27583=CARTESIAN_POINT ( 'NONE',  ( -16.98659385650551812, -9.302874398569244363, 51.68646062012417985 ) ) ;
#27591=FACE_OUTER_BOUND ( 'NONE', #24589, .T. ) ;
#27601=CARTESIAN_POINT ( 'NONE',  ( -22.44284385759799250, -7.587656875400192291, 49.25157356644813689 ) ) ;
#27606=ORIENTED_EDGE ( 'NONE', *, *, #26525, .T. ) ;
#27635=VECTOR ( 'NONE', #18708, 1000.000000000000114 ) ;
#27644=AXIS2_PLACEMENT_3D ( 'NONE', #4927, #8366, #34939 ) ;
#27652=CARTESIAN_POINT ( 'NONE',  ( -18.02409385650551599, -6.426201560718813433, 50.50509628382439331 ) ) ;
#27653=AXIS2_PLACEMENT_3D ( 'NONE', #33739, #3720, #29335 ) ;
#27674=DIRECTION ( 'NONE',  ( 0.000000000000000000, -0.9999954153791273948, -0.003028072113819838245 ) ) ;
#27676=DIRECTION ( 'NONE',  ( 4.115385489419834812E-17, 0.9999954153791273948, 0.003028072113822188795 ) ) ;
#27680=CARTESIAN_POINT ( 'NONE',  ( -20.72409385541304161, -9.359200813967568422, 50.49621490985803263 ) ) ;
#27696=B_SPLINE_CURVE_WITH_KNOTS ( 'NONE', 1,
 ( #10841, #28827 ),
 .UNSPECIFIED., .F., .F.,
 ( 2, 2 ),
 ( 0.000000000000000000, 1.000000000000000000 ),
 .UNSPECIFIED. ) ;
#27717=ORIENTED_EDGE ( 'NONE', *, *, #7915, .T. ) ;
#27737=CARTESIAN_POINT ( 'NONE',  ( -22.16159385650551528, -9.295667164867525756, 49.30633214617472504 ) ) ;
#27753=EDGE_CURVE ( 'NONE', #16463, #33928, #32249, .T. ) ;
#27762=ORIENTED_EDGE ( 'NONE', *, *, #29523, .F. ) ;
#27781=CARTESIAN_POINT ( 'NONE',  ( -16.56159385650551386, -9.295667164867525756, 49.30633214617472504 ) ) ;
#27792=CARTESIAN_POINT ( 'NONE',  ( -22.63659385541299685, -8.995762431863267850, 51.38120296130590958 ) ) ;
#27797=DIRECTION ( 'NONE',  ( 2.231660450020913765E-16, 0.9999954153791275058, 0.003028072113822189229 ) ) ;
#27812=EDGE_LOOP ( 'NONE', ( #3222, #14692, #19470, #43602, #25714 ) ) ;
#27820=CARTESIAN_POINT ( 'NONE',  ( -15.94284385541290483, -7.587656875400093703, 49.25157356644789530 ) ) ;
#27822=CARTESIAN_POINT ( 'NONE',  ( -18.05534385650551599, -7.417179338643134834, 52.18511593390279302 ) ) ;
#27840=CARTESIAN_POINT ( 'NONE',  ( -19.06784385759798894, -9.357632978295830739, 49.97845033065684106 ) ) ;
#27844=ORIENTED_EDGE ( 'NONE', *, *, #6275, .F. ) ;
#27892=CARTESIAN_POINT ( 'NONE',  ( -17.77409385759798965, -6.859212275519751323, 50.50378509014259265 ) ) ;
#27893=CARTESIAN_POINT ( 'NONE',  ( -15.32409385650551670, -6.426201560718813433, 50.50509628382439331 ) ) ;
#27913=CARTESIAN_POINT ( 'NONE',  ( -16.70534385759799534, -7.595227055684746986, 51.75156210489594599 ) ) ;
#27917=CARTESIAN_POINT ( 'NONE',  ( -21.68034385541304587, -9.360768649639302552, 51.01397948905921709 ) ) ;
#27925=LINE ( 'NONE', #43203, #19414 ) ;
#27927=ORIENTED_EDGE ( 'NONE', *, *, #2242, .F. ) ;
#27934=CARTESIAN_POINT ( 'NONE',  ( 18.57590614458706924, 1.890747609047612077, 50.53028072113853142 ) ) ;
#27942=CARTESIAN_POINT ( 'NONE',  ( -36.42409385541304800, -9.359200813967566646, 50.49621490985803263 ) ) ;
#27963=EDGE_CURVE ( 'NONE', #19332, #43983, #36764, .T. ) ;
#27965=CARTESIAN_POINT ( 'NONE',  ( -15.07409385759798859, -6.859212275519751323, 50.50378509014259265 ) ) ;
#27969=CARTESIAN_POINT ( 'NONE',  ( -21.09284385650551741, -7.406986770994973490, 48.81910596585309747 ) ) ;
#27974=CARTESIAN_POINT ( 'NONE',  ( -21.31784385650551883, -9.790100578890868377, 49.79778022625163203 ) ) ;
#27982=CARTESIAN_POINT ( 'NONE',  ( -12.82409385759799036, -9.359200813967568422, 50.49621490985803263 ) ) ;
#28018=CARTESIAN_POINT ( 'NONE',  ( -19.71159385650551599, -6.922745924619793101, 51.69366785382590024 ) ) ;
#28020=EDGE_CURVE ( 'NONE', #18062, #20335, #12495, .T. ) ;
#28039=CARTESIAN_POINT ( 'NONE',  ( -13.63659385541286717, -8.995762431863431274, 51.38120296130607301 ) ) ;
#28079=CARTESIAN_POINT ( 'NONE',  ( -20.13659385759799036, -8.995762431863214559, 51.38120296130585274 ) ) ;
#28118=DIRECTION ( 'NONE',  ( 1.000000000000000000, -4.164305804376849172E-17, 1.614929280266638808E-16 ) ) ;
#28136=CARTESIAN_POINT ( 'NONE',  ( -16.95534385650551812, -7.417179338643134834, 52.18511593390279302 ) ) ;
#28163=CARTESIAN_POINT ( 'NONE',  ( -18.41784385541304303, -6.860780111191487229, 51.02154966934377001 ) ) ;
#28178=AXIS2_PLACEMENT_3D ( 'NONE', #23419, #16240, #42378 ) ;
#28219=CARTESIAN_POINT ( 'NONE',  ( -21.26159385650551314, -9.295667164867525756, 49.30633214617472504 ) ) ;
#28224=CARTESIAN_POINT ( 'NONE',  ( -13.29909385650551812, -8.114302828567740988, 52.18300498402516041 ) ) ;
#28226=ORIENTED_EDGE ( 'NONE', *, *, #12473, .T. ) ;
#28247=LINE ( 'NONE', #2132, #47273 ) ;
#28258=VERTEX_POINT ( 'NONE', #44986 ) ;
#28271=CARTESIAN_POINT ( 'NONE',  ( -18.08034385650551812, -6.424090610841176385, 49.80797279389977916 ) ) ;
#28297=CARTESIAN_POINT ( 'NONE',  ( -13.80534385541286113, -7.595227055684621753, 51.75156210489625863 ) ) ;
#28309=CARTESIAN_POINT ( 'NONE',  ( -22.66784385759799392, -9.357632978295830739, 49.97845033065683396 ) ) ;
#28315=CARTESIAN_POINT ( 'NONE',  ( -15.01784385759799179, -6.860780111191481900, 51.02154966934377001 ) ) ;
#28320=CARTESIAN_POINT ( 'NONE',  ( -14.00534385650551705, -8.801233750844183135, 48.81488406609782515 ) ) ;
#28321=ORIENTED_EDGE ( 'NONE', *, *, #34090, .F. ) ;
#28330=DIRECTION ( 'NONE',  ( 0.000000000000000000, 0.9999954153791273948, 0.003028072113819836077 ) ) ;
#28337=CARTESIAN_POINT ( 'NONE',  ( -17.26784385759799179, -9.357632978295830739, 49.97845033065684106 ) ) ;
#28372=CARTESIAN_POINT ( 'NONE',  ( -18.28034385759798752, -9.360768649639306105, 51.01397948905922419 ) ) ;
#28378=CIRCLE ( 'NONE', #7147, 1.900000000000000133 ) ;
#28384=AXIS2_PLACEMENT_3D ( 'NONE', #48380, #8031, #41487 ) ;
#28399=CARTESIAN_POINT ( 'NONE',  ( -22.72409385759798894, -9.359200813967568422, 50.49621490985803263 ) ) ;
#28415=CARTESIAN_POINT ( 'NONE',  ( -18.58659385541304232, -7.222650657624104298, 49.61879703869476543 ) ) ;
#28416=MECHANICAL_DESIGN_GEOMETRIC_PRESENTATION_REPRESENTATION('',(#4064),#29992);
#28435=DIRECTION ( 'NONE',  ( -1.000000000000000000, 4.164305804376849172E-17, -1.614929280266638808E-16 ) ) ;
#28441=LINE ( 'NONE', #24749, #29196 ) ;
#28472=CARTESIAN_POINT ( 'NONE',  ( -19.29284385650551670, -7.406986770994973490, 48.81910596585309747 ) ) ;
#28477=CARTESIAN_POINT ( 'NONE',  ( -17.88659385650551670, -9.302874398569244363, 51.68646062012417985 ) ) ;
#28520=CARTESIAN_POINT ( 'NONE',  ( -17.06784385650551528, -6.428312510596451368, 51.20221977374900035 ) ) ;
#28536=CARTESIAN_POINT ( 'NONE',  ( -21.56784385650551528, -6.428312510596450480, 51.20221977374900035 ) ) ;
#28538=FACE_OUTER_BOUND ( 'NONE', #31955, .T. ) ;
#28550=CARTESIAN_POINT ( 'NONE',  ( 18.57590614458695200, 1.644564126066233145, 49.26952947973238395 ) ) ;
#28558=CARTESIAN_POINT ( 'NONE',  ( -15.13034385650551528, -9.794322478646142471, 51.19202720610083190 ) ) ;
#28576=CARTESIAN_POINT ( 'NONE',  ( -19.46159385759798965, -7.228003583438117552, 51.38655588711986155 ) ) ;
#28579=( BOUNDED_CURVE ( )  B_SPLINE_CURVE ( 2, ( #17360, #2351, #3067, #32402, #40995, #43982, #48368, #32854, #47422 ),
 .UNSPECIFIED., .F., .F. ) 
 B_SPLINE_CURVE_WITH_KNOTS ( ( 3, 2, 2, 2, 3 ),
 ( 0.04166666666666656027, 0.05208333333333329401, 0.06250000000000002776, 0.07291666666666676844, 0.08333333333333348136 ),
 .UNSPECIFIED. ) 
 CURVE ( )  GEOMETRIC_REPRESENTATION_ITEM ( )  RATIONAL_B_SPLINE_CURVE ( ( 1.000000000000000666, 0.9238795325112859613, 1.000000000000000000, 0.9238795325112867385, 1.000000000000000000, 0.9238795325112867385, 1.000000000000000000, 0.9238795325112856283, 1.000000000000001110 ) ) 
 REPRESENTATION_ITEM ( '' )  );
#28608=FACE_OUTER_BOUND ( 'NONE', #29694, .T. ) ;
#28622=CARTESIAN_POINT ( 'NONE',  ( -13.13034385650551883, -9.794322478646142471, 51.19202720610083190 ) ) ;
#28627=DIRECTION ( 'NONE',  ( -4.115385489419834812E-17, -0.9999954153791273948, -0.003028072113822188795 ) ) ;
#28651=CARTESIAN_POINT ( 'NONE',  ( -19.20534385541304090, -7.595227055684746986, 51.75156210489594599 ) ) ;
#28693=DIRECTION ( 'NONE',  ( 1.000000000000000000, -4.164305804376849172E-17, 1.614929280266638808E-16 ) ) ;
#28698=AXIS2_PLACEMENT_3D ( 'NONE', #44891, #37455, #34753 ) ;
#28699=CARTESIAN_POINT ( 'NONE',  ( -17.54909385650551812, -8.104110260919579645, 48.81699501597546487 ) ) ;
#28704=CARTESIAN_POINT ( 'NONE',  ( -17.26784385650551457, -6.428312510596451368, 51.20221977374900035 ) ) ;
#28707=VERTEX_POINT ( 'NONE', #43344 ) ;
#28723=CARTESIAN_POINT ( 'NONE',  ( -16.95534385541304445, -8.623186033802570094, 49.24843789510465797 ) ) ;
#28766=CARTESIAN_POINT ( 'NONE',  ( -20.94909385650551670, -8.104110260919577868, 48.81699501597546487 ) ) ;
#28770=EDGE_CURVE ( 'NONE', #35620, #44349, #28378, .T. ) ;
#28790=CARTESIAN_POINT ( 'NONE',  ( -14.45534385650551989, -7.417179338643134834, 52.18511593390279302 ) ) ;
#28807=VERTEX_POINT ( 'NONE', #2917 ) ;
#28810=CARTESIAN_POINT ( 'NONE',  ( -19.34909385759798894, -8.112991634885936776, 51.74999426922421719 ) ) ;
#28812=DIRECTION ( 'NONE',  ( 1.000000000000000000, 1.669677910507523057E-21, 6.493791346278465266E-22 ) ) ;
#28827=CARTESIAN_POINT ( 'NONE',  ( -23.17409385650551457, -9.792211528768504536, 50.49490371617623197 ) ) ;
#28855=CARTESIAN_POINT ( 'NONE',  ( -13.41159385650551528, -6.922745924619793101, 51.69366785382590024 ) ) ;
#28873=CARTESIAN_POINT ( 'NONE',  ( 9.825906144586950219, -6.109215713985405749, 50.50605614422795497 ) ) ;
#28885=CARTESIAN_POINT ( 'NONE',  ( -17.74284385541304232, -7.587656875400192291, 49.25157356644813689 ) ) ;
#28917=CARTESIAN_POINT ( 'NONE',  ( -21.73659385650551812, -6.915538690918074494, 49.31353937987644542 ) ) ;
#28931=LINE ( 'NONE', #25251, #42097 ) ;
#28936=AXIS2_PLACEMENT_3D ( 'NONE', #4214, #45336, #22939 ) ;
#28939=CARTESIAN_POINT ( 'NONE',  ( -19.57409385650551670, -9.792211528768504536, 50.49490371617623197 ) ) ;
#28943=CARTESIAN_POINT ( 'NONE',  ( -19.85534385650552025, -7.417179338643134834, 52.18511593390279302 ) ) ;
#28986=ORIENTED_EDGE ( 'NONE', *, *, #34795, .T. ) ;
#29005=CARTESIAN_POINT ( 'NONE',  ( -18.24909385650551741, -8.104110260919579645, 48.81699501597546487 ) ) ;
#29017=CARTESIAN_POINT ( 'NONE',  ( 18.82590614458706924, 1.903197776136028807, 48.78032500931639959 ) ) ;
#29018=DIRECTION ( 'NONE',  ( 1.000000000000000000, -4.164305804376849172E-17, 1.614929280266638808E-16 ) ) ;
#29027=CARTESIAN_POINT ( 'NONE',  ( -15.07409385650551670, -9.792211528768504536, 50.49490371617623197 ) ) ;
#29030=DIRECTION ( 'NONE',  ( 0.000000000000000000, 1.000000000000000000, 0.000000000000000000 ) ) ;
#29031=AXIS2_PLACEMENT_3D ( 'NONE', #29301, #44568, #33698 ) ;
#29032=DIRECTION ( 'NONE',  ( -0.9524241471993249997, 0.3047743298226213149, 0.0009228828802126874372 ) ) ;
#29034=EDGE_LOOP ( 'NONE', ( #10284, #3522, #4991, #44318 ) ) ;
#29036=VECTOR ( 'NONE', #39880, 1000.000000000000000 ) ;
#29050=CARTESIAN_POINT ( 'NONE',  ( -16.42409385759798823, -9.359200813967568422, 50.49621490985803263 ) ) ;
#29054=CARTESIAN_POINT ( 'NONE',  ( 10.57590614458695377, -0.1092432217106413528, 50.52422457691089619 ) ) ;
#29066=CIRCLE ( 'NONE', #19662, 1.049999999999998934 ) ;
#29068=DIRECTION ( 'NONE',  ( 0.000000000000000000, -0.9999954153791273948, -0.003028072113819838245 ) ) ;
#29075=LINE ( 'NONE', #7662, #27635 ) ;
#29087=CARTESIAN_POINT ( 'NONE',  ( -22.89284385650552167, -7.406986770994972602, 48.81910596585309747 ) ) ;
#29091=ORIENTED_EDGE ( 'NONE', *, *, #30482, .T. ) ;
#29129=CARTESIAN_POINT ( 'NONE',  ( -19.31784385541304516, -6.860780111191487229, 51.02154966934377001 ) ) ;
#29142=( BOUNDED_CURVE ( )  B_SPLINE_CURVE ( 2, ( #768, #45834, #1007, #46065, #23670, #8891, #12325, #23910, #5191 ),
 .UNSPECIFIED., .F., .F. ) 
 B_SPLINE_CURVE_WITH_KNOTS ( ( 3, 2, 2, 2, 3 ),
 ( 0.06687857201681655928, 0.06786219470523666142, 0.06884581739365676356, 0.06982944008207687958, 0.07081306277049698172 ),
 .UNSPECIFIED. ) 
 CURVE ( )  GEOMETRIC_REPRESENTATION_ITEM ( )  RATIONAL_B_SPLINE_CURVE ( ( 0.9999999999999756861, 0.9238795325113110524, 1.000000000000000000, 0.9238795325112867385, 1.000000000000000000, 0.9238795325112867385, 1.000000000000000000, 0.9238795325112509893, 1.000000000000035749 ) ) 
 REPRESENTATION_ITEM ( '' )  );
#29162=CARTESIAN_POINT ( 'NONE',  ( -22.29909385650551812, -8.114302828567740988, 52.18300498402516041 ) ) ;
#29188=CARTESIAN_POINT ( 'NONE',  ( -17.09909385650551528, -8.114302828567740988, 52.18300498402516041 ) ) ;
#29191=FACE_OUTER_BOUND ( 'NONE', #36889, .T. ) ;
#29193=CARTESIAN_POINT ( 'NONE',  ( -20.36159385650551812, -9.295667164867525756, 49.30633214617472504 ) ) ;
#29196=VECTOR ( 'NONE', #21042, 1000.000000000000000 ) ;
#29209=CARTESIAN_POINT ( 'NONE',  ( 23.62590614458706639, -0.009252390952106800612, 50.53028072113869484 ) ) ;
#29211=CARTESIAN_POINT ( 'NONE',  ( -16.67409385541329669, -6.859212275519744217, 50.50378509014024075 ) ) ;
#29242=CARTESIAN_POINT ( 'NONE',  ( -12.82409385759799036, -9.359200813967568422, 50.49621490985803263 ) ) ;
#29255=CARTESIAN_POINT ( 'NONE',  ( -19.48659385650551457, -9.302874398569244363, 51.68646062012417985 ) ) ;
#29268=EDGE_LOOP ( 'NONE', ( #7025, #734 ) ) ;
#29293=CARTESIAN_POINT ( 'NONE',  ( -16.48034385759799036, -9.360768649639302552, 51.01397948905922419 ) ) ;
#29301=CARTESIAN_POINT ( 'NONE',  ( 0.000000000000000000, 0.000000000000000000, 0.000000000000000000 ) ) ;
#29335=DIRECTION ( 'NONE',  ( 0.000000000000000000, 1.000000000000000000, 0.000000000000000000 ) ) ;
#29347=DIRECTION ( 'NONE',  ( 1.000000000000000000, -4.164305804376849172E-17, 1.614929280266638808E-16 ) ) ;
#29361=CARTESIAN_POINT ( 'NONE',  ( -12.82409385759799036, -9.359200813967568422, 50.49621490985803263 ) ) ;
#29366=CARTESIAN_POINT ( 'NONE',  ( -21.62409385541304374, -9.359200813967568422, 50.49621490985803263 ) ) ;
#29372=CARTESIAN_POINT ( 'NONE',  ( -15.71784385541304552, -6.860780111191487229, 51.02154966934377711 ) ) ;
#29377=CARTESIAN_POINT ( 'NONE',  ( 10.57590614458695377, 0.6407533398237006406, 50.52649563099625851 ) ) ;
#29393=ORIENTED_EDGE ( 'NONE', *, *, #38286, .F. ) ;
#29418=CARTESIAN_POINT ( 'NONE',  ( -17.79909385650551812, -8.114302828567740988, 52.18300498402516041 ) ) ;
#29424=CARTESIAN_POINT ( 'NONE',  ( -19.91159385650551528, -6.922745924619793101, 51.69366785382590024 ) ) ;
#29429=CARTESIAN_POINT ( 'NONE',  ( -19.23659385650551457, -6.915538690918075382, 49.31353937987644542 ) ) ;
#29444=CARTESIAN_POINT ( 'NONE',  ( -17.34909385541293858, -8.112991634885936776, 51.74999426922440193 ) ) ;
#29446=VERTEX_POINT ( 'NONE', #46438 ) ;
#29468=VERTEX_POINT ( 'NONE', #46188 ) ;
#29491=CARTESIAN_POINT ( 'NONE',  ( -17.79909385650551812, -8.114302828567740988, 52.18300498402516041 ) ) ;
#29509=PRODUCT_DEFINITION_SHAPE ( 'NONE', 'NONE',  #16217 ) ;
#29515=VERTEX_POINT ( 'NONE', #39762 ) ;
#29523=EDGE_CURVE ( 'NONE', #28707, #10899, #3050, .T. ) ;
#29532=CARTESIAN_POINT ( 'NONE',  ( -15.13034385759799250, -6.857644439848013640, 49.98602051094139398 ) ) ;
#29547=SURFACE_SIDE_STYLE ('',( #44345 ) ) ;
#29569=CARTESIAN_POINT ( 'NONE',  ( -21.99284385650551243, -7.406986770994972602, 48.81910596585309747 ) ) ;
#29607=CARTESIAN_POINT ( 'NONE',  ( -20.53034385759798752, -6.857644439848019857, 49.98602051094138687 ) ) ;
#29608=CARTESIAN_POINT ( 'NONE',  ( -21.39909385541298548, -8.105421454601382081, 49.25000573077630150 ) ) ;
#29614=CARTESIAN_POINT ( 'NONE',  ( -15.99909385541304196, -8.105421454601382081, 49.25000573077640098 ) ) ;
#29639=VERTEX_POINT ( 'NONE', #3543 ) ;
#29643=VECTOR ( 'NONE', #17495, 1000.000000000000000 ) ;
#29659=EDGE_LOOP ( 'NONE', ( #5313, #24153, #38174 ) ) ;
#29661=CARTESIAN_POINT ( 'NONE',  ( -16.39284385650552167, -7.406986770994973490, 48.81910596585309747 ) ) ;
#29670=CARTESIAN_POINT ( 'NONE',  ( -16.48034385650551670, -6.424090610841176385, 49.80797279389977916 ) ) ;
#29672=DIRECTION ( 'NONE',  ( 1.000000000000000000, -4.164305804376849788E-17, 1.614929280266638808E-16 ) ) ;
#29673=CARTESIAN_POINT ( 'NONE',  ( -14.00534385650551883, -8.801233750844183135, 48.81488406609782515 ) ) ;
#29689=ORIENTED_EDGE ( 'NONE', *, *, #681, .T. ) ;
#29694=EDGE_LOOP ( 'NONE', ( #34796, #28321, #38820 ) ) ;
#29697=DIRECTION ( 'NONE',  ( 0.000000000000000000, -0.9999954153791273948, -0.003028072113819838245 ) ) ;
#29716=EDGE_CURVE ( 'NONE', #43417, #9318, #37505, .T. ) ;
#29729=ORIENTED_EDGE ( 'NONE', *, *, #3036, .T. ) ;
#29741=CARTESIAN_POINT ( 'NONE',  ( -20.38659385650551670, -9.302874398569244363, 51.68646062012417985 ) ) ;
#29774=VERTEX_POINT ( 'NONE', #8716 ) ;
#29785=CARTESIAN_POINT ( 'NONE',  ( -16.19909385759799036, -8.105421454601382081, 49.25000573077640098 ) ) ;
#29818=AXIS2_PLACEMENT_3D ( 'NONE', #21504, #36486, #2288 ) ;
#29820=VERTEX_POINT ( 'NONE', #15836 ) ;
#29826=CARTESIAN_POINT ( 'NONE',  ( -22.66784385650551670, -6.428312510596451368, 51.20221977374900035 ) ) ;
#29837=DIRECTION ( 'NONE',  ( 1.000000000000000000, -4.164305804376849788E-17, 1.614929280266638808E-16 ) ) ;
#29854=DIRECTION ( 'NONE',  ( 4.115385489419834196E-17, 0.9999954153791273948, 0.003028072113822188795 ) ) ;
#29863=ORIENTED_EDGE ( 'NONE', *, *, #37081, .T. ) ;
#29865=CARTESIAN_POINT ( 'NONE',  ( -14.36784385541304232, -9.357632978295830739, 49.97845033065684106 ) ) ;
#29877=CARTESIAN_POINT ( 'NONE',  ( 18.57590614458706924, 2.136931092028983681, 51.79103196254472863 ) ) ;
#29888=VERTEX_POINT ( 'NONE', #32332 ) ;
#29901=CARTESIAN_POINT ( 'NONE',  ( -20.38659385650551670, -9.302874398569244363, 51.68646062012417985 ) ) ;
#29905=EDGE_LOOP ( 'NONE', ( #46418, #27844 ) ) ;
#29914=CARTESIAN_POINT ( 'NONE',  ( -13.29909385650551812, -8.114302828567740988, 52.18300498402516041 ) ) ;
#29921=CARTESIAN_POINT ( 'NONE',  ( -14.45534385650551989, -7.417179338643134834, 52.18511593390279302 ) ) ;
#29926=CARTESIAN_POINT ( 'NONE',  ( -14.51159385650551492, -6.922745924619793101, 51.69366785382590024 ) ) ;
#29935=EDGE_CURVE ( 'NONE', #17825, #20557, #15847, .T. ) ;
#29936=ORIENTED_EDGE ( 'NONE', *, *, #43597, .F. ) ;
#29940=EDGE_CURVE ( 'NONE', #27443, #9159, #22152, .T. ) ;
#29990=CARTESIAN_POINT ( 'NONE',  ( -17.40534385650551741, -8.801233750844183135, 48.81488406609782515 ) ) ;
#29992=( GEOMETRIC_REPRESENTATION_CONTEXT ( 3 ) GLOBAL_UNCERTAINTY_ASSIGNED_CONTEXT ( ( #31709 ) ) GLOBAL_UNIT_ASSIGNED_CONTEXT ( ( #26344, #44574, #7894 ) ) REPRESENTATION_CONTEXT ( 'NONE', 'WORKASPACE' ) );
#30003=EDGE_CURVE ( 'NONE', #32441, #19332, #21915, .T. ) ;
#30005=CARTESIAN_POINT ( 'NONE',  ( -22.72409385759798894, -9.359200813967568422, 50.49621490985803263 ) ) ;
#30042=CARTESIAN_POINT ( 'NONE',  ( -14.90534385759799463, -7.595227055684746986, 51.75156210489594599 ) ) ;
#30057=SURFACE_STYLE_USAGE ( .BOTH. , #29547 ) ;
#30067=CARTESIAN_POINT ( 'NONE',  ( 18.57590614458695200, 1.636933384339416264, 51.78951792648778252 ) ) ;
#30068=LINE ( 'NONE', #33719, #33583 ) ;
#30078=EDGE_CURVE ( 'NONE', #13279, #32426, #2493, .T. ) ;
#30079=CARTESIAN_POINT ( 'NONE',  ( -20.08034385650551812, -6.424090610841176385, 49.80797279389978627 ) ) ;
#30105=CARTESIAN_POINT ( 'NONE',  ( 7.325906144586951996, -6.109215713985405749, 50.50605614422795497 ) ) ;
#30112=CARTESIAN_POINT ( 'NONE',  ( -20.75534385759799250, -8.623186033802570094, 49.24843789510466507 ) ) ;
#30118=CARTESIAN_POINT ( 'NONE',  ( -14.53659385541304339, -8.995762431863214559, 51.38120296130585274 ) ) ;
#30120=CARTESIAN_POINT ( 'NONE',  ( -15.74909385759799108, -8.112991634885936776, 51.74999426922421719 ) ) ;
#30151=CARTESIAN_POINT ( 'NONE',  ( -19.93659385650551741, -6.915538690918074494, 49.31353937987644542 ) ) ;
#30154=CARTESIAN_POINT ( 'NONE',  ( -21.37409385759799108, -6.859212275519751323, 50.50378509014259265 ) ) ;
#30168=CARTESIAN_POINT ( 'NONE',  ( -14.14284385650552167, -8.811426318492348031, 52.18089403414752070 ) ) ;
#30175=ORIENTED_EDGE ( 'NONE', *, *, #1683, .T. ) ;
#30177=CARTESIAN_POINT ( 'NONE',  ( -15.52409385650551421, -6.426201560718813433, 50.50509628382439331 ) ) ;
#30181=CARTESIAN_POINT ( 'NONE',  ( -16.76159385650551314, -9.295667164867525756, 49.30633214617472504 ) ) ;
#30202=ORIENTED_EDGE ( 'NONE', *, *, #17839, .F. ) ;
#30242=LINE ( 'NONE', #45261, #25245 ) ;
#30244=CARTESIAN_POINT ( 'NONE',  ( -14.48034385650551847, -6.424090610841176385, 49.80797279389977916 ) ) ;
#30284=CARTESIAN_POINT ( 'NONE',  ( -21.90534385650552096, -8.801233750844183135, 48.81488406609782515 ) ) ;
#30308=EDGE_LOOP ( 'NONE', ( #22953, #42728, #44766, #9201, #43725 ) ) ;
#30320=ORIENTED_EDGE ( 'NONE', *, *, #47944, .T. ) ;
#30325=PLANE ( 'NONE',  #28936 ) ;
#30326=CARTESIAN_POINT ( 'NONE',  ( -21.03659385650551528, -6.915538690918074494, 49.31353937987644542 ) ) ;
#30364=CARTESIAN_POINT ( 'NONE',  ( -23.14284385541300182, -7.587656875400161205, 49.25157356644805873 ) ) ;
#30367=ADVANCED_FACE ( 'NONE', ( #41724 ), #11204, .T. ) ;
#30375=CARTESIAN_POINT ( 'NONE',  ( -18.78659385759798894, -7.222650657624104298, 49.61879703869476543 ) ) ;
#30393=CARTESIAN_POINT ( 'NONE',  ( -19.99284385650551599, -7.406986770994972602, 48.81910596585309747 ) ) ;
#30396=CARTESIAN_POINT ( 'NONE',  ( -21.14909385759798965, -8.112991634885936776, 51.74999426922421719 ) ) ;
#30399=CARTESIAN_POINT ( 'NONE',  ( -21.54284385759798681, -7.587656875400192291, 49.25157356644813689 ) ) ;
#30410=CARTESIAN_POINT ( 'NONE',  ( -13.41159385650551528, -6.922745924619793101, 51.69366785382590024 ) ) ;
#30413=FACE_OUTER_BOUND ( 'NONE', #33180, .T. ) ;
#30416=VERTEX_POINT ( 'NONE', #4070 ) ;
#30418=CARTESIAN_POINT ( 'NONE',  ( -13.22466815457524447, -9.790356681133982164, 49.88235584379216192 ) ) ;
#30423=CARTESIAN_POINT ( 'NONE',  ( -14.34284385650551563, -8.811426318492348031, 52.18089403414752070 ) ) ;
#30430=ADVANCED_FACE ( 'NONE', ( #30413 ), #19837, .T. ) ;
#30433=AXIS2_PLACEMENT_3D ( 'NONE', #24180, #46597, #20233 ) ;
#30434=CIRCLE ( 'NONE', #46166, 0.2499999999999976408 ) ;
#30454=ORIENTED_EDGE ( 'NONE', *, *, #19366, .T. ) ;
#30464=CARTESIAN_POINT ( 'NONE',  ( -13.17364477763805652, -9.395196358873663556, 49.41429196092195042 ) ) ;
#30482=EDGE_CURVE ( 'NONE', #17825, #21318, #23990, .T. ) ;
#30488=CARTESIAN_POINT ( 'NONE',  ( -14.36784385650551954, -6.428312510596451368, 51.20221977374900035 ) ) ;
#30527=CARTESIAN_POINT ( 'NONE',  ( 18.87590614458706995, 1.890747609047893185, 50.53028072113869484 ) ) ;
#30528=CARTESIAN_POINT ( 'NONE',  ( 18.07590614458695200, 2.144077342217588722, 49.43104278224995340 ) ) ;
#30529=CARTESIAN_POINT ( 'NONE',  ( -13.38659385759799214, -7.222650657624104298, 49.61879703869476543 ) ) ;
#30532=CYLINDRICAL_SURFACE ( 'NONE', #18447, 1.249999999999998668 ) ;
#30554=DIRECTION ( 'NONE',  ( 1.616182858256158472E-16, 0.003028072113829171491, -0.9999954153791273948 ) ) ;
#30567=CARTESIAN_POINT ( 'NONE',  ( -21.88034385650551883, -6.424090610841176385, 49.80797279389978627 ) ) ;
#30572=ORIENTED_EDGE ( 'NONE', *, *, #21274, .T. ) ;
#30588=FACE_OUTER_BOUND ( 'NONE', #12457, .T. ) ;
#30592=FACE_OUTER_BOUND ( 'NONE', #38250, .T. ) ;
#30593=DIRECTION ( 'NONE',  ( 4.115385489419892128E-17, 0.9999954153791273948, 0.003028072113818697231 ) ) ;
#30630=CYLINDRICAL_SURFACE ( 'NONE', #44968, 1.249999999999998668 ) ;
#30632=CARTESIAN_POINT ( 'NONE',  ( -17.38034385759799250, -9.360768649639311434, 51.01397948905922419 ) ) ;
#30638=CARTESIAN_POINT ( 'NONE',  ( -19.76784385650551457, -6.428312510596451368, 51.20221977374900035 ) ) ;
#30651=AXIS2_PLACEMENT_3D ( 'NONE', #16509, #9637, #9141 ) ;
#30652=CIRCLE ( 'NONE', #46348, 1.049999999999998934 ) ;
#30657=CARTESIAN_POINT ( 'NONE',  ( -14.93034385650551599, -9.794322478646142471, 51.19202720610083901 ) ) ;
#30665=CARTESIAN_POINT ( 'NONE',  ( -22.63659385541304303, -8.995762431863214559, 51.38120296130585274 ) ) ;
#30672=ADVANCED_FACE ( 'NONE', ( #14791 ), #45020, .T. ) ;
#30701=EDGE_CURVE ( 'NONE', #2071, #28807, #5591, .T. ) ;
#30707=CARTESIAN_POINT ( 'NONE',  ( -12.97364571557156232, -9.395203622806569399, 49.41430056510258595 ) ) ;
#30728=CARTESIAN_POINT ( 'NONE',  ( -14.31159385650551741, -6.922745924619793101, 51.69366785382590024 ) ) ;
#30743=DIRECTION ( 'NONE',  ( -1.616182858256118783E-16, -0.003028072113822189229, 0.9999954153791275058 ) ) ;
#30756=AXIS2_PLACEMENT_3D ( 'NONE', #6543, #40035, #44231 ) ;
#30770=DIRECTION ( 'NONE',  ( 0.000000000000000000, -0.9999954153791273948, -0.003028072113819838245 ) ) ;
#30772=CARTESIAN_POINT ( 'NONE',  ( -22.52409385650551954, -6.426201560718812544, 50.50509628382439331 ) ) ;
#30804=CARTESIAN_POINT ( 'NONE',  ( 18.46573386768564973, 3.116243883476752963, 50.28399048308536123 ) ) ;
#30808=FACE_OUTER_BOUND ( 'NONE', #39828, .T. ) ;
#30809=CARTESIAN_POINT ( 'NONE',  ( -17.54909385650551812, -8.104110260919579645, 48.81699501597546487 ) ) ;
#30817=CARTESIAN_POINT ( 'NONE',  ( -16.33659385541304232, -8.995762431863216335, 51.38120296130585274 ) ) ;
#30831=CARTESIAN_POINT ( 'NONE',  ( -20.86784385759799321, -9.357632978295830739, 49.97845033065684106 ) ) ;
#30835=DIRECTION ( 'NONE',  ( 0.000000000000000000, -0.9999954153791273948, -0.003028072113819836944 ) ) ;
#30853=AXIS2_PLACEMENT_3D ( 'NONE', #40992, #19309, #7274 ) ;
#30859=ORIENTED_EDGE ( 'NONE', *, *, #45036, .T. ) ;
#30877=FACE_OUTER_BOUND ( 'NONE', #19208, .T. ) ;
#30878=CARTESIAN_POINT ( 'NONE',  ( -18.41784385650552736, -9.790100578890868377, 49.79778022625163203 ) ) ;
#30880=ADVANCED_FACE ( 'NONE', ( #35473 ), #2229, .F. ) ;
#30896=CARTESIAN_POINT ( 'NONE',  ( -16.59284385759799108, -8.630756214087126565, 51.74842643355248129 ) ) ;
#30901=CARTESIAN_POINT ( 'NONE',  ( -22.86159385541304090, -7.228003583438117552, 51.38655588711986155 ) ) ;
#30913=CARTESIAN_POINT ( 'NONE',  ( 18.87590614458706995, 1.878653161019418816, 52.23023769833749697 ) ) ;
#30929=CYLINDRICAL_SURFACE ( 'NONE', #678, 1.249999999999998668 ) ;
#30937=ORIENTED_EDGE ( 'NONE', *, *, #39967, .F. ) ;
#30956=CARTESIAN_POINT ( 'NONE',  ( -21.54284385650551670, -8.811426318492348031, 52.18089403414751359 ) ) ;
#30962=CARTESIAN_POINT ( 'NONE',  ( -15.66159385650551705, -9.295667164867525756, 49.30633214617472504 ) ) ;
#30994=DIRECTION ( 'NONE',  ( -1.000000000000000000, 4.164305804376849172E-17, -1.614929280266638808E-16 ) ) ;
#31000=CARTESIAN_POINT ( 'NONE',  ( -21.23034385650552025, -9.794322478646142471, 51.19202720610083901 ) ) ;
#31032=ORIENTED_EDGE ( 'NONE', *, *, #15801, .T. ) ;
#31042=CARTESIAN_POINT ( 'NONE',  ( -18.44909385650551670, -8.104110260919579645, 48.81699501597546487 ) ) ;
#31048=CARTESIAN_POINT ( 'NONE',  ( -16.22409385541304871, -9.359200813967568422, 50.49621490985801842 ) ) ;
#31063=CARTESIAN_POINT ( 'NONE',  ( 10.57590614458695377, 1.890747609047612521, 50.53028072113853142 ) ) ;
#31106=CARTESIAN_POINT ( 'NONE',  ( -14.53659385650551705, -6.915538690918075382, 49.31353937987644542 ) ) ;
#31124=CARTESIAN_POINT ( 'NONE',  ( -16.64909385759798965, -8.112991634885936776, 51.74999426922421719 ) ) ;
#31127=CARTESIAN_POINT ( 'NONE',  ( -20.49909385541304374, -8.105421454601382081, 49.25000573077640098 ) ) ;
#31145=CARTESIAN_POINT ( 'NONE',  ( -19.68659385759799108, -7.222650657624104298, 49.61879703869476543 ) ) ;
#31180=CARTESIAN_POINT ( 'NONE',  ( -36.42409385541304800, -9.359200813967566646, 50.49621490985803263 ) ) ;
#31185=ORIENTED_EDGE ( 'NONE', *, *, #18456, .T. ) ;
#31187=CARTESIAN_POINT ( 'NONE',  ( -21.14909385650551599, -8.104110260919577868, 48.81699501597546487 ) ) ;
#31193=CARTESIAN_POINT ( 'NONE',  ( -22.27409385650551243, -9.792211528768504536, 50.49490371617623197 ) ) ;
#31195=AXIS2_PLACEMENT_3D ( 'NONE', #26106, #14992, #45082 ) ;
#31229=EDGE_CURVE ( 'NONE', #4206, #13279, #37023, .T. ) ;
#31238=CARTESIAN_POINT ( 'NONE',  ( -20.16159385650551883, -9.295667164867525756, 49.30633214617472504 ) ) ;
#31248=CARTESIAN_POINT ( 'NONE',  ( 18.82590614458706924, 1.878297441959757785, 52.28023643296099010 ) ) ;
#31251=CARTESIAN_POINT ( 'NONE',  ( -14.17409385759798823, -6.859212275519751323, 50.50378509014259265 ) ) ;
#31254=CARTESIAN_POINT ( 'NONE',  ( -13.86159385541286326, -7.228003583437902613, 51.38655588712008182 ) ) ;
#31267=ORIENTED_EDGE ( 'NONE', *, *, #24895, .T. ) ;
#31274=CARTESIAN_POINT ( 'NONE',  ( -16.25534385650551528, -7.417179338643134834, 52.18511593390279302 ) ) ;
#31311=VERTEX_POINT ( 'NONE', #22344 ) ;
#31315=ORIENTED_EDGE ( 'NONE', *, *, #4122, .T. ) ;
#31343=CARTESIAN_POINT ( 'NONE',  ( -16.89909385650551599, -8.114302828567740988, 52.18300498402516041 ) ) ;
#31358=EDGE_CURVE ( 'NONE', #7797, #33382, #22111, .T. ) ;
#31368=AXIS2_PLACEMENT_3D ( 'NONE', #42630, #2208, #20199 ) ;
#31372=CARTESIAN_POINT ( 'NONE',  ( -22.58034385541304445, -9.360768649639302552, 51.01397948905921709 ) ) ;
#31384=DIRECTION ( 'NONE',  ( -1.000000000000000000, 4.164305804376849172E-17, -1.614929280266638808E-16 ) ) ;
#31407=VECTOR ( 'NONE', #29347, 1000.000000000000000 ) ;
#31424=CARTESIAN_POINT ( 'NONE',  ( -20.64284385650552167, -8.811426318492348031, 52.18089403414751359 ) ) ;
#31426=CIRCLE ( 'NONE', #16468, 1.949999999999999956 ) ;
#31429=CARTESIAN_POINT ( 'NONE',  ( -13.35534385650551492, -7.417179338643134834, 52.18511593390279302 ) ) ;
#31479=CARTESIAN_POINT ( 'NONE',  ( -17.51784385650551812, -9.790100578890868377, 49.79778022625163203 ) ) ;
#31489=CARTESIAN_POINT ( 'NONE',  ( -22.97409385541299542, -6.859212275519753099, 50.50378509014307582 ) ) ;
#31500=CARTESIAN_POINT ( 'NONE',  ( -13.97409385541301496, -6.859212275519754876, 50.50378509014287687 ) ) ;
#31502=AXIS2_PLACEMENT_3D ( 'NONE', #7831, #37584, #15415 ) ;
#31508=EDGE_CURVE ( 'NONE', #29774, #24601, #30242, .T. ) ;
#31522=CARTESIAN_POINT ( 'NONE',  ( -16.93034385650551954, -9.794322478646142471, 51.19202720610083190 ) ) ;
#31536=CARTESIAN_POINT ( 'NONE',  ( -36.42409385541304800, -7.059211358595575803, 50.50317947571981847 ) ) ;
#31569=ORIENTED_EDGE ( 'NONE', *, *, #21942, .T. ) ;
#31576=DIRECTION ( 'NONE',  ( 0.000000000000000000, -0.9999954153791273948, -0.003028072113819838245 ) ) ;
#31589=CARTESIAN_POINT ( 'NONE',  ( -36.42409385541304800, -6.859212275519750435, 50.50378509014258555 ) ) ;
#31594=CARTESIAN_POINT ( 'NONE',  ( -17.46159385650551599, -9.295667164867525756, 49.30633214617472504 ) ) ;
#31625=CARTESIAN_POINT ( 'NONE',  ( -23.31159385541304019, -8.990409506049200417, 49.61344411288074951 ) ) ;
#31675=CARTESIAN_POINT ( 'NONE',  ( -23.17409385650551457, -9.792211528768504536, 50.49490371617623197 ) ) ;
#31679=CARTESIAN_POINT ( 'NONE',  ( -21.43034385650551954, -9.794322478646142471, 51.19202720610083901 ) ) ;
#31680=EDGE_CURVE ( 'NONE', #31825, #29639, #40943, .T. ) ;
#31688=ADVANCED_FACE ( 'NONE', ( #25981 ), #36786, .T. ) ;
#31709=UNCERTAINTY_MEASURE_WITH_UNIT (LENGTH_MEASURE( 1.000000000000000082E-05 ), #26344, 'distance_accuracy_value', 'NONE');
#31719=ADVANCED_FACE ( 'NONE', ( #29191 ), #44232, .T. ) ;
#31721=ORIENTED_EDGE ( 'NONE', *, *, #35044, .F. ) ;
#31726=CARTESIAN_POINT ( 'NONE',  ( -18.36159385650551812, -9.295667164867525756, 49.30633214617472504 ) ) ;
#31754=CARTESIAN_POINT ( 'NONE',  ( -22.33034385759799179, -6.857644439848018969, 49.98602051094138687 ) ) ;
#31763=CARTESIAN_POINT ( 'NONE',  ( -17.43659385650551741, -6.915538690918075382, 49.31353937987644542 ) ) ;
#31764=ORIENTED_EDGE ( 'NONE', *, *, #35914, .F. ) ;
#31782=CARTESIAN_POINT ( 'NONE',  ( -17.71784385759799108, -6.860780111191487229, 51.02154966934377001 ) ) ;
#31807=EDGE_LOOP ( 'NONE', ( #30202, #47679 ) ) ;
#31825=VERTEX_POINT ( 'NONE', #4310 ) ;
#31826=LINE ( 'NONE', #39936, #40395 ) ;
#31831=CARTESIAN_POINT ( 'NONE',  ( -18.16784385759799036, -9.357632978295827186, 49.97845033065683396 ) ) ;
#31832=CARTESIAN_POINT ( 'NONE',  ( -17.01159385650551670, -6.922745924619793101, 51.69366785382590024 ) ) ;
#31839=DIRECTION ( 'NONE',  ( -1.616182858256118783E-16, -0.003028072113822189229, 0.9999954153791275058 ) ) ;
#31854=CARTESIAN_POINT ( 'NONE',  ( -16.42409385759798823, -9.359200813967568422, 50.49621490985803263 ) ) ;
#31858=CARTESIAN_POINT ( 'NONE',  ( -17.18034385541304232, -9.360768649639302552, 51.01397948905922419 ) ) ;
#31872=CARTESIAN_POINT ( 'NONE',  ( -15.77409385541301035, -6.859212275519753099, 50.50378509014291240 ) ) ;
#31909=CARTESIAN_POINT ( 'NONE',  ( -15.24284385759798965, -7.587656875400192291, 49.25157356644813689 ) ) ;
#31919=CARTESIAN_POINT ( 'NONE',  ( -13.02466687598806239, -9.790356633151166221, 49.88233999786937289 ) ) ;
#31938=ORIENTED_EDGE ( 'NONE', *, *, #698, .F. ) ;
#31955=EDGE_LOOP ( 'NONE', ( #38742, #41609, #29729, #19133 ) ) ;
#31960=CARTESIAN_POINT ( 'NONE',  ( -18.75534385650551528, -7.417179338643134834, 52.18511593390279302 ) ) ;
#31965=VECTOR ( 'NONE', #4150, 1000.000000000000000 ) ;
#31977=DIRECTION ( 'NONE',  ( -2.231660450020913765E-16, -0.9999954153791275058, -0.003028072113822189229 ) ) ;
#31997=AXIS2_PLACEMENT_3D ( 'NONE', #27299, #42326, #46512 ) ;
#32003=CARTESIAN_POINT ( 'NONE',  ( -15.35534385650552203, -7.417179338643134834, 52.18511593390279302 ) ) ;
#32022=CARTESIAN_POINT ( 'NONE',  ( -17.43659385759799108, -8.995762431863214559, 51.38120296130585274 ) ) ;
#32035=ORIENTED_EDGE ( 'NONE', *, *, #48520, .T. ) ;
#32048=BREP_WITH_VOIDS ( 'NONE', #40135, ( #3125 ) );
#32054=ORIENTED_EDGE ( 'NONE', *, *, #27753, .T. ) ;
#32059=FACE_OUTER_BOUND ( 'NONE', #46686, .T. ) ;
#32072=LINE ( 'NONE', #31589, #15557 ) ;
#32102=CARTESIAN_POINT ( 'NONE',  ( -16.50534385541304161, -7.595227055684746986, 51.75156210489594599 ) ) ;
#32114=CIRCLE ( 'NONE', #21078, 0.2499999999999976408 ) ;
#32125=DIRECTION ( 'NONE',  ( 0.000000000000000000, 1.000000000000000000, 0.000000000000000000 ) ) ;
#32133=CARTESIAN_POINT ( 'NONE',  ( 18.54465614458695200, 0.6407533398237036382, 50.52649563099625851 ) ) ;
#32134=LINE ( 'NONE', #27942, #16034 ) ;
#32162=CARTESIAN_POINT ( 'NONE',  ( -18.22409385650551528, -6.426201560718813433, 50.50509628382439331 ) ) ;
#32167=CARTESIAN_POINT ( 'NONE',  ( -18.89909385650551599, -8.114302828567740988, 52.18300498402516041 ) ) ;
#32171=AXIS2_PLACEMENT_3D ( 'NONE', #1946, #16945, #43569 ) ;
#32200=ADVANCED_FACE ( 'NONE', ( #13960 ), #43564, .F. ) ;
#32212=CARTESIAN_POINT ( 'NONE',  ( -17.18034385650552309, -6.424090610841176385, 49.80797279389977916 ) ) ;
#32229=CARTESIAN_POINT ( 'NONE',  ( -21.28659385650551528, -9.302874398569244363, 51.68646062012417985 ) ) ;
#32249=LINE ( 'NONE', #28550, #44832 ) ;
#32253=CARTESIAN_POINT ( 'NONE',  ( -15.07409385759798859, -6.859212275519751323, 50.50378509014259265 ) ) ;
#32257=CARTESIAN_POINT ( 'NONE',  ( -13.38659385650551847, -9.302874398569244363, 51.68646062012417985 ) ) ;
#32275=CARTESIAN_POINT ( 'NONE',  ( -19.79909385759798823, -8.105421454601382081, 49.25000573077640098 ) ) ;
#32280=EDGE_CURVE ( 'NONE', #12981, #34525, #45216, .T. ) ;
#32298=VERTEX_POINT ( 'NONE', #48444 ) ;
#32308=DIRECTION ( 'NONE',  ( 1.000000000000000000, 1.669677910507523057E-21, 6.493791346278465266E-22 ) ) ;
#32332=CARTESIAN_POINT ( 'NONE',  ( 18.62590614458706995, 3.140741878271803067, 50.53406581128081143 ) ) ;
#32348=CIRCLE ( 'NONE', #11094, 0.7500000000000023315 ) ;
#32356=CARTESIAN_POINT ( 'NONE',  ( -16.33659385541304232, -8.995762431863214559, 51.38120296130585274 ) ) ;
#32363=EDGE_CURVE ( 'NONE', #17990, #48035, #7594, .T. ) ;
#32371=ORIENTED_EDGE ( 'NONE', *, *, #21942, .F. ) ;
#32396=ORIENTED_EDGE ( 'NONE', *, *, #17601, .T. ) ;
#32402=CARTESIAN_POINT ( 'NONE',  ( -22.10534385759799392, -7.595227055684746986, 51.75156210489594599 ) ) ;
#32407=CARTESIAN_POINT ( 'NONE',  ( -17.77409385650551243, -9.792211528768504536, 50.49490371617623197 ) ) ;
#32410=CARTESIAN_POINT ( 'NONE',  ( -17.71784385650551741, -9.790100578890868377, 49.79778022625163203 ) ) ;
#32426=VERTEX_POINT ( 'NONE', #23579 ) ;
#32436=DIRECTION ( 'NONE',  ( 0.000000000000000000, 0.9999954153791273948, 0.003028072113820366902 ) ) ;
#32437=ORIENTED_EDGE ( 'NONE', *, *, #43145, .T. ) ;
#32441=VERTEX_POINT ( 'NONE', #27503 ) ;
#32450=CARTESIAN_POINT ( 'NONE',  ( -17.34909385650551883, -8.104110260919579645, 48.81699501597546487 ) ) ;
#32467=CARTESIAN_POINT ( 'NONE',  ( -19.93659385650551741, -6.915538690918074494, 49.31353937987644542 ) ) ;
#32468=( BOUNDED_CURVE ( )  B_SPLINE_CURVE ( 2, ( #3496, #10655, #33269, #36970, #17107, #31909, #46926, #36070, #27965 ),
 .UNSPECIFIED., .F., .F. ) 
 B_SPLINE_CURVE_WITH_KNOTS ( ( 3, 2, 2, 2, 3 ),
 ( 0.6666666666666665186, 0.6770833333333332593, 0.6874999999999998890, 0.6979166666666665186, 0.7083333333333332593 ),
 .UNSPECIFIED. ) 
 CURVE ( )  GEOMETRIC_REPRESENTATION_ITEM ( )  RATIONAL_B_SPLINE_CURVE ( ( 1.000000000000000888, 0.9238795325112859613, 1.000000000000000000, 0.9238795325112867385, 1.000000000000000000, 0.9238795325112867385, 1.000000000000000000, 0.9238795325112875156, 0.9999999999999992228 ) ) 
 REPRESENTATION_ITEM ( '' )  );
#32480=ORIENTED_EDGE ( 'NONE', *, *, #2274, .F. ) ;
#32486=CARTESIAN_POINT ( 'NONE',  ( -14.73659385650551457, -6.915538690918075382, 49.31353937987644542 ) ) ;
#32499=ORIENTED_EDGE ( 'NONE', *, *, #4638, .T. ) ;
#32505=CARTESIAN_POINT ( 'NONE',  ( -18.95534385759798823, -8.623186033802570094, 49.24843789510466507 ) ) ;
#32507=CARTESIAN_POINT ( 'NONE',  ( 23.52590614458706852, 1.890747609047893185, 50.53028072113869484 ) ) ;
#32512=EDGE_CURVE ( 'NONE', #24436, #1563, #27021, .T. ) ;
#32529=LINE ( 'NONE', #47554, #11116 ) ;
#32551=CARTESIAN_POINT ( 'NONE',  ( -14.31159385650551741, -6.922745924619793101, 51.69366785382590024 ) ) ;
#32554=CARTESIAN_POINT ( 'NONE',  ( 8.575906144586951996, -8.108449526715205025, 50.25000114615553315 ) ) ;
#32559=CARTESIAN_POINT ( 'NONE',  ( -22.97409385650551528, -9.792211528768504536, 50.49490371617623197 ) ) ;
#32567=AXIS2_PLACEMENT_3D ( 'NONE', #21550, #37261, #40485 ) ;
#32579=CARTESIAN_POINT ( 'NONE',  ( -19.71159385541304232, -8.990409506049200417, 49.61344411288074951 ) ) ;
#32634=CARTESIAN_POINT ( 'NONE',  ( -17.43659385650551741, -6.915538690918075382, 49.31353937987644542 ) ) ;
#32637=CARTESIAN_POINT ( 'NONE',  ( 10.57590614458695377, 1.890747609047612521, 50.53028072113853142 ) ) ;
#32638=CARTESIAN_POINT ( 'NONE',  ( -17.21159385650551599, -6.922745924619793101, 51.69366785382590024 ) ) ;
#32678=EDGE_LOOP ( 'NONE', ( #97, #27457, #6941, #29936, #5644, #44660, #13995, #47019 ) ) ;
#32693=CARTESIAN_POINT ( 'NONE',  ( -18.81159385650551741, -6.922745924619793101, 51.69366785382590024 ) ) ;
#32700=ORIENTED_EDGE ( 'NONE', *, *, #47944, .F. ) ;
#32719=( BOUNDED_SURFACE ( )  B_SPLINE_SURFACE ( 1, 2, ( 
 ( #31675, #45970, #42764, #39299, #5093, #9268, #12230, #4602, #34631, #5585, #16144, #43251, #20102, #27250, #46696, #38566, #8541, #24295, #12466, #23815, #8797, #20598, #12715, #914, #46930, #24052, #23318, #4854, #1872, #30956, #19873, #12943, #13172, #34870, #28219, #9034, #31187, #27969, #1376, #46209, #38311, #35596, #27491, #39047, #38815, #31424, #42994, #5335, #20350, #46461, #35359, #16641, #16872, #6045, #35830, #47656, #14128, #9760, #29424, #39780, #24545, #2113, #47900, #10482, #28939, #13896, #17365, #39541, #43736, #28472, #17112, #9988, #21075, #40275, #9520, #10242, #36315, #36782, #13424, #36543, #36074, #21565, #2828, #25011, #2354, #2602, #40034, #40501, #32162, #5821, #47177, #43496, #43985, #6296, #24779, #47426, #32407, #17600, #13656, #17834, #28699, #21327, #32634, #20833, #25257, #6541, #21788, #32859, #29188, #44230, #6777, #25484, #3071, #18078, #33090, #48139, #14370, #26465, #136, #29670, #41729, #37275, #4307, #15118, #26714, #48372, #7026, #18832, #7771, #3563, #45435, #10960, #44957, #45197, #11689, #18568, #30177, #7522, #3818, #37780, #33576, #44705, #4076, #25978, #10711, #8020, #11437, #22525, #23032, #38017, #41478, #19072, #19314, #34320, #15606, #29921, #25726, #604, #7280, #41234, #22281, #22043, #22786, #37520, #48624, #37037, #3321, #14606, #18324, #33838, #44456, #14858, #40744, #34082, #33332, #372, #15357, #30418, #41000, #11211, #26222 ),
 ( #1318, #42216, #31625, #12173, #27433, #12892, #38510, #45683, #16329, #1572, #30901, #12656, #8737, #11940, #30665, #31372, #26957, #8480, #41977, #38252, #8248, #38997, #23266, #19561, #5525, #5277, #4534, #35055, #46646, #20545, #34570, #27917, #15854, #854, #16580, #45916, #27192, #35545, #20047, #23510, #4791, #42941, #42466, #8975, #1088, #19818, #23764, #38756, #27680, #34816, #1819, #16088, #31127, #9215, #46150, #42713, #12409, #5037, #24238, #46400, #23996, #20292, #35299, #39246, #35777, #9939, #32579, #40221, #2301, #32810, #13119, #39729, #24955, #29129, #2552, #28651, #44180, #10430, #13842, #25203, #25439, #40448, #36725, #17307, #46879, #6723, #28415, #13605, #43439, #28163, #17551, #43683, #24726, #9462, #43192, #20777, #24486, #39974, #14078, #5995, #16818, #28885, #39491, #6248, #36494, #21269, #2058, #47610, #17058, #36265, #21739, #31858, #43928, #10188, #6490, #21512, #9709, #17785, #47123, #2775, #47840, #21020, #5770, #32102, #13367, #36017, #32356, #47375, #33041, #3013, #3756, #18024, #29614, #48085, #10660, #14321, #11384, #29372, #40685, #26653, #26407, #25669, #7470, #19019, #41671, #44404, #4011, #36978, #6965, #37720, #21984, #33276, #7959, #41182, #18271, #3268, #34025, #14796, #30118, #22228, #48316, #29865, #11150, #71, #14549, #22974, #37219, #44643, #15297, #10900, #15060, #40936, #25924, #315, #3503, #45142, #18515, #33520, #7222, #48566, #44899 ) ),
 .UNSPECIFIED., .F., .F., .F. ) 
 B_SPLINE_SURFACE_WITH_KNOTS ( ( 2, 2 ),
 ( 3, 2, 2, 2, 2, 2, 2, 2, 2, 2, 2, 2, 2, 2, 2, 2, 2, 2, 2, 2, 2, 2, 2, 2, 2, 2, 2, 2, 2, 2, 2, 2, 2, 2, 2, 2, 2, 2, 2, 2, 2, 2, 2, 2, 2, 2, 2, 2, 2, 2, 2, 2, 2, 2, 2, 2, 2, 2, 2, 2, 2, 2, 2, 2, 2, 2, 2, 2, 2, 2, 2, 2, 2, 2, 2, 2, 2, 2, 2, 2, 2, 2, 2, 2, 2, 2, 2, 2, 2, 2, 3 ),
 ( 0.000000000000000000, 1.000000000000000000 ),
 ( 0.000000000000000000, 0.01041666666666666609, 0.02083333333333333218, 0.03125000000000000000, 0.04166666666666666435, 0.05208333333333333565, 0.06250000000000000000, 0.07291666666666667129, 0.08333333333333332871, 0.09375000000000000000, 0.1041666666666666713, 0.1145833333333333287, 0.1250000000000000000, 0.1354166666666666574, 0.1458333333333333426, 0.1562500000000000000, 0.1666666666666666574, 0.1770833333333333426, 0.1875000000000000000, 0.1979166666666666574, 0.2083333333333333426, 0.2187500000000000000, 0.2291666666666666574, 0.2395833333333333426, 0.2500000000000000000, 0.2604166666666666852, 0.2708333333333333148, 0.2812500000000000000, 0.2916666666666666852, 0.3020833333333333148, 0.3125000000000000000, 0.3229166666666666852, 0.3333333333333333148, 0.3437500000000000000, 0.3541666666666666852, 0.3645833333333333148, 0.3750000000000000000, 0.3854166666666666852, 0.3958333333333333148, 0.4062500000000000000, 0.4166666666666666852, 0.4270833333333333148, 0.4375000000000000000, 0.4479166666666666852, 0.4583333333333333148, 0.4687500000000000000, 0.4791666666666666852, 0.4895833333333333148, 0.5000000000000000000, 0.5104166666666666297, 0.5208333333333333703, 0.5312500000000000000, 0.5416666666666666297, 0.5520833333333333703, 0.5625000000000000000, 0.5729166666666666297, 0.5833333333333333703, 0.5937500000000000000, 0.6041666666666666297, 0.6145833333333333703, 0.6250000000000000000, 0.6354166666666666297, 0.6458333333333333703, 0.6562500000000000000, 0.6666666666666666297, 0.6770833333333333703, 0.6875000000000000000, 0.6979166666666666297, 0.7083333333333333703, 0.7187500000000000000, 0.7291666666666666297, 0.7395833333333333703, 0.7500000000000000000, 0.7604166666666666297, 0.7708333333333333703, 0.7812500000000000000, 0.7916666666666666297, 0.8020833333333333703, 0.8125000000000000000, 0.8229166666666666297, 0.8333333333333333703, 0.8437500000000000000, 0.8541666666666666297, 0.8645833333333333703, 0.8750000000000000000, 0.8854166666666666297, 0.8958333333333333703, 0.9062500000000000000, 0.9166666666666666297, 0.9259048894201962199, 0.9351639383143981465 ),
 .UNSPECIFIED. ) 
 GEOMETRIC_REPRESENTATION_ITEM ( )  RATIONAL_B_SPLINE_SURFACE ( (
 ( 1.000000000000000000, 0.9238795325112867385, 1.000000000000000000, 0.9238795325112867385, 1.000000000000000000, 0.9238795325112867385, 1.000000000000000000, 0.9238795325112867385, 1.000000000000000000, 0.9238795325112867385, 1.000000000000000000, 0.9238795325112867385, 1.000000000000000000, 0.9238795325112867385, 1.000000000000000000, 0.9238795325112867385, 1.000000000000000000, 0.9238795325112867385, 1.000000000000000000, 0.9238795325112867385, 1.000000000000000000, 0.9238795325112867385, 1.000000000000000000, 0.9238795325112867385, 1.000000000000000000, 0.9238795325112867385, 1.000000000000000000, 0.9238795325112867385, 1.000000000000000000, 0.9238795325112867385, 1.000000000000000000, 0.9238795325112867385, 1.000000000000000000, 0.9238795325112867385, 1.000000000000000000, 0.9238795325112867385, 1.000000000000000000, 0.9238795325112867385, 1.000000000000000000, 0.9238795325112867385, 1.000000000000000000, 0.9238795325112867385, 1.000000000000000000, 0.9238795325112867385, 1.000000000000000000, 0.9238795325112867385, 1.000000000000000000, 0.9238795325112867385, 1.000000000000000000, 0.9238795325112867385, 1.000000000000000000, 0.9238795325112867385, 1.000000000000000000, 0.9238795325112867385, 1.000000000000000000, 0.9238795325112867385, 1.000000000000000000, 0.9238795325112867385, 1.000000000000000000, 0.9238795325112867385, 1.000000000000000000, 0.9238795325112867385, 1.000000000000000000, 0.9238795325112867385, 1.000000000000000000, 0.9238795325112867385, 1.000000000000000000, 0.9238795325112867385, 1.000000000000000000, 0.9238795325112867385, 1.000000000000000000, 0.9238795325112867385, 1.000000000000000000, 0.9238795325112867385, 1.000000000000000000, 0.9238795325112867385, 1.000000000000000000, 0.9238795325112867385, 1.000000000000000000, 0.9238795325112867385, 1.000000000000000000, 0.9238795325112867385, 1.000000000000000000, 0.9238795325112867385, 1.000000000000000000, 0.9238795325112867385, 1.000000000000000000, 0.9238795325112867385, 1.000000000000000000, 0.9238795325112867385, 1.000000000000000000, 0.9238795325112867385, 1.000000000000000000, 0.9238795325112867385, 1.000000000000000000, 0.9238795325112867385, 1.000000000000000000, 0.9238795325112867385, 1.000000000000000000, 0.9238795325112867385, 1.000000000000000000, 0.9238795325112867385, 1.000000000000000000, 0.9238795325112867385, 1.000000000000000000, 0.9238795325112867385, 1.000000000000000000, 0.9238795325112867385, 1.000000000000000000, 0.9238795325112867385, 1.000000000000000000, 0.9238795325112867385, 1.000000000000000000, 0.9238795325112867385, 1.000000000000000000, 0.9238795325112867385, 1.000000000000000000, 0.9238795325112867385, 1.000000000000000000, 0.9238795325112867385, 1.000000000000000000, 0.9238795325112867385, 1.000000000000000000, 0.9238795325112867385, 1.000000000000000000, 0.9238795325112867385, 1.000000000000000000, 0.9238795325112867385, 1.000000000000000000, 0.9238795325112867385, 1.000000000000000000, 0.9238795325112867385, 1.000000000000000000, 0.9238795325112867385, 1.000000000000000000, 0.9238795325112867385, 1.000000000000000000, 0.9238795325112867385, 1.000000000000000000, 0.9238795325112867385, 1.000000000000000000, 0.9238795325112867385, 1.000000000000000000, 0.9238795325112867385, 1.000000000000000000, 0.9238795325112867385, 1.000000000000000000, 0.9238795325112867385, 1.000000000000000000, 0.9238795325112867385, 1.000000000000000000, 0.9238795325112867385, 1.000000000000000000, 0.9238795325112867385, 1.000000000000000000, 0.9238795325112867385, 1.000000000000000000, 0.9238795325112867385, 1.000000000000000000, 0.9238795325112867385, 1.000000000000000000, 0.9238795325112867385, 1.000000000000000000, 0.9238795325112867385, 1.000000000000000000, 0.9238795325112867385, 1.000000000000000000, 0.9238795325112867385, 1.000000000000000000, 0.9238795325112867385, 1.000000000000000000, 0.9238795325112867385, 1.000000000000000000, 0.9238795325112867385, 1.000000000000000000, 0.9238795325112867385, 1.000000000000000000, 0.9324910878627006294, 0.9847253504145836445, 0.9847253504145836445, 0.9847253504145836445),
 ( 1.000000000000000000, 0.9238795325112867385, 1.000000000000000000, 0.9238795325112867385, 1.000000000000000000, 0.9238795325112867385, 1.000000000000000000, 0.9238795325112867385, 1.000000000000000000, 0.9238795325112867385, 1.000000000000000000, 0.9238795325112867385, 1.000000000000000000, 0.9238795325112867385, 1.000000000000000000, 0.9238795325112867385, 1.000000000000000000, 0.9238795325112867385, 1.000000000000000000, 0.9238795325112867385, 1.000000000000000000, 0.9238795325112867385, 1.000000000000000000, 0.9238795325112867385, 1.000000000000000000, 0.9238795325112867385, 1.000000000000000000, 0.9238795325112867385, 1.000000000000000000, 0.9238795325112867385, 1.000000000000000000, 0.9238795325112867385, 1.000000000000000000, 0.9238795325112867385, 1.000000000000000000, 0.9238795325112867385, 1.000000000000000000, 0.9238795325112867385, 1.000000000000000000, 0.9238795325112867385, 1.000000000000000000, 0.9238795325112867385, 1.000000000000000000, 0.9238795325112867385, 1.000000000000000000, 0.9238795325112867385, 1.000000000000000000, 0.9238795325112867385, 1.000000000000000000, 0.9238795325112867385, 1.000000000000000000, 0.9238795325112867385, 1.000000000000000000, 0.9238795325112867385, 1.000000000000000000, 0.9238795325112867385, 1.000000000000000000, 0.9238795325112867385, 1.000000000000000000, 0.9238795325112867385, 1.000000000000000000, 0.9238795325112867385, 1.000000000000000000, 0.9238795325112867385, 1.000000000000000000, 0.9238795325112867385, 1.000000000000000000, 0.9238795325112867385, 1.000000000000000000, 0.9238795325112867385, 1.000000000000000000, 0.9238795325112867385, 1.000000000000000000, 0.9238795325112867385, 1.000000000000000000, 0.9238795325112867385, 1.000000000000000000, 0.9238795325112867385, 1.000000000000000000, 0.9238795325112867385, 1.000000000000000000, 0.9238795325112867385, 1.000000000000000000, 0.9238795325112867385, 1.000000000000000000, 0.9238795325112867385, 1.000000000000000000, 0.9238795325112867385, 1.000000000000000000, 0.9238795325112867385, 1.000000000000000000, 0.9238795325112867385, 1.000000000000000000, 0.9238795325112867385, 1.000000000000000000, 0.9238795325112867385, 1.000000000000000000, 0.9238795325112867385, 1.000000000000000000, 0.9238795325112867385, 1.000000000000000000, 0.9238795325112867385, 1.000000000000000000, 0.9238795325112867385, 1.000000000000000000, 0.9238795325112867385, 1.000000000000000000, 0.9238795325112867385, 1.000000000000000000, 0.9238795325112867385, 1.000000000000000000, 0.9238795325112867385, 1.000000000000000000, 0.9238795325112867385, 1.000000000000000000, 0.9238795325112867385, 1.000000000000000000, 0.9238795325112867385, 1.000000000000000000, 0.9238795325112867385, 1.000000000000000000, 0.9238795325112867385, 1.000000000000000000, 0.9238795325112867385, 1.000000000000000000, 0.9238795325112867385, 1.000000000000000000, 0.9238795325112867385, 1.000000000000000000, 0.9238795325112867385, 1.000000000000000000, 0.9238795325112867385, 1.000000000000000000, 0.9238795325112867385, 1.000000000000000000, 0.9238795325112867385, 1.000000000000000000, 0.9238795325112867385, 1.000000000000000000, 0.9238795325112867385, 1.000000000000000000, 0.9238795325112867385, 1.000000000000000000, 0.9238795325112867385, 1.000000000000000000, 0.9238795325112867385, 1.000000000000000000, 0.9238795325112867385, 1.000000000000000000, 0.9238795325112867385, 1.000000000000000000, 0.9238795325112867385, 1.000000000000000000, 0.9238795325112867385, 1.000000000000000000, 0.9238795325112867385, 1.000000000000000000, 0.9238795325112867385, 1.000000000000000000, 0.9238795325112867385, 1.000000000000000000, 0.9238795325112867385, 1.000000000000000000, 0.9238795325112867385, 1.000000000000000000, 0.9238795325112867385, 1.000000000000000000, 0.9238795325112867385, 1.000000000000000000, 0.9238795325112867385, 1.000000000000000000, 0.9238795325112867385, 1.000000000000000000, 0.9238795325112867385, 1.000000000000000000, 0.9238795325112867385, 1.000000000000000000, 0.9324910878627006294, 0.9847253504145836445, 0.9847253504145836445, 0.9847253504145836445) ) ) 
 REPRESENTATION_ITEM ( '' )  SURFACE ( )  );
#32731=ORIENTED_EDGE ( 'NONE', *, *, #40384, .T. ) ;
#32736=CARTESIAN_POINT ( 'NONE',  ( -20.08034385759798823, -9.360768649639302552, 51.01397948905922419 ) ) ;
#32759=LINE ( 'NONE', #30067, #8668 ) ;
#32772=CARTESIAN_POINT ( 'NONE',  ( -22.94909385650551314, -8.104110260919577868, 48.81699501597546487 ) ) ;
#32810=CARTESIAN_POINT ( 'NONE',  ( -19.54284385541304303, -7.587656875400192291, 49.25157356644813689 ) ) ;
#32815=CARTESIAN_POINT ( 'NONE',  ( -20.19284385759799605, -8.630756214087126565, 51.74842643355248129 ) ) ;
#32820=ORIENTED_EDGE ( 'NONE', *, *, #48332, .T. ) ;
#32822=CARTESIAN_POINT ( 'NONE',  ( -20.38659385541303237, -7.222650657624089199, 49.61879703869475833 ) ) ;
#32829=ADVANCED_FACE ( 'NONE', ( #38025 ), #14363, .F. ) ;
#32842=CARTESIAN_POINT ( 'NONE',  ( -36.42409385541304800, -6.859212275519750435, 50.50378509014258555 ) ) ;
#32847=ORIENTED_EDGE ( 'NONE', *, *, #8453, .T. ) ;
#32854=CARTESIAN_POINT ( 'NONE',  ( -21.88034385759798539, -9.360768649639309658, 51.01397948905920998 ) ) ;
#32855=AXIS2_PLACEMENT_3D ( 'NONE', #36561, #39802, #2375 ) ;
#32857=ORIENTED_EDGE ( 'NONE', *, *, #35044, .T. ) ;
#32859=CARTESIAN_POINT ( 'NONE',  ( -17.15534385650551741, -7.417179338643134834, 52.18511593390279302 ) ) ;
#32865=CARTESIAN_POINT ( 'NONE',  ( -19.68659385650551386, -9.302874398569244363, 51.68646062012417985 ) ) ;
#32873=ORIENTED_EDGE ( 'NONE', *, *, #9276, .F. ) ;
#32880=CARTESIAN_POINT ( 'NONE',  ( -16.73034385541296132, -6.857644439847485174, 49.98602051094192689 ) ) ;
#32924=CARTESIAN_POINT ( 'NONE',  ( -20.55534385650551599, -7.417179338643134834, 52.18511593390279302 ) ) ;
#32934=CARTESIAN_POINT ( 'NONE',  ( 18.62590614458706995, 1.890747609047893185, 50.53028072113869484 ) ) ;
#32961=CARTESIAN_POINT ( 'NONE',  ( -13.55534385759799143, -8.623186033802571870, 49.24843789510467218 ) ) ;
#32963=FACE_OUTER_BOUND ( 'NONE', #30308, .T. ) ;
#32975=ORIENTED_EDGE ( 'NONE', *, *, #30078, .T. ) ;
#32991=ORIENTED_EDGE ( 'NONE', *, *, #5805, .F. ) ;
#32998=CARTESIAN_POINT ( 'NONE',  ( -36.42409385541304800, -6.859212275519750435, 50.50378509014258555 ) ) ;
#33019=CARTESIAN_POINT ( 'NONE',  ( -13.27409385650551599, -9.792211528768504536, 50.49490371617623197 ) ) ;
#33021=AXIS2_PLACEMENT_3D ( 'NONE', #40404, #24680, #24912 ) ;
#33041=CARTESIAN_POINT ( 'NONE',  ( -16.22409385541304516, -9.359200813967568422, 50.49621490985803263 ) ) ;
#33061=ORIENTED_EDGE ( 'NONE', *, *, #22500, .T. ) ;
#33090=CARTESIAN_POINT ( 'NONE',  ( -16.76159385650551314, -9.295667164867525756, 49.30633214617472504 ) ) ;
#33097=CARTESIAN_POINT ( 'NONE',  ( -18.78659385650551528, -9.302874398569244363, 51.68646062012417985 ) ) ;
#33108=ORIENTED_EDGE ( 'NONE', *, *, #38974, .F. ) ;
#33114=CARTESIAN_POINT ( 'NONE',  ( -17.23659385541294142, -8.995762431863342456, 51.38120296130598064 ) ) ;
#33116=VECTOR ( 'NONE', #2338, 1000.000000000000000 ) ;
#33130=CARTESIAN_POINT ( 'NONE',  ( 10.57590614458695377, 1.644457370994424572, 49.30478444670939808 ) ) ;
#33136=( BOUNDED_CURVE ( )  B_SPLINE_CURVE ( 2, ( #3880, #8073, #33900, #33388, #15408, #4130, #428, #41540, #18886 ),
 .UNSPECIFIED., .F., .F. ) 
 B_SPLINE_CURVE_WITH_KNOTS ( ( 3, 2, 2, 2, 3 ),
 ( 0.03540611873294381706, 0.03638973639061496290, 0.03737335404828610874, 0.03835697170595725458, 0.03934058936362840042 ),
 .UNSPECIFIED. ) 
 CURVE ( )  GEOMETRIC_REPRESENTATION_ITEM ( )  RATIONAL_B_SPLINE_CURVE ( ( 0.9999999999999245048, 0.9238795325113622336, 1.000000000000000000, 0.9238795325112867385, 1.000000000000000000, 0.9238795325112867385, 1.000000000000000000, 0.9238795325113857704, 0.9999999999999009681 ) ) 
 REPRESENTATION_ITEM ( '' )  );
#33157=AXIS2_PLACEMENT_3D ( 'NONE', #39610, #21148, #44058 ) ;
#33163=CARTESIAN_POINT ( 'NONE',  ( -19.82409385650551670, -6.426201560718813433, 50.50509628382439331 ) ) ;
#33166=EDGE_CURVE ( 'NONE', #4941, #29515, #43991, .T. ) ;
#33168=CARTESIAN_POINT ( 'NONE',  ( -12.95698253826988022, -9.064354784168759949, 49.69365525927820215 ) ) ;
#33173=ORIENTED_EDGE ( 'NONE', *, *, #38286, .T. ) ;
#33175=CARTESIAN_POINT ( 'NONE',  ( -36.42409385541304800, -9.359200813967566646, 50.49621490985803263 ) ) ;
#33180=EDGE_LOOP ( 'NONE', ( #36897, #46093, #40159, #9839 ) ) ;
#33202=CARTESIAN_POINT ( 'NONE',  ( -16.98659385759799179, -7.222650657624104298, 49.61879703869476543 ) ) ;
#33238=CARTESIAN_POINT ( 'NONE',  ( -20.64284385650552522, -8.811426318492348031, 52.18089403414751359 ) ) ;
#33241=CARTESIAN_POINT ( 'NONE',  ( -14.00534385759799427, -7.595227055684746986, 51.75156210489594599 ) ) ;
#33269=CARTESIAN_POINT ( 'NONE',  ( -15.41159385759799072, -8.990409506049202193, 49.61344411288074951 ) ) ;
#33270=CARTESIAN_POINT ( 'NONE',  ( -20.69909385759799036, -8.105421454601382081, 49.25000573077640098 ) ) ;
#33276=CARTESIAN_POINT ( 'NONE',  ( -14.93034385541304232, -6.857644439848013640, 49.98602051094139398 ) ) ;
#33278=CARTESIAN_POINT ( 'NONE',  ( -15.86159385759799001, -7.228003583438117552, 51.38655588711986155 ) ) ;
#33282=CARTESIAN_POINT ( 'NONE',  ( -15.97409385759799072, -6.859212275519751323, 50.50378509014259265 ) ) ;
#33293=LINE ( 'NONE', #94, #41698 ) ;
#33307=CARTESIAN_POINT ( 'NONE',  ( -21.90534385650552096, -8.801233750844183135, 48.81488406609782515 ) ) ;
#33325=CARTESIAN_POINT ( 'NONE',  ( -15.43659385650551741, -6.915538690918075382, 49.31353937987644542 ) ) ;
#33332=CARTESIAN_POINT ( 'NONE',  ( -13.38659385650551847, -9.302874398569244363, 51.68646062012417985 ) ) ;
#33336=CARTESIAN_POINT ( 'NONE',  ( -16.42409385650551812, -6.426201560718813433, 50.50509628382439331 ) ) ;
#33337=VECTOR ( 'NONE', #40378, 1000.000000000000000 ) ;
#33353=CARTESIAN_POINT ( 'NONE',  ( -22.72409385759798894, -9.359200813967568422, 50.49621490985803263 ) ) ;
#33382=VERTEX_POINT ( 'NONE', #43702 ) ;
#33388=CARTESIAN_POINT ( 'NONE',  ( -19.20534385541296629, -7.595227055684692807, 51.75156210489608810 ) ) ;
#33390=CARTESIAN_POINT ( 'NONE',  ( -13.04909385759799001, -8.112991634885936776, 51.74999426922421719 ) ) ;
#33400=CARTESIAN_POINT ( 'NONE',  ( -17.57409385650551314, -9.792211528768504536, 50.49490371617623197 ) ) ;
#33440=EDGE_CURVE ( 'NONE', #23343, #21318, #23063, .T. ) ;
#33441=CARTESIAN_POINT ( 'NONE',  ( -16.64909385759798965, -8.112991634885936776, 51.74999426922421719 ) ) ;
#33455=EDGE_CURVE ( 'NONE', #16463, #33382, #1821, .T. ) ;
#33479=CARTESIAN_POINT ( 'NONE',  ( -21.31784385650551883, -9.790100578890868377, 49.79778022625163203 ) ) ;
#33482=DIRECTION ( 'NONE',  ( -0.9524241471993249997, 0.3047743298226213149, 0.0009228828802126874372 ) ) ;
#33499=CARTESIAN_POINT ( 'NONE',  ( -13.44284385650551705, -8.811426318492348031, 52.18089403414752070 ) ) ;
#33513=FACE_OUTER_BOUND ( 'NONE', #19261, .T. ) ;
#33520=CARTESIAN_POINT ( 'NONE',  ( -13.47466815348276903, -9.357823189459354651, 50.04126597187313763 ) ) ;
#33527=CARTESIAN_POINT ( 'NONE',  ( -20.08034385759798468, -9.360768649639306105, 51.01397948905921709 ) ) ;
#33542=DIRECTION ( 'NONE',  ( 1.000000000000000000, -4.164305804376849172E-17, 1.614929280266638808E-16 ) ) ;
#33553=CARTESIAN_POINT ( 'NONE',  ( -20.16159385650551883, -9.295667164867525756, 49.30633214617472504 ) ) ;
#33568=CARTESIAN_POINT ( 'NONE',  ( -15.88659385650551670, -9.302874398569244363, 51.68646062012417985 ) ) ;
#33576=CARTESIAN_POINT ( 'NONE',  ( -15.29909385650551634, -8.114302828567740988, 52.18300498402516041 ) ) ;
#33581=CARTESIAN_POINT ( 'NONE',  ( -15.86159385650551634, -9.295667164867525756, 49.30633214617472504 ) ) ;
#33583=VECTOR ( 'NONE', #41623, 1000.000000000000000 ) ;
#33614=CARTESIAN_POINT ( 'NONE',  ( 18.87590614458706995, 1.902842057076367777, 48.83032374393989272 ) ) ;
#33637=CARTESIAN_POINT ( 'NONE',  ( -12.93659385759799285, -8.995762431863214559, 51.38120296130585274 ) ) ;
#33647=CARTESIAN_POINT ( 'NONE',  ( -17.46159385650551599, -9.295667164867525756, 49.30633214617472504 ) ) ;
#33654=VECTOR ( 'NONE', #2219, 1000.000000000000000 ) ;
#33658=VECTOR ( 'NONE', #41266, 1000.000000000000000 ) ;
#33686=CARTESIAN_POINT ( 'NONE',  ( -14.23034385759799036, -6.857644439848014528, 49.98602051094139398 ) ) ;
#33695=CARTESIAN_POINT ( 'NONE',  ( -23.17409385650551457, -9.792211528768504536, 50.49490371617623197 ) ) ;
#33698=DIRECTION ( 'NONE',  ( 1.000000000000000000, 0.000000000000000000, 0.000000000000000000 ) ) ;
#33711=ORIENTED_EDGE ( 'NONE', *, *, #39967, .T. ) ;
#33719=CARTESIAN_POINT ( 'NONE',  ( -36.42409385541304800, -9.359200813967566646, 50.49621490985803263 ) ) ;
#33732=LINE ( 'NONE', #29, #47486 ) ;
#33734=CARTESIAN_POINT ( 'NONE',  ( -19.68659385650551386, -9.302874398569244363, 51.68646062012417985 ) ) ;
#33739=CARTESIAN_POINT ( 'NONE',  ( 22.62590614458706639, 1.890747609047612077, 50.53028072113853142 ) ) ;
#33742=CARTESIAN_POINT ( 'NONE',  ( -22.41159385541302385, -8.990409506049225286, 49.61344411288072820 ) ) ;
#33758=CARTESIAN_POINT ( 'NONE',  ( -22.97409385541299542, -6.859212275519753099, 50.50378509014307582 ) ) ;
#33764=DIRECTION ( 'NONE',  ( 1.616182858256118783E-16, 0.003028072113822189229, -0.9999954153791275058 ) ) ;
#33797=ORIENTED_EDGE ( 'NONE', *, *, #21964, .T. ) ;
#33800=ADVANCED_FACE ( 'NONE', ( #24194, #46837 ), #13564, .T. ) ;
#33814=CARTESIAN_POINT ( 'NONE',  ( -19.48659385650551457, -9.302874398569244363, 51.68646062012417985 ) ) ;
#33829=CARTESIAN_POINT ( 'NONE',  ( -15.54909385650551634, -8.104110260919579645, 48.81699501597546487 ) ) ;
#33831=CARTESIAN_POINT ( 'NONE',  ( 23.52590614458706852, 3.890747609047893185, 50.53028072113869484 ) ) ;
#33838=CARTESIAN_POINT ( 'NONE',  ( -13.66784385650551670, -6.428312510596451368, 51.20221977374900035 ) ) ;
#33843=CARTESIAN_POINT ( 'NONE',  ( -15.13034385650551528, -9.794322478646142471, 51.19202720610083901 ) ) ;
#33851=DIRECTION ( 'NONE',  ( 0.000000000000000000, -0.007114381193220190198, 0.9999746924698832418 ) ) ;
#33900=CARTESIAN_POINT ( 'NONE',  ( -19.26159385541296487, -7.228003583438021629, 51.38655588711996103 ) ) ;
#33913=CARTESIAN_POINT ( 'NONE',  ( -17.01159385650551670, -6.922745924619793101, 51.69366785382590024 ) ) ;
#33915=AXIS2_PLACEMENT_3D ( 'NONE', #44960, #25487, #26224 ) ;
#33928=VERTEX_POINT ( 'NONE', #37174 ) ;
#33953=CARTESIAN_POINT ( 'NONE',  ( -22.80534385650551599, -8.801233750844183135, 48.81488406609782515 ) ) ;
#33957=CARTESIAN_POINT ( 'NONE',  ( -14.56784385759798894, -9.357632978295830739, 49.97845033065683396 ) ) ;
#33983=VERTEX_POINT ( 'NONE', #41376 ) ;
#33986=CARTESIAN_POINT ( 'NONE',  ( -20.47409385650551528, -9.792211528768504536, 50.49490371617623197 ) ) ;
#33992=CARTESIAN_POINT ( 'NONE',  ( -22.24284385541302456, -7.587656875400178080, 49.25157356644810136 ) ) ;
#34013=CARTESIAN_POINT ( 'NONE',  ( 10.57590614458695377, -0.1092432217106413528, 50.52422457691089619 ) ) ;
#34019=CARTESIAN_POINT ( 'NONE',  ( -21.56784385541339688, -9.357632978298600079, 49.97845033065944875 ) ) ;
#34025=CARTESIAN_POINT ( 'NONE',  ( -14.64909385541304410, -8.112991634885936776, 51.74999426922421719 ) ) ;
#34027=CARTESIAN_POINT ( 'NONE',  ( -23.25534385541299898, -8.623186033802600292, 49.24843789510458691 ) ) ;
#34053=DIRECTION ( 'NONE',  ( 0.000000000000000000, 0.007114381193220285608, -0.9999746924698833528 ) ) ;
#34057=CARTESIAN_POINT ( 'NONE',  ( -21.56784385650551883, -6.428312510596449592, 51.20221977374900035 ) ) ;
#34074=CARTESIAN_POINT ( 'NONE',  ( -13.74909385650551563, -8.104110260919579645, 48.81699501597546487 ) ) ;
#34082=CARTESIAN_POINT ( 'NONE',  ( -13.44284385650551705, -8.811426318492348031, 52.18089403414752070 ) ) ;
#34083=APPLICATION_CONTEXT ( 'automotive_design' ) ;
#34086=CARTESIAN_POINT ( 'NONE',  ( -15.29909385650551634, -8.114302828567740988, 52.18300498402516041 ) ) ;
#34090=EDGE_CURVE ( 'NONE', #33928, #37274, #33732, .T. ) ;
#34147=CARTESIAN_POINT ( 'NONE',  ( -16.56159385650551386, -9.295667164867525756, 49.30633214617472504 ) ) ;
#34189=CARTESIAN_POINT ( 'NONE',  ( -21.17409385650551812, -9.792211528768504536, 50.49490371617623197 ) ) ;
#34190=LINE ( 'NONE', #38363, #39979 ) ;
#34199=AXIS2_PLACEMENT_3D ( 'NONE', #31063, #41659, #30835 ) ;
#34206=CARTESIAN_POINT ( 'NONE',  ( -15.04284385541304481, -7.587656875400194068, 49.25157356644814399 ) ) ;
#34227=CARTESIAN_POINT ( 'NONE',  ( -21.76784385650551457, -6.428312510596451368, 51.20221977374900035 ) ) ;
#34245=CARTESIAN_POINT ( 'NONE',  ( -21.14909385759798965, -8.112991634885936776, 51.74999426922421719 ) ) ;
#34252=CARTESIAN_POINT ( 'NONE',  ( 8.575906144586950219, 2.110465741754207425, 60.53099189295826221 ) ) ;
#34262=CARTESIAN_POINT ( 'NONE',  ( -22.46784385650551741, -6.428312510596450480, 51.20221977374900035 ) ) ;
#34264=ADVANCED_FACE ( 'NONE', ( #14636 ), #48651, .T. ) ;
#34292=FACE_OUTER_BOUND ( 'NONE', #21459, .T. ) ;
#34296=CARTESIAN_POINT ( 'NONE',  ( -19.82409385650551670, -6.426201560718813433, 50.50509628382439331 ) ) ;
#34310=CARTESIAN_POINT ( 'NONE',  ( -16.05534385650551243, -7.417179338643134834, 52.18511593390279302 ) ) ;
#34312=CARTESIAN_POINT ( 'NONE',  ( -36.42409385541304800, -8.109206544743658540, 50.50000000000030553 ) ) ;
#34320=CARTESIAN_POINT ( 'NONE',  ( -14.56784385650551528, -6.428312510596451368, 51.20221977374900035 ) ) ;
#34323=CARTESIAN_POINT ( 'NONE',  ( -15.74909385650551386, -8.104110260919579645, 48.81699501597546487 ) ) ;
#34386=CARTESIAN_POINT ( 'NONE',  ( -17.23659385650551812, -6.915538690918074494, 49.31353937987644542 ) ) ;
#34417=CARTESIAN_POINT ( 'NONE',  ( -22.97409385650551528, -9.792211528768504536, 50.49490371617623197 ) ) ;
#34422=EDGE_CURVE ( 'NONE', #43983, #1692, #32134, .T. ) ;
#34428=CARTESIAN_POINT ( 'NONE',  ( -20.55534385650551599, -7.417179338643134834, 52.18511593390279302 ) ) ;
#34440=VECTOR ( 'NONE', #41959, 1000.000000000000000 ) ;
#34452=( BOUNDED_CURVE ( )  B_SPLINE_CURVE ( 2, ( #47677, #44009, #6069, #28723, #44247, #17857, #2377, #32880, #29211 ),
 .UNSPECIFIED., .F., .F. ) 
 B_SPLINE_CURVE_WITH_KNOTS ( ( 3, 2, 2, 2, 3 ),
 ( 0.05507682622128801109, 0.05606042056139406982, 0.05704401490150013548, 0.05802760924160620809, 0.05901120358171226682 ),
 .UNSPECIFIED. ) 
 CURVE ( )  GEOMETRIC_REPRESENTATION_ITEM ( )  RATIONAL_B_SPLINE_CURVE ( ( 0.9999999999993087751, 0.9238795325119779633, 1.000000000000000000, 0.9238795325112867385, 1.000000000000000000, 0.9238795325112867385, 1.000000000000000000, 0.9238795325111853751, 1.000000000000101474 ) ) 
 REPRESENTATION_ITEM ( '' )  );
#34470=CARTESIAN_POINT ( 'NONE',  ( -15.91784385650552025, -9.790100578890868377, 49.79778022625163203 ) ) ;
#34479=CARTESIAN_POINT ( 'NONE',  ( -16.50534385541304161, -7.595227055684746098, 51.75156210489594599 ) ) ;
#34493=CARTESIAN_POINT ( 'NONE',  ( -22.38659385759799036, -7.222650657624104298, 49.61879703869476543 ) ) ;
#34525=VERTEX_POINT ( 'NONE', #16848 ) ;
#34536=CARTESIAN_POINT ( 'NONE',  ( -17.60534385759799036, -7.595227055684746986, 51.75156210489594599 ) ) ;
#34542=CARTESIAN_POINT ( 'NONE',  ( -20.10534385650552025, -8.801233750844183135, 48.81488406609782515 ) ) ;
#34550=SHAPE_REPRESENTATION ( 'Speed Governor Worm Gear Train', ( #29031 ), #9367 ) ;
#34568=ORIENTED_EDGE ( 'NONE', *, *, #32363, .F. ) ;
#34570=CARTESIAN_POINT ( 'NONE',  ( -21.73659385541304090, -8.995762431863214559, 51.38120296130585274 ) ) ;
#34575=CARTESIAN_POINT ( 'NONE',  ( 18.87590614458706995, 1.890747609047893185, 50.53028072113869484 ) ) ;
#34620=CARTESIAN_POINT ( 'NONE',  ( -21.90534385541302598, -7.595227055684733664, 51.75156210489598152 ) ) ;
#34631=CARTESIAN_POINT ( 'NONE',  ( -22.72409385650551528, -6.426201560718813433, 50.50509628382439331 ) ) ;
#34636=ORIENTED_EDGE ( 'NONE', *, *, #23010, .T. ) ;
#34638=CARTESIAN_POINT ( 'NONE',  ( -15.71784385650551741, -9.790100578890868377, 49.79778022625163203 ) ) ;
#34656=CARTESIAN_POINT ( 'NONE',  ( -36.42409385541304800, -8.109206544743658540, 50.50000000000030553 ) ) ;
#34682=DIRECTION ( 'NONE',  ( 0.000000000000000000, 0.007114381193220324640, -0.9999746924698832418 ) ) ;
#34684=CARTESIAN_POINT ( 'NONE',  ( -21.79284385650551314, -7.406986770994973490, 48.81910596585309747 ) ) ;
#34709=ADVANCED_FACE ( 'NONE', ( #34292 ), #45177, .T. ) ;
#34711=DIRECTION ( 'NONE',  ( 1.674255585786183705E-21, -0.9999746924698832418, -0.007114381193220357599 ) ) ;
#34727=CARTESIAN_POINT ( 'NONE',  ( -16.14284385650551812, -8.811426318492348031, 52.18089403414751359 ) ) ;
#34729=CARTESIAN_POINT ( 'NONE',  ( 18.82590614458706924, 1.904976371434334181, 48.53033133619892681 ) ) ;
#34739=ORIENTED_EDGE ( 'NONE', *, *, #17839, .T. ) ;
#34749=CYLINDRICAL_SURFACE ( 'NONE', #34199, 1.249999999999999334 ) ;
#34753=DIRECTION ( 'NONE',  ( 0.000000000000000000, 1.000000000000000000, 0.000000000000000000 ) ) ;
#34790=DIRECTION ( 'NONE',  ( -3.361323641615342917E-32, -0.9999954153791273948, -0.003028072113822189229 ) ) ;
#34793=DIRECTION ( 'NONE',  ( 0.000000000000000000, -0.007114381193220324640, 0.9999746924698832418 ) ) ;
#34794=CARTESIAN_POINT ( 'NONE',  ( -14.70534385650551989, -8.801233750844183135, 48.81488406609782515 ) ) ;
#34795=EDGE_CURVE ( 'NONE', #12705, #29888, #38861, .T. ) ;
#34796=ORIENTED_EDGE ( 'NONE', *, *, #45495, .F. ) ;
#34816=CARTESIAN_POINT ( 'NONE',  ( -20.66784385541303948, -9.357632978295830739, 49.97845033065684106 ) ) ;
#34835=EDGE_CURVE ( 'NONE', #45882, #2071, #31826, .T. ) ;
#34864=CARTESIAN_POINT ( 'NONE',  ( -15.97409385759799072, -6.859212275519751323, 50.50378509014259265 ) ) ;
#34869=EDGE_LOOP ( 'NONE', ( #27762, #28226, #37942, #6160 ) ) ;
#34870=CARTESIAN_POINT ( 'NONE',  ( -21.31784385650551883, -9.790100578890868377, 49.79778022625163203 ) ) ;
#34876=CARTESIAN_POINT ( 'NONE',  ( -12.97364361214796347, -9.395187332399693503, 49.41428126932424192 ) ) ;
#34890=ORIENTED_EDGE ( 'NONE', *, *, #37765, .T. ) ;
#34923=CARTESIAN_POINT ( 'NONE',  ( -20.78034385650551386, -6.424090610841174609, 49.80797279389977916 ) ) ;
#34935=ADVANCED_FACE ( 'NONE', ( #35742 ), #5740, .F. ) ;
#34939=DIRECTION ( 'NONE',  ( 0.000000000000000000, -0.9999954153791273948, -0.003028072113819838245 ) ) ;
#34958=CARTESIAN_POINT ( 'NONE',  ( -17.94284385650551528, -8.811426318492348031, 52.18089403414751359 ) ) ;
#34995=CARTESIAN_POINT ( 'NONE',  ( -21.68034385650551599, -6.424090610841174609, 49.80797279389977916 ) ) ;
#35023=DIRECTION ( 'NONE',  ( -1.616182858256118783E-16, -0.003028072113822189229, 0.9999954153791275058 ) ) ;
#35027=CARTESIAN_POINT ( 'NONE',  ( -16.73034385650551670, -9.794322478646142471, 51.19202720610083190 ) ) ;
#35044=EDGE_CURVE ( 'NONE', #47460, #20025, #47804, .T. ) ;
#35055=CARTESIAN_POINT ( 'NONE',  ( -21.90534385541304374, -7.595227055684746986, 51.75156210489594599 ) ) ;
#35116=CARTESIAN_POINT ( 'NONE',  ( -22.33034385650551812, -9.794322478646142471, 51.19202720610083901 ) ) ;
#35124=( BOUNDED_CURVE ( )  B_SPLINE_CURVE ( 3, ( #48168, #37307, #45230, #48408 ),
 .UNSPECIFIED., .F., .F. ) 
 B_SPLINE_CURVE_WITH_KNOTS ( ( 4, 4 ),
 ( 6.081827386389253576, 6.484543227969918888 ),
 .UNSPECIFIED. ) 
 CURVE ( )  GEOMETRIC_REPRESENTATION_ITEM ( )  RATIONAL_B_SPLINE_CURVE ( ( 1.000000000000000000, 0.9865305980755139093, 0.9865305980755139093, 1.000000000000000000 ) ) 
 REPRESENTATION_ITEM ( '' )  );
#35144=LINE ( 'NONE', #7675, #47893 ) ;
#35162=CARTESIAN_POINT ( 'NONE',  ( -18.19284385650551883, -7.406986770994973490, 48.81910596585309747 ) ) ;
#35181=EDGE_CURVE ( 'NONE', #1692, #48324, #7890, .T. ) ;
#35201=CARTESIAN_POINT ( 'NONE',  ( -18.84284385650551741, -8.811426318492348031, 52.18089403414751359 ) ) ;
#35220=CARTESIAN_POINT ( 'NONE',  ( -21.54284385759798681, -7.587656875400192291, 49.25157356644813689 ) ) ;
#35227=ADVANCED_FACE ( 'NONE', ( #27101, #42127 ), #24390, .T. ) ;
#35272=CARTESIAN_POINT ( 'NONE',  ( -16.22409385650551883, -6.426201560718813433, 50.50509628382439331 ) ) ;
#35299=CARTESIAN_POINT ( 'NONE',  ( -19.93659385541304019, -8.995762431863214559, 51.38120296130585274 ) ) ;
#35309=( BOUNDED_SURFACE ( )  B_SPLINE_SURFACE ( 1, 2, ( 
 ( #26889, #45612, #46575, #27112, #27356, #27601, #34493, #8658, #1019, #16014, #19975, #19478, #11863, #23921, #41899, #7940, #38922, #23684, #38682, #5201, #20208, #35220, #8177, #23190, #38180, #37948, #4234, #19243, #34245, #4462, #4965, #779, #15775, #30831, #45844, #12100, #42141, #8406, #40142, #24156, #9634, #10100, #1979, #24877, #47295, #6162, #28079, #32736, #25123, #13766, #16976, #16740, #32275, #21436, #6407, #2218, #24650, #13530, #28576, #24402, #28810, #43103, #39650, #43847, #20704, #27840, #43604, #32505, #13047, #9862, #5921, #2467, #17230, #5449, #39413, #5695, #42869, #20466, #9140, #21188, #12818, #1748, #36420, #36182, #35462, #39891, #2700, #17707, #39161, #31782, #46802, #35694, #9382, #20942, #32022, #47040, #13283, #28337, #17476, #47531, #43363, #35942, #33202, #44817, #7390, #44330, #25363, #13996, #33441, #44560, #2933, #29293, #29050, #40376, #37383, #25591, #29785, #3675, #36902, #18680, #3427, #48237, #37140, #14474, #10582, #11071, #18940, #48480, #25837, #26329, #17943, #26093, #40601, #41105, #22390, #29532, #6885, #40857, #10816, #30042, #6644, #44097, #21661, #7139, #18432, #10350, #14244, #3184, #21899, #22156, #18194, #33686, #14712, #36082, #14977, #47760, #45068, #36651, #11315, #41342, #7635, #22640, #37638, #32961, #3933, #48007, #30529, #5143, #23136, #15958, #38362, #46261, #27058, #962, #45305, #12518, #12042, #4906, #8847 ),
 ( #480, #19918, #19678, #33953, #38127, #15465, #4655, #247, #30772, #7879, #8595, #37894, #45793, #15225, #42082, #27543, #720, #15715, #22900, #30284, #42585, #34684, #11552, #19184, #23863, #26576, #41597, #23625, #38867, #45547, #4182, #31000, #34189, #38622, #8351, #23368, #11806, #26828, #4403, #34923, #41847, #8121, #19422, #34428, #46022, #12277, #42327, #27301, #1188, #16194, #31238, #42810, #24594, #36125, #44450, #16445, #21127, #5386, #28018, #40734, #46977, #24341, #10703, #9574, #35408, #24096, #25719, #20405, #47228, #2408, #1685, #43045, #16924, #20647, #17418, #31960, #35877, #16685, #39589, #20151, #13221, #12990, #31726, #35641, #1431, #35162, #1923, #28271, #9084, #39102, #39831, #43300, #29418, #6099, #2159, #46747, #9322, #31479, #5866, #20883, #32450, #39352, #17159, #32212, #13473, #28520, #5639, #43544, #9808, #24820, #46514, #47475, #14364, #12767, #27781, #26703, #41722, #29661, #40989, #44695, #19307, #15593, #37027, #34310, #18561, #3807, #33568, #18314, #7762, #18823, #10952, #25970, #33829, #597, #33325, #126, #4298, #44947, #19065, #41470, #365, #22274, #26949, #30657, #8012, #11202, #7272, #26455, #45676, #11932, #45189, #15110, #22778, #37771, #48613, #23025, #37265, #30168, #38010, #14850, #22033, #4067, #7015, #3555, #34074, #11428, #45425, #15348, #48364, #3314, #30410, #14599, #29914, #26214, #11678, #41226, #7512, #22518, #37512 ) ),
 .UNSPECIFIED., .F., .F., .F. ) 
 B_SPLINE_SURFACE_WITH_KNOTS ( ( 2, 2 ),
 ( 3, 2, 2, 2, 2, 2, 2, 2, 2, 2, 2, 2, 2, 2, 2, 2, 2, 2, 2, 2, 2, 2, 2, 2, 2, 2, 2, 2, 2, 2, 2, 2, 2, 2, 2, 2, 2, 2, 2, 2, 2, 2, 2, 2, 2, 2, 2, 2, 2, 2, 2, 2, 2, 2, 2, 2, 2, 2, 2, 2, 2, 2, 2, 2, 2, 2, 2, 2, 2, 2, 2, 2, 2, 2, 2, 2, 2, 2, 2, 2, 2, 2, 2, 2, 2, 2, 2, 2, 2, 3 ),
 ( 0.000000000000000000, 1.000000000000000000 ),
 ( 0.000000000000000000, 0.01041666666666666609, 0.02083333333333333218, 0.03125000000000000000, 0.04166666666666666435, 0.05208333333333333565, 0.06250000000000000000, 0.07291666666666667129, 0.08333333333333332871, 0.09375000000000000000, 0.1041666666666666713, 0.1145833333333333287, 0.1250000000000000000, 0.1354166666666666574, 0.1458333333333333426, 0.1562500000000000000, 0.1666666666666666574, 0.1770833333333333426, 0.1875000000000000000, 0.1979166666666666574, 0.2083333333333333426, 0.2187500000000000000, 0.2291666666666666574, 0.2395833333333333426, 0.2500000000000000000, 0.2604166666666666852, 0.2708333333333333148, 0.2812500000000000000, 0.2916666666666666852, 0.3020833333333333148, 0.3125000000000000000, 0.3229166666666666852, 0.3333333333333333148, 0.3437500000000000000, 0.3541666666666666852, 0.3645833333333333148, 0.3750000000000000000, 0.3854166666666666852, 0.3958333333333333148, 0.4062500000000000000, 0.4166666666666666852, 0.4270833333333333148, 0.4375000000000000000, 0.4479166666666666852, 0.4583333333333333148, 0.4687500000000000000, 0.4791666666666666852, 0.4895833333333333148, 0.5000000000000000000, 0.5104166666666666297, 0.5208333333333333703, 0.5312500000000000000, 0.5416666666666666297, 0.5520833333333333703, 0.5625000000000000000, 0.5729166666666666297, 0.5833333333333333703, 0.5937500000000000000, 0.6041666666666666297, 0.6145833333333333703, 0.6250000000000000000, 0.6354166666666666297, 0.6458333333333333703, 0.6562500000000000000, 0.6666666666666666297, 0.6770833333333333703, 0.6875000000000000000, 0.6979166666666666297, 0.7083333333333333703, 0.7187500000000000000, 0.7291666666666666297, 0.7395833333333333703, 0.7500000000000000000, 0.7604166666666666297, 0.7708333333333333703, 0.7812500000000000000, 0.7916666666666666297, 0.8020833333333333703, 0.8125000000000000000, 0.8229166666666666297, 0.8333333333333333703, 0.8437500000000000000, 0.8541666666666666297, 0.8645833333333333703, 0.8750000000000000000, 0.8854166666666666297, 0.8958333333333333703, 0.9062500000000000000, 0.9166666666666666297, 0.9259047100830449795 ),
 .UNSPECIFIED. ) 
 GEOMETRIC_REPRESENTATION_ITEM ( )  RATIONAL_B_SPLINE_SURFACE ( (
 ( 1.000000000000000000, 0.9238795325112867385, 1.000000000000000000, 0.9238795325112867385, 1.000000000000000000, 0.9238795325112867385, 1.000000000000000000, 0.9238795325112867385, 1.000000000000000000, 0.9238795325112867385, 1.000000000000000000, 0.9238795325112867385, 1.000000000000000000, 0.9238795325112867385, 1.000000000000000000, 0.9238795325112867385, 1.000000000000000000, 0.9238795325112867385, 1.000000000000000000, 0.9238795325112867385, 1.000000000000000000, 0.9238795325112867385, 1.000000000000000000, 0.9238795325112867385, 1.000000000000000000, 0.9238795325112867385, 1.000000000000000000, 0.9238795325112867385, 1.000000000000000000, 0.9238795325112867385, 1.000000000000000000, 0.9238795325112867385, 1.000000000000000000, 0.9238795325112867385, 1.000000000000000000, 0.9238795325112867385, 1.000000000000000000, 0.9238795325112867385, 1.000000000000000000, 0.9238795325112867385, 1.000000000000000000, 0.9238795325112867385, 1.000000000000000000, 0.9238795325112867385, 1.000000000000000000, 0.9238795325112867385, 1.000000000000000000, 0.9238795325112867385, 1.000000000000000000, 0.9238795325112867385, 1.000000000000000000, 0.9238795325112867385, 1.000000000000000000, 0.9238795325112867385, 1.000000000000000000, 0.9238795325112867385, 1.000000000000000000, 0.9238795325112867385, 1.000000000000000000, 0.9238795325112867385, 1.000000000000000000, 0.9238795325112867385, 1.000000000000000000, 0.9238795325112867385, 1.000000000000000000, 0.9238795325112867385, 1.000000000000000000, 0.9238795325112867385, 1.000000000000000000, 0.9238795325112867385, 1.000000000000000000, 0.9238795325112867385, 1.000000000000000000, 0.9238795325112867385, 1.000000000000000000, 0.9238795325112867385, 1.000000000000000000, 0.9238795325112867385, 1.000000000000000000, 0.9238795325112867385, 1.000000000000000000, 0.9238795325112867385, 1.000000000000000000, 0.9238795325112867385, 1.000000000000000000, 0.9238795325112867385, 1.000000000000000000, 0.9238795325112867385, 1.000000000000000000, 0.9238795325112867385, 1.000000000000000000, 0.9238795325112867385, 1.000000000000000000, 0.9238795325112867385, 1.000000000000000000, 0.9238795325112867385, 1.000000000000000000, 0.9238795325112867385, 1.000000000000000000, 0.9238795325112867385, 1.000000000000000000, 0.9238795325112867385, 1.000000000000000000, 0.9238795325112867385, 1.000000000000000000, 0.9238795325112867385, 1.000000000000000000, 0.9238795325112867385, 1.000000000000000000, 0.9238795325112867385, 1.000000000000000000, 0.9238795325112867385, 1.000000000000000000, 0.9238795325112867385, 1.000000000000000000, 0.9238795325112867385, 1.000000000000000000, 0.9238795325112867385, 1.000000000000000000, 0.9238795325112867385, 1.000000000000000000, 0.9238795325112867385, 1.000000000000000000, 0.9238795325112867385, 1.000000000000000000, 0.9238795325112867385, 1.000000000000000000, 0.9238795325112867385, 1.000000000000000000, 0.9238795325112867385, 1.000000000000000000, 0.9238795325112867385, 1.000000000000000000, 0.9238795325112867385, 1.000000000000000000, 0.9238795325112867385, 1.000000000000000000, 0.9238795325112867385, 1.000000000000000000, 0.9238795325112867385, 1.000000000000000000, 0.9238795325112867385, 1.000000000000000000, 0.9238795325112867385, 1.000000000000000000, 0.9238795325112867385, 1.000000000000000000, 0.9238795325112867385, 1.000000000000000000, 0.9238795325112867385, 1.000000000000000000, 0.9238795325112867385, 1.000000000000000000, 0.9238795325112867385, 1.000000000000000000, 0.9238795325112867385, 1.000000000000000000, 0.9238795325112867385, 1.000000000000000000, 0.9238795325112867385, 1.000000000000000000, 0.9238795325112867385, 1.000000000000000000, 0.9238795325112867385, 1.000000000000000000, 0.9238795325112867385, 1.000000000000000000, 0.9238795325112867385, 1.000000000000000000, 0.9238795325112867385, 1.000000000000000000, 0.9238795325112867385, 1.000000000000000000, 0.9238795325112867385, 1.000000000000000000, 0.9238795325112867385, 1.000000000000000000, 0.9324923983805685213, 0.9847233224627454096),
 ( 1.000000000000000000, 0.9238795325112867385, 1.000000000000000000, 0.9238795325112867385, 1.000000000000000000, 0.9238795325112867385, 1.000000000000000000, 0.9238795325112867385, 1.000000000000000000, 0.9238795325112867385, 1.000000000000000000, 0.9238795325112867385, 1.000000000000000000, 0.9238795325112867385, 1.000000000000000000, 0.9238795325112867385, 1.000000000000000000, 0.9238795325112867385, 1.000000000000000000, 0.9238795325112867385, 1.000000000000000000, 0.9238795325112867385, 1.000000000000000000, 0.9238795325112867385, 1.000000000000000000, 0.9238795325112867385, 1.000000000000000000, 0.9238795325112867385, 1.000000000000000000, 0.9238795325112867385, 1.000000000000000000, 0.9238795325112867385, 1.000000000000000000, 0.9238795325112867385, 1.000000000000000000, 0.9238795325112867385, 1.000000000000000000, 0.9238795325112867385, 1.000000000000000000, 0.9238795325112867385, 1.000000000000000000, 0.9238795325112867385, 1.000000000000000000, 0.9238795325112867385, 1.000000000000000000, 0.9238795325112867385, 1.000000000000000000, 0.9238795325112867385, 1.000000000000000000, 0.9238795325112867385, 1.000000000000000000, 0.9238795325112867385, 1.000000000000000000, 0.9238795325112867385, 1.000000000000000000, 0.9238795325112867385, 1.000000000000000000, 0.9238795325112867385, 1.000000000000000000, 0.9238795325112867385, 1.000000000000000000, 0.9238795325112867385, 1.000000000000000000, 0.9238795325112867385, 1.000000000000000000, 0.9238795325112867385, 1.000000000000000000, 0.9238795325112867385, 1.000000000000000000, 0.9238795325112867385, 1.000000000000000000, 0.9238795325112867385, 1.000000000000000000, 0.9238795325112867385, 1.000000000000000000, 0.9238795325112867385, 1.000000000000000000, 0.9238795325112867385, 1.000000000000000000, 0.9238795325112867385, 1.000000000000000000, 0.9238795325112867385, 1.000000000000000000, 0.9238795325112867385, 1.000000000000000000, 0.9238795325112867385, 1.000000000000000000, 0.9238795325112867385, 1.000000000000000000, 0.9238795325112867385, 1.000000000000000000, 0.9238795325112867385, 1.000000000000000000, 0.9238795325112867385, 1.000000000000000000, 0.9238795325112867385, 1.000000000000000000, 0.9238795325112867385, 1.000000000000000000, 0.9238795325112867385, 1.000000000000000000, 0.9238795325112867385, 1.000000000000000000, 0.9238795325112867385, 1.000000000000000000, 0.9238795325112867385, 1.000000000000000000, 0.9238795325112867385, 1.000000000000000000, 0.9238795325112867385, 1.000000000000000000, 0.9238795325112867385, 1.000000000000000000, 0.9238795325112867385, 1.000000000000000000, 0.9238795325112867385, 1.000000000000000000, 0.9238795325112867385, 1.000000000000000000, 0.9238795325112867385, 1.000000000000000000, 0.9238795325112867385, 1.000000000000000000, 0.9238795325112867385, 1.000000000000000000, 0.9238795325112867385, 1.000000000000000000, 0.9238795325112867385, 1.000000000000000000, 0.9238795325112867385, 1.000000000000000000, 0.9238795325112867385, 1.000000000000000000, 0.9238795325112867385, 1.000000000000000000, 0.9238795325112867385, 1.000000000000000000, 0.9238795325112867385, 1.000000000000000000, 0.9238795325112867385, 1.000000000000000000, 0.9238795325112867385, 1.000000000000000000, 0.9238795325112867385, 1.000000000000000000, 0.9238795325112867385, 1.000000000000000000, 0.9238795325112867385, 1.000000000000000000, 0.9238795325112867385, 1.000000000000000000, 0.9238795325112867385, 1.000000000000000000, 0.9238795325112867385, 1.000000000000000000, 0.9238795325112867385, 1.000000000000000000, 0.9238795325112867385, 1.000000000000000000, 0.9238795325112867385, 1.000000000000000000, 0.9238795325112867385, 1.000000000000000000, 0.9238795325112867385, 1.000000000000000000, 0.9238795325112867385, 1.000000000000000000, 0.9238795325112867385, 1.000000000000000000, 0.9238795325112867385, 1.000000000000000000, 0.9238795325112867385, 1.000000000000000000, 0.9238795325112867385, 1.000000000000000000, 0.9238795325112867385, 1.000000000000000000, 0.9324923983805685213, 0.9847233224627454096) ) ) 
 REPRESENTATION_ITEM ( '' )  SURFACE ( )  );
#35313=CARTESIAN_POINT ( 'NONE',  ( 23.52590614458706852, 3.790747609047893540, 50.53028072113869484 ) ) ;
#35338=ORIENTED_EDGE ( 'NONE', *, *, #3191, .F. ) ;
#35344=ORIENTED_EDGE ( 'NONE', *, *, #30003, .T. ) ;
#35346=( BOUNDED_CURVE ( )  B_SPLINE_CURVE ( 2, ( #8875, #45588, #7914, #1463, #23896, #27090, #38158, #27332, #16478 ),
 .UNSPECIFIED., .F., .F. ) 
 B_SPLINE_CURVE_WITH_KNOTS ( ( 3, 2, 2, 2, 3 ),
 ( 0.5000000000000002220, 0.5104166666666668517, 0.5208333333333334814, 0.5312500000000001110, 0.5416666666666667407 ),
 .UNSPECIFIED. ) 
 CURVE ( )  GEOMETRIC_REPRESENTATION_ITEM ( )  RATIONAL_B_SPLINE_CURVE ( ( 0.9999999999999983347, 0.9238795325112884038, 1.000000000000000000, 0.9238795325112867385, 1.000000000000000000, 0.9238795325112867385, 1.000000000000000000, 0.9238795325112859613, 1.000000000000000888 ) ) 
 REPRESENTATION_ITEM ( '' )  );
#35359=CARTESIAN_POINT ( 'NONE',  ( -20.36159385650551812, -9.295667164867525756, 49.30633214617472504 ) ) ;
#35361=AXIS2_PLACEMENT_3D ( 'NONE', #27569, #23887, #27081 ) ;
#35364=CARTESIAN_POINT ( 'NONE',  ( -21.99284385650551243, -7.406986770994973490, 48.81910596585309747 ) ) ;
#35399=VECTOR ( 'NONE', #3139, 1000.000000000000000 ) ;
#35408=CARTESIAN_POINT ( 'NONE',  ( -19.37409385650551741, -9.792211528768504536, 50.49490371617623197 ) ) ;
#35424=DIRECTION ( 'NONE',  ( 0.000000000000000000, -0.9999954153791273948, -0.003028072113819838245 ) ) ;
#35445=CARTESIAN_POINT ( 'NONE',  ( -17.38034385650551883, -6.424090610841176385, 49.80797279389978627 ) ) ;
#35462=CARTESIAN_POINT ( 'NONE',  ( -17.99909385759799108, -8.105421454601382081, 49.25000573077640098 ) ) ;
#35473=FACE_OUTER_BOUND ( 'NONE', #36627, .T. ) ;
#35477=VERTEX_POINT ( 'NONE', #34417 ) ;
#35478=EDGE_LOOP ( 'NONE', ( #2211, #25476, #32857, #44906 ) ) ;
#35509=DIRECTION ( 'NONE',  ( -1.000000000000000000, 4.164305804376849172E-17, -1.614929280266638808E-16 ) ) ;
#35520=CARTESIAN_POINT ( 'NONE',  ( -17.74284385650551599, -8.811426318492348031, 52.18089403414751359 ) ) ;
#35524=ORIENTED_EDGE ( 'NONE', *, *, #23253, .T. ) ;
#35541=CARTESIAN_POINT ( 'NONE',  ( -16.48034385759799392, -9.360768649639298999, 51.01397948905923130 ) ) ;
#35545=CARTESIAN_POINT ( 'NONE',  ( -21.34284385541304374, -7.587656875400192291, 49.25157356644813689 ) ) ;
#35561=VERTEX_POINT ( 'NONE', #45293 ) ;
#35576=CARTESIAN_POINT ( 'NONE',  ( 18.54465614458695910, 3.140487395509476976, 50.61810660878216339 ) ) ;
#35585=EDGE_LOOP ( 'NONE', ( #16753, #39469 ) ) ;
#35590=ADVANCED_FACE ( 'NONE', ( #11062 ), #26084, .T. ) ;
#35595=ORIENTED_EDGE ( 'NONE', *, *, #37765, .F. ) ;
#35596=CARTESIAN_POINT ( 'NONE',  ( -20.86784385650551954, -6.428312510596451368, 51.20221977374900035 ) ) ;
#35601=CARTESIAN_POINT ( 'NONE',  ( -22.10534385650551670, -8.801233750844183135, 48.81488406609782515 ) ) ;
#35619=( BOUNDED_CURVE ( )  B_SPLINE_CURVE ( 2, ( #18287, #48337, #14569, #41935, #38715, #333, #27157, #1053, #15318 ),
 .UNSPECIFIED., .F., .F. ) 
 B_SPLINE_CURVE_WITH_KNOTS ( ( 3, 2, 2, 2, 3 ),
 ( 0.04327498545061642110, 0.04425837495377543673, 0.04524176445693445237, 0.04622515396009346106, 0.04720854346325247669 ),
 .UNSPECIFIED. ) 
 CURVE ( )  GEOMETRIC_REPRESENTATION_ITEM ( )  RATIONAL_B_SPLINE_CURVE ( ( 1.000000000000174527, 0.9238795325111123224, 1.000000000000000000, 0.9238795325112867385, 1.000000000000000000, 0.9238795325112867385, 1.000000000000000000, 0.9238795325112583168, 1.000000000000028422 ) ) 
 REPRESENTATION_ITEM ( '' )  );
#35620=VERTEX_POINT ( 'NONE', #4898 ) ;
#35627=CARTESIAN_POINT ( 'NONE',  ( -36.42409385541304800, -8.109206544743658540, 50.50000000000030553 ) ) ;
#35628=DIRECTION ( 'NONE',  ( -0.9524241471993249997, -0.3047743298226212039, -0.0009228828802129951337 ) ) ;
#35633=EDGE_LOOP ( 'NONE', ( #35344, #4912, #14771, #24828, #32820, #10634, #19327, #8914, #21528, #4249, #40043, #13523, #19301, #7152, #3857, #969, #2426, #8549, #37078, #34636, #40426, #4087, #16861, #36447, #8688, #12939 ) ) ;
#35641=CARTESIAN_POINT ( 'NONE',  ( -18.30534385650551954, -8.801233750844183135, 48.81488406609782515 ) ) ;
#35660=FACE_OUTER_BOUND ( 'NONE', #36072, .T. ) ;
#35669=ORIENTED_EDGE ( 'NONE', *, *, #44681, .T. ) ;
#35677=CARTESIAN_POINT ( 'NONE',  ( -14.51159385650551492, -6.922745924619793101, 51.69366785382590024 ) ) ;
#35681=FACE_OUTER_BOUND ( 'NONE', #12208, .T. ) ;
#35682=EDGE_LOOP ( 'NONE', ( #1619, #32975, #45367, #42556 ) ) ;
#35694=CARTESIAN_POINT ( 'NONE',  ( -17.60534385759799036, -7.595227055684746986, 51.75156210489594599 ) ) ;
#35718=ORIENTED_EDGE ( 'NONE', *, *, #41170, .F. ) ;
#35727=ORIENTED_EDGE ( 'NONE', *, *, #25067, .F. ) ;
#35742=FACE_OUTER_BOUND ( 'NONE', #27812, .T. ) ;
#35748=CARTESIAN_POINT ( 'NONE',  ( -17.96784385650551741, -6.428312510596451368, 51.20221977374900035 ) ) ;
#35752=FACE_OUTER_BOUND ( 'NONE', #44789, .T. ) ;
#35758=CARTESIAN_POINT ( 'NONE',  ( 6.575906144586949331, -6.859212275519752211, 50.50378509014259265 ) ) ;
#35777=CARTESIAN_POINT ( 'NONE',  ( -19.82409385541304303, -9.359200813967568422, 50.49621490985803263 ) ) ;
#35830=CARTESIAN_POINT ( 'NONE',  ( -20.13659385650551670, -6.915538690918075382, 49.31353937987644542 ) ) ;
#35835=CARTESIAN_POINT ( 'NONE',  ( -22.66784385650551670, -6.428312510596451368, 51.20221977374900035 ) ) ;
#35864=CYLINDRICAL_SURFACE ( 'NONE', #25881, 1.049999999999998934 ) ;
#35877=CARTESIAN_POINT ( 'NONE',  ( -18.69909385650551670, -8.114302828567740988, 52.18300498402516041 ) ) ;
#35891=DIRECTION ( 'NONE',  ( -1.000000000000000000, 2.276824562219560297E-16, 0.000000000000000000 ) ) ;
#35892=CARTESIAN_POINT ( 'NONE',  ( -22.91784385650551670, -9.790100578890868377, 49.79778022625162492 ) ) ;
#35903=( BOUNDED_CURVE ( )  B_SPLINE_CURVE ( 2, ( #36557, #36089, #39796, #25742, #25502, #2370, #14383, #44472, #6557 ),
 .UNSPECIFIED., .F., .F. ) 
 B_SPLINE_CURVE_WITH_KNOTS ( ( 3, 2, 2, 2, 3 ),
 ( 0.03147235863061165206, 0.03245579865619469678, 0.03343923868177773456, 0.03442267870736077234, 0.03540611873294381706 ),
 .UNSPECIFIED. ) 
 CURVE ( )  GEOMETRIC_REPRESENTATION_ITEM ( )  RATIONAL_B_SPLINE_CURVE ( ( 1.000000000000000888, 0.9238795325112859613, 1.000000000000000000, 0.9238795325112867385, 1.000000000000000000, 0.9238795325112867385, 1.000000000000000000, 0.9238795325112112433, 1.000000000000075495 ) ) 
 REPRESENTATION_ITEM ( '' )  );
#35914=EDGE_CURVE ( 'NONE', #43983, #35477, #8921, .T. ) ;
#35923=CARTESIAN_POINT ( 'NONE',  ( -13.44284385650551705, -8.811426318492348031, 52.18089403414752070 ) ) ;
#35942=CARTESIAN_POINT ( 'NONE',  ( -17.04284385759799036, -7.587656875400192291, 49.25157356644813689 ) ) ;
#35943=CARTESIAN_POINT ( 'NONE',  ( -36.42409385541304800, -6.859212275519750435, 50.50378509014258555 ) ) ;
#35986=DIRECTION ( 'NONE',  ( 0.9524241471993248886, -0.3047743298226213149, -0.0009228828802126874372 ) ) ;
#35994=CARTESIAN_POINT ( 'NONE',  ( -17.88659385759798681, -7.222650657624104298, 49.61879703869476543 ) ) ;
#36002=AXIS2_PLACEMENT_3D ( 'NONE', #3474, #29837, #41152 ) ;
#36009=ADVANCED_FACE ( 'NONE', ( #21718 ), #7445, .T. ) ;
#36011=PLANE ( 'NONE',  #29818 ) ;
#36017=CARTESIAN_POINT ( 'NONE',  ( -16.39284385541304800, -8.630756214087126565, 51.74842643355248129 ) ) ;
#36026=ORIENTED_EDGE ( 'NONE', *, *, #39825, .T. ) ;
#36028=CIRCLE ( 'NONE', #691, 2.000000000000000000 ) ;
#36070=CARTESIAN_POINT ( 'NONE',  ( -15.13034385759799072, -6.857644439848019857, 49.98602051094139398 ) ) ;
#36072=EDGE_LOOP ( 'NONE', ( #39741, #42089, #47383, #43992 ) ) ;
#36074=CARTESIAN_POINT ( 'NONE',  ( -18.67409385650551457, -9.792211528768504536, 50.49490371617623197 ) ) ;
#36077=CARTESIAN_POINT ( 'NONE',  ( -19.40534385650551741, -8.801233750844183135, 48.81488406609782515 ) ) ;
#36082=CARTESIAN_POINT ( 'NONE',  ( -14.11784385759798965, -6.860780111191487229, 51.02154966934377711 ) ) ;
#36089=CARTESIAN_POINT ( 'NONE',  ( -19.76784385541295919, -9.357632978295972848, 49.97845033065677001 ) ) ;
#36112=CARTESIAN_POINT ( 'NONE',  ( -19.12409385759799108, -9.359200813967568422, 50.49621490985803263 ) ) ;
#36125=CARTESIAN_POINT ( 'NONE',  ( -19.99284385650551243, -7.406986770994973490, 48.81910596585309747 ) ) ;
#36140=CARTESIAN_POINT ( 'NONE',  ( -19.88034385650552238, -6.424090610841174609, 49.80797279389977916 ) ) ;
#36149=DIRECTION ( 'NONE',  ( 0.000000000000000000, -0.007114381193220334181, 0.9999746924698833528 ) ) ;
#36161=CARTESIAN_POINT ( 'NONE',  ( -13.66784385650551670, -6.428312510596451368, 51.20221977374900035 ) ) ;
#36181=EDGE_CURVE ( 'NONE', #26883, #10524, #39703, .T. ) ;
#36182=CARTESIAN_POINT ( 'NONE',  ( -18.05534385759799321, -8.623186033802570094, 49.24843789510466507 ) ) ;
#36218=CARTESIAN_POINT ( 'NONE',  ( -18.39284385759799179, -8.630756214087126565, 51.74842643355248129 ) ) ;
#36227=LINE ( 'NONE', #13804, #20599 ) ;
#36237=CARTESIAN_POINT ( 'NONE',  ( -13.52409385650551599, -6.426201560718813433, 50.50509628382439331 ) ) ;
#36265=CARTESIAN_POINT ( 'NONE',  ( -17.29284385541304303, -8.630756214087126565, 51.74842643355248129 ) ) ;
#36281=CARTESIAN_POINT ( 'NONE',  ( -20.61159385541303379, -8.990409506049216404, 49.61344411288074241 ) ) ;
#36297=CARTESIAN_POINT ( 'NONE',  ( -22.41159385650551528, -6.922745924619793101, 51.69366785382590024 ) ) ;
#36299=ORIENTED_EDGE ( 'NONE', *, *, #13411, .T. ) ;
#36304=CARTESIAN_POINT ( 'NONE',  ( -17.74284385541294284, -7.587656875400116796, 49.25157356644795925 ) ) ;
#36315=CARTESIAN_POINT ( 'NONE',  ( -18.89909385650551599, -8.114302828567740988, 52.18300498402516041 ) ) ;
#36317=CARTESIAN_POINT ( 'NONE',  ( 18.46573386768564973, 0.6667653706753842169, 50.27657325150214973 ) ) ;
#36320=CARTESIAN_POINT ( 'NONE',  ( -18.73034385650551670, -9.794322478646142471, 51.19202720610083901 ) ) ;
#36379=CARTESIAN_POINT ( 'NONE',  ( -20.27409385650551599, -9.792211528768504536, 50.49490371617623197 ) ) ;
#36401=CARTESIAN_POINT ( 'NONE',  ( -14.11784385650551776, -9.790100578890868377, 49.79778022625163203 ) ) ;
#36420=CARTESIAN_POINT ( 'NONE',  ( -18.11159385759799179, -8.990409506049200417, 49.61344411288074951 ) ) ;
#36447=ORIENTED_EDGE ( 'NONE', *, *, #9932, .T. ) ;
#36470=CARTESIAN_POINT ( 'NONE',  ( -14.42409385650551457, -6.426201560718813433, 50.50509628382439331 ) ) ;
#36486=DIRECTION ( 'NONE',  ( 1.000000000000000000, 1.669677910507523057E-21, 6.493791346278465266E-22 ) ) ;
#36494=CARTESIAN_POINT ( 'NONE',  ( -17.57409385541304303, -6.859212275519751323, 50.50378509014259265 ) ) ;
#36534=EDGE_LOOP ( 'NONE', ( #38554, #27328, #20081, #14262 ) ) ;
#36543=CARTESIAN_POINT ( 'NONE',  ( -18.73034385650551670, -9.794322478646142471, 51.19202720610083901 ) ) ;
#36545=AXIS2_PLACEMENT_3D ( 'NONE', #19002, #11608, #26638 ) ;
#36548=CARTESIAN_POINT ( 'NONE',  ( -17.60534385650551670, -8.801233750844183135, 48.81488406609782515 ) ) ;
#36552=EDGE_CURVE ( 'NONE', #20955, #21742, #46277, .T. ) ;
#36557=CARTESIAN_POINT ( 'NONE',  ( -19.82409385541304303, -9.359200813967568422, 50.49621490985803263 ) ) ;
#36559=CARTESIAN_POINT ( 'NONE',  ( -17.40534385541293716, -7.595227055684673267, 51.75156210489613073 ) ) ;
#36561=CARTESIAN_POINT ( 'NONE',  ( 18.62590614458706995, 1.890747609047893185, 50.53028072113869484 ) ) ;
#36576=LINE ( 'NONE', #17869, #9310 ) ;
#36612=CARTESIAN_POINT ( 'NONE',  ( -20.83659385650551599, -6.915538690918074494, 49.31353937987644542 ) ) ;
#36614=VECTOR ( 'NONE', #9463, 1000.000000000000114 ) ;
#36627=EDGE_LOOP ( 'NONE', ( #16608, #24251, #5918 ) ) ;
#36651=CARTESIAN_POINT ( 'NONE',  ( -13.89284385759799179, -8.630756214087126565, 51.74842643355248129 ) ) ;
#36671=( BOUNDED_CURVE ( )  B_SPLINE_CURVE ( 3, ( #37873, #4164, #19165, #3410 ),
 .UNSPECIFIED., .F., .F. ) 
 B_SPLINE_CURVE_WITH_KNOTS ( ( 4, 4 ),
 ( 6.081827386389255352, 6.484543227969919776 ),
 .UNSPECIFIED. ) 
 CURVE ( )  GEOMETRIC_REPRESENTATION_ITEM ( )  RATIONAL_B_SPLINE_CURVE ( ( 1.000000000000000000, 0.9865305980755139093, 0.9865305980755139093, 1.000000000000000000 ) ) 
 REPRESENTATION_ITEM ( '' )  );
#36685=DIRECTION ( 'NONE',  ( 0.000000000000000000, 0.007114381193220334181, -0.9999746924698833528 ) ) ;
#36697=DIRECTION ( 'NONE',  ( -1.000000000000000000, -1.669677910507523057E-21, -6.493791346278465266E-22 ) ) ;
#36722=EDGE_CURVE ( 'NONE', #35477, #21919, #21102, .T. ) ;
#36725=CARTESIAN_POINT ( 'NONE',  ( -18.81159385541304374, -8.990409506049200417, 49.61344411288074951 ) ) ;
#36728=CARTESIAN_POINT ( 'NONE',  ( -36.42409385541304800, -8.109206544743658540, 50.50000000000030553 ) ) ;
#36739=CARTESIAN_POINT ( 'NONE',  ( -20.55534385541303521, -8.623186033802577199, 49.24843789510464376 ) ) ;
#36752=ORIENTED_EDGE ( 'NONE', *, *, #12709, .F. ) ;
#36762=DIRECTION ( 'NONE',  ( 1.616182858256118783E-16, 0.003028072113822189229, -0.9999954153791275058 ) ) ;
#36764=B_SPLINE_CURVE_WITH_KNOTS ( 'NONE', 1,
 ( #45525, #41824 ),
 .UNSPECIFIED., .F., .F.,
 ( 2, 2 ),
 ( 0.000000000000000000, 1.000000000000000000 ),
 .UNSPECIFIED. ) ;
#36782=CARTESIAN_POINT ( 'NONE',  ( -18.84284385650551386, -8.811426318492348031, 52.18089403414751359 ) ) ;
#36786=CYLINDRICAL_SURFACE ( 'NONE', #23713, 1.249999999999999334 ) ;
#36788=CARTESIAN_POINT ( 'NONE',  ( -17.43659385650551741, -6.915538690918075382, 49.31353937987644542 ) ) ;
#36805=CARTESIAN_POINT ( 'NONE',  ( -17.29284385541293645, -8.630756214087201172, 51.74842643355267313 ) ) ;
#36808=VECTOR ( 'NONE', #9003, 1000.000000000000000 ) ;
#36828=AXIS2_PLACEMENT_3D ( 'NONE', #22602, #7356, #48701 ) ;
#36854=CARTESIAN_POINT ( 'NONE',  ( -18.30534385650551954, -8.801233750844183135, 48.81488406609782515 ) ) ;
#36855=VECTOR ( 'NONE', #4224, 1000.000000000000000 ) ;
#36865=ORIENTED_EDGE ( 'NONE', *, *, #23010, .F. ) ;
#36889=EDGE_LOOP ( 'NONE', ( #36026, #35669, #20968, #39546 ) ) ;
#36897=ORIENTED_EDGE ( 'NONE', *, *, #31680, .F. ) ;
#36902=CARTESIAN_POINT ( 'NONE',  ( -16.08659385759798965, -7.222650657624104298, 49.61879703869476543 ) ) ;
#36938=LINE ( 'NONE', #32998, #4541 ) ;
#36940=CARTESIAN_POINT ( 'NONE',  ( -22.27409385650551243, -9.792211528768504536, 50.49490371617623197 ) ) ;
#36949=CARTESIAN_POINT ( 'NONE',  ( -13.58034385650551812, -6.424090610841176385, 49.80797279389978627 ) ) ;
#36966=DIRECTION ( 'NONE',  ( 2.231660450020913271E-16, 0.9999954153791273948, 0.003028072113822188795 ) ) ;
#36970=CARTESIAN_POINT ( 'NONE',  ( -15.35534385759799036, -8.623186033802571870, 49.24843789510467218 ) ) ;
#36972=CARTESIAN_POINT ( 'NONE',  ( -21.28659385541298121, -7.222650657624032355, 49.61879703869470148 ) ) ;
#36978=CARTESIAN_POINT ( 'NONE',  ( -15.15534385541304552, -8.623186033802571870, 49.24843789510467218 ) ) ;
#36996=CARTESIAN_POINT ( 'NONE',  ( -20.66784385541298263, -9.357632978295557180, 49.97845033065652842 ) ) ;
#37004=LINE ( 'NONE', #13387, #24217 ) ;
#37023=CIRCLE ( 'NONE', #26834, 1.249999999999999334 ) ;
#37027=CARTESIAN_POINT ( 'NONE',  ( -16.11159385650551457, -6.922745924619793101, 51.69366785382590024 ) ) ;
#37037=CARTESIAN_POINT ( 'NONE',  ( -13.89284385650552167, -7.406986770994973490, 48.81910596585309747 ) ) ;
#37041=CARTESIAN_POINT ( 'NONE',  ( -18.56159385650551741, -9.295667164867525756, 49.30633214617472504 ) ) ;
#37078=ORIENTED_EDGE ( 'NONE', *, *, #6334, .T. ) ;
#37081=EDGE_CURVE ( 'NONE', #27443, #47374, #39626, .T. ) ;
#37104=CARTESIAN_POINT ( 'NONE',  ( -18.02409385650551599, -6.426201560718813433, 50.50509628382439331 ) ) ;
#37140=CARTESIAN_POINT ( 'NONE',  ( -15.86159385759799001, -7.228003583438117552, 51.38655588711986155 ) ) ;
#37166=( BOUNDED_CURVE ( )  B_SPLINE_CURVE ( 2, ( #6454, #21474, #15020, #33241, #44367, #2738, #21702, #37180, #41146 ),
 .UNSPECIFIED., .F., .F. ) 
 B_SPLINE_CURVE_WITH_KNOTS ( ( 3, 2, 2, 2, 3 ),
 ( 0.7916666666666667407, 0.8020833333333334814, 0.8125000000000001110, 0.8229166666666667407, 0.8333333333333334814 ),
 .UNSPECIFIED. ) 
 CURVE ( )  GEOMETRIC_REPRESENTATION_ITEM ( )  RATIONAL_B_SPLINE_CURVE ( ( 0.9999999999999992228, 0.9238795325112875156, 1.000000000000000000, 0.9238795325112867385, 1.000000000000000000, 0.9238795325112867385, 1.000000000000000000, 0.9238795325112859613, 1.000000000000000888 ) ) 
 REPRESENTATION_ITEM ( '' )  );
#37174=CARTESIAN_POINT ( 'NONE',  ( 18.57590614458695200, 1.644564126066233145, 49.26952947973238395 ) ) ;
#37177=CARTESIAN_POINT ( 'NONE',  ( -20.41784385650551314, -9.790100578890868377, 49.79778022625163203 ) ) ;
#37180=CARTESIAN_POINT ( 'NONE',  ( -13.78034385759798752, -9.360768649639306105, 51.01397948905921709 ) ) ;
#37219=CARTESIAN_POINT ( 'NONE',  ( -14.08659385541304410, -7.222650657624104298, 49.61879703869476543 ) ) ;
#37227=CARTESIAN_POINT ( 'NONE',  ( -20.30534385759798965, -7.595227055684746986, 51.75156210489594599 ) ) ;
#37235=DIRECTION ( 'NONE',  ( 1.000000000000000000, 1.669677910507523057E-21, 6.493791346278465266E-22 ) ) ;
#37250=CARTESIAN_POINT ( 'NONE',  ( -20.83659385650551599, -6.915538690918074494, 49.31353937987644542 ) ) ;
#37261=DIRECTION ( 'NONE',  ( 1.000000000000000000, 1.669677910507523057E-21, 6.493791346278465266E-22 ) ) ;
#37264=ORIENTED_EDGE ( 'NONE', *, *, #9282, .T. ) ;
#37265=CARTESIAN_POINT ( 'NONE',  ( -14.19909385650551847, -8.114302828567740988, 52.18300498402516041 ) ) ;
#37267=( BOUNDED_CURVE ( )  B_SPLINE_CURVE ( 2, ( #23707, #16270, #796, #34027, #15300, #30364, #11629, #26655, #41676 ),
 .UNSPECIFIED., .F., .F. ) 
 B_SPLINE_CURVE_WITH_KNOTS ( ( 3, 2, 2, 2, 3 ),
 ( 3.223963992799358462E-49, 0.0009834168075315858487, 0.001966833615063171697, 0.002950250422594757546, 0.003933667230126343395 ),
 .UNSPECIFIED. ) 
 CURVE ( )  GEOMETRIC_REPRESENTATION_ITEM ( )  RATIONAL_B_SPLINE_CURVE ( ( 1.000000000000000000, 0.9238795325112867385, 1.000000000000000000, 0.9238795325112867385, 1.000000000000000000, 0.9238795325112867385, 1.000000000000000000, 0.9238795325113238199, 0.9999999999999629186 ) ) 
 REPRESENTATION_ITEM ( '' )  );
#37274=VERTEX_POINT ( 'NONE', #44554 ) ;
#37275=CARTESIAN_POINT ( 'NONE',  ( -16.36784385650551954, -6.428312510596451368, 51.20221977374900035 ) ) ;
#37279=CARTESIAN_POINT ( 'NONE',  ( -14.79284385650551670, -7.406986770994973490, 48.81910596585309747 ) ) ;
#37307=CARTESIAN_POINT ( 'NONE',  ( 18.57132275349405148, 1.810087817303917657, 49.27149739157786712 ) ) ;
#37343=DIRECTION ( 'NONE',  ( 1.000000000000000000, -4.164305804376849788E-17, 1.614929280266638808E-16 ) ) ;
#37345=CARTESIAN_POINT ( 'NONE',  ( -14.98659385650551457, -9.302874398569244363, 51.68646062012417985 ) ) ;
#37359=EDGE_CURVE ( 'NONE', #38445, #33928, #47166, .T. ) ;
#37370=ORIENTED_EDGE ( 'NONE', *, *, #649, .F. ) ;
#37383=CARTESIAN_POINT ( 'NONE',  ( -16.31159385759798752, -8.990409506049202193, 49.61344411288074951 ) ) ;
#37414=AXIS2_PLACEMENT_3D ( 'NONE', #48254, #21451, #29068 ) ;
#37422=CARTESIAN_POINT ( 'NONE',  ( -21.37409385650551741, -9.792211528768504536, 50.49490371617623197 ) ) ;
#37434=EDGE_CURVE ( 'NONE', #11000, #4941, #9468, .T. ) ;
#37454=EDGE_CURVE ( 'NONE', #1741, #46443, #47506, .T. ) ;
#37455=DIRECTION ( 'NONE',  ( 1.000000000000000000, 1.669677910507523057E-21, 6.493791346278465266E-22 ) ) ;
#37461=AXIS2_PLACEMENT_3D ( 'NONE', #30528, #41340, #719 ) ;
#37499=CARTESIAN_POINT ( 'NONE',  ( -18.36159385650551812, -9.295667164867525756, 49.30633214617472504 ) ) ;
#37505=LINE ( 'NONE', #3800, #39439 ) ;
#37512=CARTESIAN_POINT ( 'NONE',  ( -12.97364781899516650, -9.395219913213448848, 49.41431986088092998 ) ) ;
#37520=CARTESIAN_POINT ( 'NONE',  ( -14.00534385650551883, -8.801233750844183135, 48.81488406609782515 ) ) ;
#37523=CARTESIAN_POINT ( 'NONE',  ( -15.07409385650551670, -9.792211528768504536, 50.49490371617623197 ) ) ;
#37524=AXIS2_PLACEMENT_3D ( 'NONE', #24830, #25543, #2417 ) ;
#37526=ORIENTED_EDGE ( 'NONE', *, *, #26585, .F. ) ;
#37562=DIRECTION ( 'NONE',  ( 0.000000000000000000, -0.9999954153791273948, -0.003028072113819838245 ) ) ;
#37566=TOROIDAL_SURFACE ( 'NONE', #41527, 1.999999999999999112, 1.249999999999999334 ) ;
#37584=DIRECTION ( 'NONE',  ( -1.000000000000000000, -1.669677910507523057E-21, -6.493791346278465266E-22 ) ) ;
#37589=CARTESIAN_POINT ( 'NONE',  ( -15.32409385650551670, -6.426201560718813433, 50.50509628382439331 ) ) ;
#37618=DIRECTION ( 'NONE',  ( -7.236285704734400469E-17, 0.7640846180167337742, 0.6451160333693637394 ) ) ;
#37638=CARTESIAN_POINT ( 'NONE',  ( -13.61159385759799001, -8.990409506049202193, 49.61344411288074951 ) ) ;
#37663=DIRECTION ( 'NONE',  ( -1.616182858256117057E-16, -0.003028072113818697231, 0.9999954153791273948 ) ) ;
#37679=CARTESIAN_POINT ( 'NONE',  ( -19.40534385650551741, -8.801233750844183135, 48.81488406609782515 ) ) ;
#37716=CARTESIAN_POINT ( 'NONE',  ( 18.87590614458706995, 1.890747609047893185, 50.53028072113869484 ) ) ;
#37720=CARTESIAN_POINT ( 'NONE',  ( -15.04284385541304125, -7.587656875400194068, 49.25157356644813689 ) ) ;
#37731=CARTESIAN_POINT ( 'NONE',  ( -18.95534385759798823, -8.623186033802570094, 49.24843789510466507 ) ) ;
#37749=CARTESIAN_POINT ( 'NONE',  ( 18.62590614458706995, 1.890747609047893185, 50.53028072113869484 ) ) ;
#37753=CARTESIAN_POINT ( 'NONE',  ( -18.30534385650551599, -8.801233750844183135, 48.81488406609782515 ) ) ;
#37754=ORIENTED_EDGE ( 'NONE', *, *, #30003, .F. ) ;
#37757=ORIENTED_EDGE ( 'NONE', *, *, #41060, .F. ) ;
#37765=EDGE_CURVE ( 'NONE', #2504, #3256, #16316, .T. ) ;
#37768=ADVANCED_FACE ( 'NONE', ( #38743 ), #38984, .T. ) ;
#37771=CARTESIAN_POINT ( 'NONE',  ( -14.36784385650551954, -6.428312510596451368, 51.20221977374900035 ) ) ;
#37780=CARTESIAN_POINT ( 'NONE',  ( -15.35534385650551847, -7.417179338643134834, 52.18511593390279302 ) ) ;
#37784=CARTESIAN_POINT ( 'NONE',  ( -15.46784385650551918, -6.428312510596451368, 51.20221977374900035 ) ) ;
#37785=VECTOR ( 'NONE', #15333, 1000.000000000000114 ) ;
#37790=FACE_OUTER_BOUND ( 'NONE', #18077, .T. ) ;
#37799=AXIS2_PLACEMENT_3D ( 'NONE', #7389, #22389, #45304 ) ;
#37819=CARTESIAN_POINT ( 'NONE',  ( -14.53659385541304694, -8.995762431863209230, 51.38120296130584563 ) ) ;
#37823=FACE_OUTER_BOUND ( 'NONE', #29034, .T. ) ;
#37850=CARTESIAN_POINT ( 'NONE',  ( -16.05534385650551243, -7.417179338643134834, 52.18511593390279302 ) ) ;
#37868=EDGE_LOOP ( 'NONE', ( #7756, #41110, #38264 ) ) ;
#37873=CARTESIAN_POINT ( 'NONE',  ( 18.46573386768564973, 2.137037847100790255, 51.75577699556767897 ) ) ;
#37891=CARTESIAN_POINT ( 'NONE',  ( -19.40534385759799463, -7.595227055684746986, 51.75156210489594599 ) ) ;
#37894=CARTESIAN_POINT ( 'NONE',  ( -22.35534385650551670, -7.417179338643134834, 52.18511593390279302 ) ) ;
#37897=DIRECTION ( 'NONE',  ( 1.000000000000000000, -4.164305804376849172E-17, 1.614929280266638808E-16 ) ) ;
#37920=ORIENTED_EDGE ( 'NONE', *, *, #1683, .F. ) ;
#37929=CARTESIAN_POINT ( 'NONE',  ( -21.48659385650551457, -9.302874398569244363, 51.68646062012417985 ) ) ;
#37939=LINE ( 'NONE', #294, #36855 ) ;
#37942=ORIENTED_EDGE ( 'NONE', *, *, #31508, .T. ) ;
#37948=CARTESIAN_POINT ( 'NONE',  ( -21.31784385759798539, -6.860780111191487229, 51.02154966934377001 ) ) ;
#37996=CARTESIAN_POINT ( 'NONE',  ( -19.88034385650552238, -6.424090610841176385, 49.80797279389978627 ) ) ;
#38010=CARTESIAN_POINT ( 'NONE',  ( -14.08659385650551776, -9.302874398569244363, 51.68646062012417985 ) ) ;
#38017=CARTESIAN_POINT ( 'NONE',  ( -14.79284385650551670, -7.406986770994973490, 48.81910596585309747 ) ) ;
#38022=CARTESIAN_POINT ( 'NONE',  ( -14.06159385650551741, -9.295667164867525756, 49.30633214617472504 ) ) ;
#38025=FACE_OUTER_BOUND ( 'NONE', #19400, .T. ) ;
#38042=( BOUNDED_CURVE ( )  B_SPLINE_CURVE ( 2, ( #22235, #6497, #14324, #37227, #40226, #32815, #47849, #33527, #14086 ),
 .UNSPECIFIED., .F., .F. ) 
 B_SPLINE_CURVE_WITH_KNOTS ( ( 3, 2, 2, 2, 3 ),
 ( 0.2083333333333331761, 0.2187499999999998890, 0.2291666666666666297, 0.2395833333333333703, 0.2500000000000001110 ),
 .UNSPECIFIED. ) 
 CURVE ( )  GEOMETRIC_REPRESENTATION_ITEM ( )  RATIONAL_B_SPLINE_CURVE ( ( 1.000000000000001110, 0.9238795325112855172, 1.000000000000000000, 0.9238795325112867385, 1.000000000000000000, 0.9238795325112867385, 1.000000000000000000, 0.9238795325112859613, 1.000000000000000888 ) ) 
 REPRESENTATION_ITEM ( '' )  );
#38054=CARTESIAN_POINT ( 'NONE',  ( -14.81784385541216587, -6.860780111197240849, 51.02154966934948277 ) ) ;
#38063=ORIENTED_EDGE ( 'NONE', *, *, #17429, .F. ) ;
#38072=CARTESIAN_POINT ( 'NONE',  ( -19.88034385541303450, -9.360768649639323868, 51.01397948905923130 ) ) ;
#38082=CARTESIAN_POINT ( 'NONE',  ( -20.27409385541325904, -6.859212275519745106, 50.50378509014061734 ) ) ;
#38085=CARTESIAN_POINT ( 'NONE',  ( -14.59284385650551563, -7.406986770994973490, 48.81910596585309747 ) ) ;
#38091=FACE_OUTER_BOUND ( 'NONE', #41201, .T. ) ;
#38127=CARTESIAN_POINT ( 'NONE',  ( -22.74909385650551386, -8.104110260919577868, 48.81699501597546487 ) ) ;
#38130=CARTESIAN_POINT ( 'NONE',  ( -14.23034385759798859, -6.857644439848010975, 49.98602051094140108 ) ) ;
#38149=EDGE_CURVE ( 'NONE', #46061, #4040, #25127, .T. ) ;
#38151=PLANE ( 'NONE',  #21795 ) ;
#38158=CARTESIAN_POINT ( 'NONE',  ( -16.98659385759799179, -7.222650657624104298, 49.61879703869476543 ) ) ;
#38162=CARTESIAN_POINT ( 'NONE',  ( -16.70534385650551812, -8.801233750844183135, 48.81488406609782515 ) ) ;
#38174=ORIENTED_EDGE ( 'NONE', *, *, #865, .F. ) ;
#38180=CARTESIAN_POINT ( 'NONE',  ( -21.37409385759799108, -6.859212275519751323, 50.50378509014259265 ) ) ;
#38188=CARTESIAN_POINT ( 'NONE',  ( 10.57590614458695377, 3.114729847419844599, 50.78398819077492732 ) ) ;
#38200=( BOUNDED_CURVE ( )  B_SPLINE_CURVE ( 2, ( #21284, #36996, #36281, #36739, #21527, #44195, #32822, #10443, #14565 ),
 .UNSPECIFIED., .F., .F. ) 
 B_SPLINE_CURVE_WITH_KNOTS ( ( 3, 2, 2, 2, 3 ),
 ( 0.02360435172767372594, 0.02458795513743799663, 0.02557155854720226038, 0.02655516195696652759, 0.02753876536673079828 ),
 .UNSPECIFIED. ) 
 CURVE ( )  GEOMETRIC_REPRESENTATION_ITEM ( )  RATIONAL_B_SPLINE_CURVE ( ( 0.9999999999999431566, 0.9238795325113435819, 1.000000000000000000, 0.9238795325112867385, 1.000000000000000000, 0.9238795325112867385, 1.000000000000000000, 0.9238795325108709600, 1.000000000000415890 ) ) 
 REPRESENTATION_ITEM ( '' )  );
#38212=ORIENTED_EDGE ( 'NONE', *, *, #39825, .F. ) ;
#38224=DIRECTION ( 'NONE',  ( 1.000000000000000000, 1.669677910507523057E-21, 6.493791346278465266E-22 ) ) ;
#38229=CARTESIAN_POINT ( 'NONE',  ( -21.51159385650551670, -6.922745924619793101, 51.69366785382590024 ) ) ;
#38250=EDGE_LOOP ( 'NONE', ( #32700, #18880, #3363, #7844, #40071, #36299, #33108, #18369, #17306, #9544, #8091, #43852 ) ) ;
#38252=CARTESIAN_POINT ( 'NONE',  ( -22.35534385541304658, -8.623186033802570094, 49.24843789510466507 ) ) ;
#38255=ADVANCED_FACE ( 'NONE', ( #18943 ), #30532, .T. ) ;
#38262=CIRCLE ( 'NONE', #44581, 1.249999999999999334 ) ;
#38264=ORIENTED_EDGE ( 'NONE', *, *, #21291, .T. ) ;
#38286=EDGE_CURVE ( 'NONE', #27510, #42061, #10470, .T. ) ;
#38305=CARTESIAN_POINT ( 'NONE',  ( -19.82409385541304303, -9.359200813967568422, 50.49621490985803263 ) ) ;
#38311=CARTESIAN_POINT ( 'NONE',  ( -20.92409385650551812, -6.426201560718813433, 50.50509628382439331 ) ) ;
#38319=CARTESIAN_POINT ( 'NONE',  ( -15.99909385650551741, -8.114302828567740988, 52.18300498402516041 ) ) ;
#38320=ORIENTED_EDGE ( 'NONE', *, *, #29716, .T. ) ;
#38354=CIRCLE ( 'NONE', #21849, 1.249999999999999334 ) ;
#38362=CARTESIAN_POINT ( 'NONE',  ( -13.16159385759798894, -7.228003583438117552, 51.38655588711986155 ) ) ;
#38363=CARTESIAN_POINT ( 'NONE',  ( 10.57590614458695377, 3.140741878271521514, 50.53406581128081143 ) ) ;
#38404=CARTESIAN_POINT ( 'NONE',  ( -18.67409385650551457, -9.792211528768504536, 50.49490371617623197 ) ) ;
#38443=CARTESIAN_POINT ( 'NONE',  ( -22.07409385650551670, -9.792211528768504536, 50.49490371617623197 ) ) ;
#38445=VERTEX_POINT ( 'NONE', #47480 ) ;
#38455=CARTESIAN_POINT ( 'NONE',  ( -13.49909385759798930, -8.105421454601382081, 49.25000573077640098 ) ) ;
#38481=CARTESIAN_POINT ( 'NONE',  ( -14.87409385650551741, -9.792211528768504536, 50.49490371617623197 ) ) ;
#38494=( BOUNDED_CURVE ( )  B_SPLINE_CURVE ( 2, ( #44901, #15063, #33278, #7474, #30120, #18274, #22729, #47842, #7712 ),
 .UNSPECIFIED., .F., .F. ) 
 B_SPLINE_CURVE_WITH_KNOTS ( ( 3, 2, 2, 2, 3 ),
 ( 0.6249999999999998890, 0.6354166666666665186, 0.6458333333333332593, 0.6562499999999998890, 0.6666666666666665186 ),
 .UNSPECIFIED. ) 
 CURVE ( )  GEOMETRIC_REPRESENTATION_ITEM ( )  RATIONAL_B_SPLINE_CURVE ( ( 1.000000000000000888, 0.9238795325112859613, 1.000000000000000000, 0.9238795325112867385, 1.000000000000000000, 0.9238795325112867385, 1.000000000000000000, 0.9238795325112875156, 0.9999999999999992228 ) ) 
 REPRESENTATION_ITEM ( '' )  );
#38496=AXIS2_PLACEMENT_3D ( 'NONE', #16187, #30994, #19671 ) ;
#38510=CARTESIAN_POINT ( 'NONE',  ( -23.08659385541304587, -7.222650657624104298, 49.61879703869476543 ) ) ;
#38517=DIRECTION ( 'NONE',  ( 6.374839753205896285E-22, 0.007114381193220324640, -0.9999746924698832418 ) ) ;
#38547=CARTESIAN_POINT ( 'NONE',  ( -16.67409385541329669, -6.859212275519744217, 50.50378509014024075 ) ) ;
#38554=ORIENTED_EDGE ( 'NONE', *, *, #21274, .F. ) ;
#38566=CARTESIAN_POINT ( 'NONE',  ( -22.33034385650551812, -9.794322478646142471, 51.19202720610083901 ) ) ;
#38572=CARTESIAN_POINT ( 'NONE',  ( -13.24284385650551599, -8.811426318492348031, 52.18089403414752070 ) ) ;
#38584=CARTESIAN_POINT ( 'NONE',  ( -20.72409385541304161, -9.359200813967568422, 50.49621490985803263 ) ) ;
#38606=DIRECTION ( 'NONE',  ( -1.616182858256117057E-16, -0.003028072113818697231, 0.9999954153791273948 ) ) ;
#38610=PRODUCT_DEFINITION_CONTEXT ( 'detailed design', #6119, 'design' ) ;
#38620=CARTESIAN_POINT ( 'NONE',  ( -19.12409385759799108, -9.359200813967568422, 50.49621490985803263 ) ) ;
#38622=CARTESIAN_POINT ( 'NONE',  ( -21.11784385650551954, -9.790100578890868377, 49.79778022625163203 ) ) ;
#38627=ORIENTED_EDGE ( 'NONE', *, *, #45144, .T. ) ;
#38639=LINE ( 'NONE', #26843, #46139 ) ;
#38663=CARTESIAN_POINT ( 'NONE',  ( -16.22409385541304871, -9.359200813967568422, 50.49621490985801842 ) ) ;
#38664=CARTESIAN_POINT ( 'NONE',  ( -17.15534385650551741, -7.417179338643134834, 52.18511593390279302 ) ) ;
#38667=DIRECTION ( 'NONE',  ( 0.000000000000000000, 0.9999954153791273948, 0.003028072113819836077 ) ) ;
#38682=CARTESIAN_POINT ( 'NONE',  ( -21.71159385759798965, -8.990409506049200417, 49.61344411288074951 ) ) ;
#38696=CARTESIAN_POINT ( 'NONE',  ( -22.35534385650551670, -7.417179338643134834, 52.18511593390279302 ) ) ;
#38715=CARTESIAN_POINT ( 'NONE',  ( -18.24909385541303664, -8.112991634885936776, 51.74999426922422430 ) ) ;
#38722=CARTESIAN_POINT ( 'NONE',  ( -36.42409385541304800, -8.109206544743658540, 50.50000000000030553 ) ) ;
#38730=CARTESIAN_POINT ( 'NONE',  ( -14.81784385650551705, -9.790100578890868377, 49.79778022625163203 ) ) ;
#38742=ORIENTED_EDGE ( 'NONE', *, *, #41580, .F. ) ;
#38743=FACE_OUTER_BOUND ( 'NONE', #24184, .T. ) ;
#38756=CARTESIAN_POINT ( 'NONE',  ( -20.78034385541304374, -9.360768649639302552, 51.01397948905921709 ) ) ;
#38765=( BOUNDED_CURVE ( )  B_SPLINE_CURVE ( 2, ( #17535, #6224, #47591, #20758, #5508, #17762, #6472, #9690, #9445 ),
 .UNSPECIFIED., .F., .F. ) 
 B_SPLINE_CURVE_WITH_KNOTS ( ( 3, 2, 2, 2, 3 ),
 ( 0.03934058936362840042, 0.04032418838537540212, 0.04130778740712241076, 0.04229138642886941940, 0.04327498545061642110 ),
 .UNSPECIFIED. ) 
 CURVE ( )  GEOMETRIC_REPRESENTATION_ITEM ( )  RATIONAL_B_SPLINE_CURVE ( ( 1.000000000000098144, 0.9238795325111885948, 1.000000000000000000, 0.9238795325112867385, 1.000000000000000000, 0.9238795325112867385, 1.000000000000000000, 0.9238795325114607104, 0.9999999999998260281 ) ) 
 REPRESENTATION_ITEM ( '' )  );
#38766=EDGE_CURVE ( 'NONE', #16419, #2504, #32468, .T. ) ;
#38775=EDGE_CURVE ( 'NONE', #24436, #15477, #19230, .T. ) ;
#38779=DIRECTION ( 'NONE',  ( 0.000000000000000000, 1.000000000000000000, 3.469446951953614189E-15 ) ) ;
#38792=DIRECTION ( 'NONE',  ( 1.000000000000000000, -4.164305804376849172E-17, 1.614929280266638808E-16 ) ) ;
#38807=CARTESIAN_POINT ( 'NONE',  ( -21.73659385541302314, -8.995762431863237651, 51.38120296130587406 ) ) ;
#38815=CARTESIAN_POINT ( 'NONE',  ( -20.69909385650551670, -8.114302828567740988, 52.18300498402516041 ) ) ;
#38820=ORIENTED_EDGE ( 'NONE', *, *, #27753, .F. ) ;
#38821=CARTESIAN_POINT ( 'NONE',  ( -20.92409385650551812, -6.426201560718813433, 50.50509628382439331 ) ) ;
#38850=EDGE_CURVE ( 'NONE', #44349, #35620, #42058, .T. ) ;
#38857=AXIS2_PLACEMENT_3D ( 'NONE', #39716, #42697, #46135 ) ;
#38861=CIRCLE ( 'NONE', #5058, 1.250000000000001998 ) ;
#38867=CARTESIAN_POINT ( 'NONE',  ( -21.39909385650551599, -8.114302828567740988, 52.18300498402516041 ) ) ;
#38902=CARTESIAN_POINT ( 'NONE',  ( -15.63659385650551670, -6.915538690918075382, 49.31353937987644542 ) ) ;
#38922=CARTESIAN_POINT ( 'NONE',  ( -21.82409385759798681, -9.359200813967568422, 50.49621490985803263 ) ) ;
#38942=EDGE_CURVE ( 'NONE', #16853, #24862, #12322, .T. ) ;
#38972=CARTESIAN_POINT ( 'NONE',  ( -15.54909385650551634, -8.104110260919579645, 48.81699501597546487 ) ) ;
#38974=EDGE_CURVE ( 'NONE', #3630, #29446, #42650, .T. ) ;
#38984=CYLINDRICAL_SURFACE ( 'NONE', #38857, 1.249999999999998668 ) ;
#38997=CARTESIAN_POINT ( 'NONE',  ( -22.24284385541303877, -7.587656875400192291, 49.25157356644813689 ) ) ;
#39046=ORIENTED_EDGE ( 'NONE', *, *, #10091, .F. ) ;
#39047=CARTESIAN_POINT ( 'NONE',  ( -20.75534385650551528, -7.417179338643134834, 52.18511593390279302 ) ) ;
#39053=CARTESIAN_POINT ( 'NONE',  ( -13.41159385650551528, -6.922745924619793101, 51.69366785382590024 ) ) ;
#39055=ADVANCED_FACE ( 'NONE', ( #24166 ), #45051, .T. ) ;
#39101=VECTOR ( 'NONE', #45642, 1000.000000000000000 ) ;
#39102=CARTESIAN_POINT ( 'NONE',  ( -17.96784385650551741, -6.428312510596451368, 51.20221977374900035 ) ) ;
#39141=CARTESIAN_POINT ( 'NONE',  ( -16.36784385650551954, -6.428312510596451368, 51.20221977374900035 ) ) ;
#39161=CARTESIAN_POINT ( 'NONE',  ( -17.77409385759798965, -6.859212275519751323, 50.50378509014259265 ) ) ;
#39218=CARTESIAN_POINT ( 'NONE',  ( -17.91159385650551528, -6.922745924619793101, 51.69366785382590024 ) ) ;
#39244=ORIENTED_EDGE ( 'NONE', *, *, #41951, .F. ) ;
#39246=CARTESIAN_POINT ( 'NONE',  ( -19.88034385541304871, -9.360768649639302552, 51.01397948905922419 ) ) ;
#39297=ORIENTED_EDGE ( 'NONE', *, *, #31680, .T. ) ;
#39299=CARTESIAN_POINT ( 'NONE',  ( -23.00534385650551528, -8.801233750844183135, 48.81488406609782515 ) ) ;
#39306=CARTESIAN_POINT ( 'NONE',  ( -13.58034385650551812, -6.424090610841176385, 49.80797279389977916 ) ) ;
#39349=CARTESIAN_POINT ( 'NONE',  ( 18.57590614458695200, 0.6299963676414561675, 50.77646420411990391 ) ) ;
#39352=CARTESIAN_POINT ( 'NONE',  ( -17.29284385650551670, -7.406986770994973490, 48.81910596585309747 ) ) ;
#39374=VECTOR ( 'NONE', #16554, 1000.000000000000000 ) ;
#39413=CARTESIAN_POINT ( 'NONE',  ( -18.56159385759799108, -7.228003583438117552, 51.38655588711986155 ) ) ;
#39425=DIRECTION ( 'NONE',  ( -4.115385489420004910E-17, -0.9999954153791273948, -0.003028072113811714535 ) ) ;
#39439=VECTOR ( 'NONE', #18552, 1000.000000000000227 ) ;
#39446=CARTESIAN_POINT ( 'NONE',  ( 22.62590614458706639, 1.890747609047893185, 50.53028072113869484 ) ) ;
#39463=CARTESIAN_POINT ( 'NONE',  ( -15.77409385650551954, -9.792211528768504536, 50.49490371617623197 ) ) ;
#39469=ORIENTED_EDGE ( 'NONE', *, *, #44277, .T. ) ;
#39491=CARTESIAN_POINT ( 'NONE',  ( -17.68659385541304374, -7.222650657624104298, 49.61879703869476543 ) ) ;
#39492=CARTESIAN_POINT ( 'NONE',  ( 18.57590614458695200, 2.144561833755798563, 49.27104351578929453 ) ) ;
#39495=ADVANCED_FACE ( 'NONE', ( #30592 ), #34749, .T. ) ;
#39510=DIRECTION ( 'NONE',  ( 0.000000000000000000, 0.9999954153791273948, 0.003028072113819836077 ) ) ;
#39528=DIRECTION ( 'NONE',  ( -4.115385489420004294E-17, -0.9999954153791273948, -0.003028072113811714535 ) ) ;
#39541=CARTESIAN_POINT ( 'NONE',  ( -19.40534385650551741, -8.801233750844183135, 48.81488406609782515 ) ) ;
#39544=CARTESIAN_POINT ( 'NONE',  ( -22.21784385650551741, -9.790100578890868377, 49.79778022625163203 ) ) ;
#39546=ORIENTED_EDGE ( 'NONE', *, *, #39883, .F. ) ;
#39589=CARTESIAN_POINT ( 'NONE',  ( -18.58659385650551599, -9.302874398569244363, 51.68646062012417985 ) ) ;
#39601=CARTESIAN_POINT ( 'NONE',  ( -22.58034385541118994, -9.360768649651129536, 51.01397948904742208 ) ) ;
#39603=DIRECTION ( 'NONE',  ( 0.000000000000000000, -0.007114381193220190198, 0.9999746924698832418 ) ) ;
#39605=CARTESIAN_POINT ( 'NONE',  ( -21.45534385650551812, -7.417179338643134834, 52.18511593390279302 ) ) ;
#39610=CARTESIAN_POINT ( 'NONE',  ( 18.07590614458695200, 1.637417875877629436, 51.62951866002712364 ) ) ;
#39626=CIRCLE ( 'NONE', #8292, 1.249999999999999556 ) ;
#39632=CARTESIAN_POINT ( 'NONE',  ( -13.72409385650551528, -6.426201560718813433, 50.50509628382439331 ) ) ;
#39650=CARTESIAN_POINT ( 'NONE',  ( -19.23659385759798823, -8.995762431863214559, 51.38120296130585274 ) ) ;
#39667=AXIS2_PLACEMENT_3D ( 'NONE', #41094, #42317, #8839 ) ;
#39669=ORIENTED_EDGE ( 'NONE', *, *, #12709, .T. ) ;
#39695=ORIENTED_EDGE ( 'NONE', *, *, #9350, .F. ) ;
#39703=CIRCLE ( 'NONE', #36545, 1.249999999999999556 ) ;
#39716=CARTESIAN_POINT ( 'NONE',  ( -36.42409385541304800, -8.109206544743658540, 50.50000000000030553 ) ) ;
#39721=CARTESIAN_POINT ( 'NONE',  ( -21.96159385541302811, -7.228003583438094459, 51.38655588711988287 ) ) ;
#39727=VERTEX_POINT ( 'NONE', #13711 ) ;
#39729=CARTESIAN_POINT ( 'NONE',  ( -19.43034385541304232, -6.857644439848013640, 49.98602051094139398 ) ) ;
#39741=ORIENTED_EDGE ( 'NONE', *, *, #16596, .T. ) ;
#39762=CARTESIAN_POINT ( 'NONE',  ( -17.12409385541300111, -9.359200813967566646, 50.49621490985766314 ) ) ;
#39776=CARTESIAN_POINT ( 'NONE',  ( 18.54465614458695555, 3.140996361033564721, 50.45002501377945947 ) ) ;
#39780=CARTESIAN_POINT ( 'NONE',  ( -19.85534385650552025, -7.417179338643134834, 52.18511593390279302 ) ) ;
#39784=CARTESIAN_POINT ( 'NONE',  ( -19.34909385650551883, -8.104110260919579645, 48.81699501597546487 ) ) ;
#39796=CARTESIAN_POINT ( 'NONE',  ( -19.71159385541296061, -8.990409506049296340, 49.61344411288065714 ) ) ;
#39802=DIRECTION ( 'NONE',  ( 1.000000000000000000, 1.669677910507523057E-21, 6.493791346278465266E-22 ) ) ;
#39815=FACE_OUTER_BOUND ( 'NONE', #17558, .T. ) ;
#39825=EDGE_CURVE ( 'NONE', #17695, #12464, #8600, .T. ) ;
#39828=EDGE_LOOP ( 'NONE', ( #5837, #1453, #35338 ) ) ;
#39830=DIRECTION ( 'NONE',  ( -4.115385489419834196E-17, -0.9999954153791273948, -0.003028072113822188795 ) ) ;
#39831=CARTESIAN_POINT ( 'NONE',  ( -17.91159385650551528, -6.922745924619793101, 51.69366785382590024 ) ) ;
#39847=CARTESIAN_POINT ( 'NONE',  ( -20.10534385650551670, -8.801233750844183135, 48.81488406609782515 ) ) ;
#39853=CARTESIAN_POINT ( 'NONE',  ( -35.42409385541304800, -9.159201730891741278, 50.49682052428079970 ) ) ;
#39880=DIRECTION ( 'NONE',  ( -1.000000000000000000, -1.669677910507523057E-21, -6.493791346278465266E-22 ) ) ;
#39883=EDGE_CURVE ( 'NONE', #17695, #31311, #16633, .T. ) ;
#39891=CARTESIAN_POINT ( 'NONE',  ( -17.94284385759799605, -7.587656875400192291, 49.25157356644813689 ) ) ;
#39936=CARTESIAN_POINT ( 'NONE',  ( -36.42409385541304800, -9.359200813967566646, 50.49621490985803263 ) ) ;
#39943=CARTESIAN_POINT ( 'NONE',  ( -13.69284385650552061, -7.406986770994972602, 48.81910596585309747 ) ) ;
#39952=CARTESIAN_POINT ( 'NONE',  ( -13.49909385650551563, -8.114302828567740988, 52.18300498402516041 ) ) ;
#39967=EDGE_CURVE ( 'NONE', #27510, #20955, #28931, .T. ) ;
#39974=CARTESIAN_POINT ( 'NONE',  ( -17.96784385541304374, -9.357632978295830739, 49.97845033065684106 ) ) ;
#39979=VECTOR ( 'NONE', #24595, 1000.000000000000000 ) ;
#39983=ORIENTED_EDGE ( 'NONE', *, *, #21291, .F. ) ;
#40006=CARTESIAN_POINT ( 'NONE',  ( -22.13034385650551883, -9.794322478646142471, 51.19202720610083190 ) ) ;
#40034=CARTESIAN_POINT ( 'NONE',  ( -18.33659385650551243, -6.915538690918075382, 49.31353937987644542 ) ) ;
#40035=DIRECTION ( 'NONE',  ( 0.3047757271037812021, -0.9524197806957002133, -0.002884009000665106303 ) ) ;
#40038=CARTESIAN_POINT ( 'NONE',  ( -19.57409385650551670, -9.792211528768504536, 50.49490371617623197 ) ) ;
#40043=ORIENTED_EDGE ( 'NONE', *, *, #18878, .T. ) ;
#40071=ORIENTED_EDGE ( 'NONE', *, *, #4262, .T. ) ;
#40074=VERTEX_POINT ( 'NONE', #33831 ) ;
#40087=TOROIDAL_SURFACE ( 'NONE', #23576, 1.899999999999999911, 0.1000000000000000056 ) ;
#40099=CARTESIAN_POINT ( 'NONE',  ( -21.00534385650551883, -8.801233750844183135, 48.81488406609782515 ) ) ;
#40123=CARTESIAN_POINT ( 'NONE',  ( 18.57590614458695200, 2.136931092028981460, 51.79103196254469310 ) ) ;
#40124=CARTESIAN_POINT ( 'NONE',  ( -13.55534385650551243, -7.417179338643134834, 52.18511593390279302 ) ) ;
#40135=CLOSED_SHELL ( 'NONE', ( #16477, #30672, #18461, #4989, #7526, #42078, #30367, #24158, #22971, #11962, #15126, #19568, #14978, #20783, #40160, #31719, #1422, #12605, #11998, #38255, #5660, #35590, #36009, #34264, #11423, #13258, #46839, #41901, #37768, #47130, #30430, #17478, #17142, #43866, #6424, #7154, #39495, #14410, #34709, #25016, #15567, #33800, #41912, #35227, #27066, #24761, #2539, #44754, #34935, #5573, #13923, #32200, #25678, #19375, #11111, #30880, #22232, #13266, #43589, #39055, #14627, #14678, #16904, #48680 ) ) ;
#40142=CARTESIAN_POINT ( 'NONE',  ( -20.58659385759798965, -7.222650657624104298, 49.61879703869476543 ) ) ;
#40159=ORIENTED_EDGE ( 'NONE', *, *, #37454, .F. ) ;
#40160=ADVANCED_FACE ( 'NONE', ( #8473 ), #41723, .T. ) ;
#40169=( BOUNDED_CURVE ( )  B_SPLINE_CURVE ( 1, ( #24755, #47157 ),
 .UNSPECIFIED., .F., .F. ) 
 B_SPLINE_CURVE_WITH_KNOTS ( ( 2, 2 ),
 ( 0.000000000000000000, 1.000000000000000000 ),
 .UNSPECIFIED. ) 
 CURVE ( )  GEOMETRIC_REPRESENTATION_ITEM ( )  RATIONAL_B_SPLINE_CURVE ( ( 0.9847253504145836445, 0.9847253504145836445 ) ) 
 REPRESENTATION_ITEM ( '' )  );
#40173=ORIENTED_EDGE ( 'NONE', *, *, #7715, .F. ) ;
#40180=CARTESIAN_POINT ( 'NONE',  ( -23.11784385650551954, -9.790100578890868377, 49.79778022625162492 ) ) ;
#40182=CARTESIAN_POINT ( 'NONE',  ( 18.82590614458706924, 1.890747609047893185, 50.53028072113869484 ) ) ;
#40221=CARTESIAN_POINT ( 'NONE',  ( -19.65534385541304019, -8.623186033802570094, 49.24843789510466507 ) ) ;
#40223=LINE ( 'NONE', #39492, #36614 ) ;
#40226=CARTESIAN_POINT ( 'NONE',  ( -20.24909385759799108, -8.112991634885936776, 51.74999426922421719 ) ) ;
#40246=AXIS2_PLACEMENT_3D ( 'NONE', #40182, #18234, #36685 ) ;
#40275=CARTESIAN_POINT ( 'NONE',  ( -19.06784385650551528, -6.428312510596451368, 51.20221977374900035 ) ) ;
#40279=CARTESIAN_POINT ( 'NONE',  ( -18.39284385650552167, -7.406986770994973490, 48.81910596585309747 ) ) ;
#40333=CARTESIAN_POINT ( 'NONE',  ( -18.19284385650551883, -7.406986770994973490, 48.81910596585309747 ) ) ;
#40355=LINE ( 'NONE', #40123, #45478 ) ;
#40356=CARTESIAN_POINT ( 'NONE',  ( -13.89284385650552167, -7.406986770994972602, 48.81910596585309747 ) ) ;
#40357=ORIENTED_EDGE ( 'NONE', *, *, #3019, .T. ) ;
#40376=CARTESIAN_POINT ( 'NONE',  ( -16.36784385759798965, -9.357632978295830739, 49.97845033065684106 ) ) ;
#40378=DIRECTION ( 'NONE',  ( 1.000000000000000000, -4.164305804376849172E-17, 1.614929280266638808E-16 ) ) ;
#40384=EDGE_CURVE ( 'NONE', #44513, #28707, #4149, .T. ) ;
#40395=VECTOR ( 'NONE', #20511, 1000.000000000000000 ) ;
#40404=CARTESIAN_POINT ( 'NONE',  ( 8.575906144586953772, 1.671029476340948561, 40.52956954931881484 ) ) ;
#40426=ORIENTED_EDGE ( 'NONE', *, *, #7715, .T. ) ;
#40448=CARTESIAN_POINT ( 'NONE',  ( -18.86784385541304943, -9.357632978295830739, 49.97845033065684106 ) ) ;
#40474=FACE_OUTER_BOUND ( 'NONE', #17196, .T. ) ;
#40483=CARTESIAN_POINT ( 'NONE',  ( 10.57590614458695377, 1.890747609047612521, 50.53028072113853142 ) ) ;
#40485=DIRECTION ( 'NONE',  ( 0.000000000000000000, 0.007114381193220334181, -0.9999746924698833528 ) ) ;
#40489=ORIENTED_EDGE ( 'NONE', *, *, #11385, .T. ) ;
#40501=CARTESIAN_POINT ( 'NONE',  ( -18.28034385650551741, -6.424090610841176385, 49.80797279389977916 ) ) ;
#40504=CARTESIAN_POINT ( 'NONE',  ( -20.30534385650551243, -8.801233750844183135, 48.81488406609782515 ) ) ;
#40517=CARTESIAN_POINT ( 'NONE',  ( -17.12409385541300111, -9.359200813967566646, 50.49621490985766314 ) ) ;
#40563=CARTESIAN_POINT ( 'NONE',  ( -17.96784385650551741, -6.428312510596451368, 51.20221977374900035 ) ) ;
#40570=EDGE_LOOP ( 'NONE', ( #16668, #48100, #41301, #26383 ) ) ;
#40601=CARTESIAN_POINT ( 'NONE',  ( -15.29909385759798823, -8.105421454601382081, 49.25000573077640098 ) ) ;
#40622=ORIENTED_EDGE ( 'NONE', *, *, #48391, .F. ) ;
#40642=CARTESIAN_POINT ( 'NONE',  ( -19.74284385650551599, -8.811426318492348031, 52.18089403414751359 ) ) ;
#40685=CARTESIAN_POINT ( 'NONE',  ( -15.66159385541304339, -7.228003583438117552, 51.38655588711986155 ) ) ;
#40718=AXIS2_PLACEMENT_3D ( 'NONE', #32554, #47355, #28627 ) ;
#40728=DIRECTION ( 'NONE',  ( 1.000000000000000000, -4.164305804376849788E-17, 1.614929280266638808E-16 ) ) ;
#40732=ORIENTED_EDGE ( 'NONE', *, *, #34835, .T. ) ;
#40734=CARTESIAN_POINT ( 'NONE',  ( -19.65534385650552451, -7.417179338643134834, 52.18511593390279302 ) ) ;
#40744=CARTESIAN_POINT ( 'NONE',  ( -13.49909385650551563, -8.114302828567740988, 52.18300498402516041 ) ) ;
#40746=CARTESIAN_POINT ( 'NONE',  ( 18.54465614458695910, 0.6410078225857483991, 50.44245483349490655 ) ) ;
#40749=CARTESIAN_POINT ( 'NONE',  ( -20.19284385650551528, -7.406986770994973490, 48.81910596585309747 ) ) ;
#40763=CARTESIAN_POINT ( 'NONE',  ( -17.57409385541300395, -6.859212275519753099, 50.50378509014294792 ) ) ;
#40781=LINE ( 'NONE', #22560, #15566 ) ;
#40812=CARTESIAN_POINT ( 'NONE',  ( -19.43034385650552309, -9.794322478646142471, 51.19202720610083901 ) ) ;
#40852=EDGE_LOOP ( 'NONE', ( #25988, #31032, #24699, #21532 ) ) ;
#40857=CARTESIAN_POINT ( 'NONE',  ( -15.01784385759799356, -6.860780111191487229, 51.02154966934377711 ) ) ;
#40868=ORIENTED_EDGE ( 'NONE', *, *, #1578, .F. ) ;
#40894=CARTESIAN_POINT ( 'NONE',  ( -22.10534385650552025, -8.801233750844183135, 48.81488406609782515 ) ) ;
#40902=DIRECTION ( 'NONE',  ( 0.000000000000000000, 0.9999954153791273948, 0.003028072113820366902 ) ) ;
#40912=CARTESIAN_POINT ( 'NONE',  ( -13.55534385650551243, -7.417179338643134834, 52.18511593390279302 ) ) ;
#40920=AXIS2_PLACEMENT_3D ( 'NONE', #42212, #5033, #27676 ) ;
#40930=CARTESIAN_POINT ( 'NONE',  ( 6.575906144586949331, -6.109215713985405749, 50.50605614422795497 ) ) ;
#40936=CARTESIAN_POINT ( 'NONE',  ( -13.80534385541303877, -7.595227055684746986, 51.75156210489594599 ) ) ;
#40943=CIRCLE ( 'NONE', #23672, 1.749999999999997558 ) ;
#40956=CARTESIAN_POINT ( 'NONE',  ( 18.87590614458706995, 1.890747609047893185, 50.53028072113869484 ) ) ;
#40973=CARTESIAN_POINT ( 'NONE',  ( -20.94909385650551670, -8.104110260919577868, 48.81699501597546487 ) ) ;
#40989=CARTESIAN_POINT ( 'NONE',  ( -16.33659385650551599, -6.915538690918074494, 49.31353937987644542 ) ) ;
#40992=CARTESIAN_POINT ( 'NONE',  ( 18.82590614458706924, 1.890747609047893185, 50.53028072113869484 ) ) ;
#40995=CARTESIAN_POINT ( 'NONE',  ( -22.04909385759799179, -8.112991634885936776, 51.74999426922421719 ) ) ;
#41000=CARTESIAN_POINT ( 'NONE',  ( -13.17364594312814852, -9.395205385347631832, 49.41430265251966603 ) ) ;
#41005=CARTESIAN_POINT ( 'NONE',  ( -15.52409385650551421, -6.426201560718813433, 50.50509628382439331 ) ) ;
#41036=CARTESIAN_POINT ( 'NONE',  ( -14.70534385541304800, -7.595227055684751427, 51.75156210489594599 ) ) ;
#41048=EDGE_LOOP ( 'NONE', ( #15873, #21484, #32371, #13991 ) ) ;
#41060=EDGE_CURVE ( 'NONE', #31825, #46443, #46099, .T. ) ;
#41067=CARTESIAN_POINT ( 'NONE',  ( -15.54909385650551634, -8.104110260919579645, 48.81699501597546487 ) ) ;
#41073=PLANE ( 'NONE',  #36828 ) ;
#41094=CARTESIAN_POINT ( 'NONE',  ( -36.42409385541304800, -8.109206544743658540, 50.50000000000030553 ) ) ;
#41101=CARTESIAN_POINT ( 'NONE',  ( -19.57409385759799036, -6.859212275519751323, 50.50378509014259265 ) ) ;
#41103=FACE_OUTER_BOUND ( 'NONE', #40570, .T. ) ;
#41105=CARTESIAN_POINT ( 'NONE',  ( -15.24284385759798788, -7.587656875400194068, 49.25157356644813689 ) ) ;
#41110=ORIENTED_EDGE ( 'NONE', *, *, #38974, .T. ) ;
#41143=CARTESIAN_POINT ( 'NONE',  ( -19.79909385650551457, -8.114302828567740988, 52.18300498402516041 ) ) ;
#41146=CARTESIAN_POINT ( 'NONE',  ( -13.72409385759798894, -9.359200813967568422, 50.49621490985803263 ) ) ;
#41152=DIRECTION ( 'NONE',  ( 0.000000000000000000, -0.9999954153791273948, -0.003028072113819836944 ) ) ;
#41170=EDGE_CURVE ( 'NONE', #29820, #20335, #9127, .T. ) ;
#41175=( BOUNDED_CURVE ( )  B_SPLINE_CURVE ( 2, ( #29361, #44633, #44393 ),
 .UNSPECIFIED., .F., .F. ) 
 B_SPLINE_CURVE_WITH_KNOTS ( ( 3, 3 ),
 ( 0.9166666666666666297, 0.9259045776023205887 ),
 .UNSPECIFIED. ) 
 CURVE ( )  GEOMETRIC_REPRESENTATION_ITEM ( )  RATIONAL_B_SPLINE_CURVE ( ( 1.000000000000000000, 0.9324933664920571630, 0.9847218244232577300 ) ) 
 REPRESENTATION_ITEM ( '' )  );
#41177=CARTESIAN_POINT ( 'NONE',  ( -21.17409385541299116, -6.859212275519752211, 50.50378509014304029 ) ) ;
#41182=CARTESIAN_POINT ( 'NONE',  ( -14.81784385541304339, -6.860780111191487229, 51.02154966934377711 ) ) ;
#41201=EDGE_LOOP ( 'NONE', ( #3367, #20092 ) ) ;
#41212=CARTESIAN_POINT ( 'NONE',  ( -18.64284385650552167, -8.811426318492348031, 52.18089403414751359 ) ) ;
#41226=CARTESIAN_POINT ( 'NONE',  ( -13.13034385650551883, -9.794322478646142471, 51.19202720610083901 ) ) ;
#41234=CARTESIAN_POINT ( 'NONE',  ( -14.23034385650551492, -9.794322478646142471, 51.19202720610083901 ) ) ;
#41239=CARTESIAN_POINT ( 'NONE',  ( -15.91784385650552025, -9.790100578890868377, 49.79778022625163203 ) ) ;
#41266=DIRECTION ( 'NONE',  ( 1.000000000000000000, -4.164305804376849788E-17, 1.614929280266638808E-16 ) ) ;
#41300=CARTESIAN_POINT ( 'NONE',  ( -14.03034385650551563, -9.794322478646142471, 51.19202720610083901 ) ) ;
#41301=ORIENTED_EDGE ( 'NONE', *, *, #6116, .F. ) ;
#41340=DIRECTION ( 'NONE',  ( 0.3047757271037810356, -0.002884009000655191491, 0.9524197806957002133 ) ) ;
#41342=CARTESIAN_POINT ( 'NONE',  ( -13.78034385759799108, -9.360768649639302552, 51.01397948905922419 ) ) ;
#41359=CARTESIAN_POINT ( 'NONE',  ( -14.98659385541304445, -7.222650657624106962, 49.61879703869476543 ) ) ;
#41376=CARTESIAN_POINT ( 'NONE',  ( 23.52590614458706852, 1.876518846661452411, 52.53023010607846288 ) ) ;
#41380=CARTESIAN_POINT ( 'NONE',  ( -19.63034385650552238, -9.794322478646142471, 51.19202720610083190 ) ) ;
#41407=CARTESIAN_POINT ( 'NONE',  ( 18.57590614458706924, 2.144455078683968452, 49.30629848276639393 ) ) ;
#41419=AXIS2_PLACEMENT_3D ( 'NONE', #7155, #11331, #26342 ) ;
#41436=ORIENTED_EDGE ( 'NONE', *, *, #36722, .T. ) ;
#41444=CARTESIAN_POINT ( 'NONE',  ( 18.57590614458706924, 0.6652513346187085563, 50.77657095919166608 ) ) ;
#41452=CARTESIAN_POINT ( 'NONE',  ( -18.58659385650551599, -9.302874398569244363, 51.68646062012417985 ) ) ;
#41470=CARTESIAN_POINT ( 'NONE',  ( -15.15534385650552096, -7.417179338643134834, 52.18511593390279302 ) ) ;
#41475=EDGE_LOOP ( 'NONE', ( #15314, #40357, #23637, #15672 ) ) ;
#41478=CARTESIAN_POINT ( 'NONE',  ( -14.73659385650551457, -6.915538690918075382, 49.31353937987644542 ) ) ;
#41481=CARTESIAN_POINT ( 'NONE',  ( -14.73659385650551457, -6.915538690918075382, 49.31353937987644542 ) ) ;
#41487=DIRECTION ( 'NONE',  ( 0.000000000000000000, -0.9999954153791273948, -0.003028072113819838245 ) ) ;
#41488=VECTOR ( 'NONE', #26193, 1000.000000000000114 ) ;
#41489=DIRECTION ( 'NONE',  ( -1.674255585786183705E-21, 0.9999746924698832418, 0.007114381193220235301 ) ) ;
#41490=EDGE_CURVE ( 'NONE', #13929, #38445, #40223, .T. ) ;
#41527=AXIS2_PLACEMENT_3D ( 'NONE', #14830, #4045, #14581 ) ;
#41529=EDGE_CURVE ( 'NONE', #12464, #16419, #38494, .T. ) ;
#41540=CARTESIAN_POINT ( 'NONE',  ( -18.98034385541304303, -9.360768649638925964, 51.01397948905978552 ) ) ;
#41544=( BOUNDED_CURVE ( )  B_SPLINE_CURVE ( 1, ( #14097, #2567 ),
 .UNSPECIFIED., .F., .F. ) 
 B_SPLINE_CURVE_WITH_KNOTS ( ( 2, 2 ),
 ( 0.000000000000000000, 1.000000000000000000 ),
 .UNSPECIFIED. ) 
 CURVE ( )  GEOMETRIC_REPRESENTATION_ITEM ( )  RATIONAL_B_SPLINE_CURVE ( ( 0.9847233224627454096, 0.9847233224627454096 ) ) 
 REPRESENTATION_ITEM ( '' )  );
#41552=CARTESIAN_POINT ( 'NONE',  ( -15.60534385650551847, -8.801233750844183135, 48.81488406609782515 ) ) ;
#41556=CARTESIAN_POINT ( 'NONE',  ( 18.57590614458695200, 0.6315104036983664182, 50.27646649643033783 ) ) ;
#41557=CIRCLE ( 'NONE', #44696, 1.250000000000001998 ) ;
#41580=EDGE_CURVE ( 'NONE', #501, #9159, #15383, .T. ) ;
#41597=CARTESIAN_POINT ( 'NONE',  ( -21.51159385650551670, -6.922745924619793101, 51.69366785382590024 ) ) ;
#41604=ORIENTED_EDGE ( 'NONE', *, *, #25555, .T. ) ;
#41609=ORIENTED_EDGE ( 'NONE', *, *, #9276, .T. ) ;
#41616=CARTESIAN_POINT ( 'NONE',  ( -14.87409385541153917, -6.859212275519794844, 50.50378509015643402 ) ) ;
#41623=DIRECTION ( 'NONE',  ( 1.000000000000000000, -4.164305804376849172E-17, 1.614929280266638808E-16 ) ) ;
#41635=CARTESIAN_POINT ( 'NONE',  ( -21.59909385650551528, -8.114302828567740988, 52.18300498402516041 ) ) ;
#41647=VERTEX_POINT ( 'NONE', #12596 ) ;
#41659=DIRECTION ( 'NONE',  ( 1.000000000000000000, -4.164305804376849788E-17, 1.614929280266638808E-16 ) ) ;
#41666=CARTESIAN_POINT ( 'NONE',  ( -33.42409385541304800, -6.859212275519750435, 50.50378509014258555 ) ) ;
#41671=CARTESIAN_POINT ( 'NONE',  ( -15.32409385541304303, -9.359200813967568422, 50.49621490985803263 ) ) ;
#41674=EDGE_CURVE ( 'NONE', #19332, #16810, #37267, .T. ) ;
#41676=CARTESIAN_POINT ( 'NONE',  ( -22.97409385541299542, -6.859212275519753099, 50.50378509014307582 ) ) ;
#41691=DIRECTION ( 'NONE',  ( 1.000000000000000000, -4.164305804376849788E-17, 1.614929280266638808E-16 ) ) ;
#41698=VECTOR ( 'NONE', #41691, 1000.000000000000000 ) ;
#41708=CARTESIAN_POINT ( 'NONE',  ( -20.66784385650552025, -6.428312510596449592, 51.20221977374900035 ) ) ;
#41715=CARTESIAN_POINT ( 'NONE',  ( -21.59909385759798894, -8.105421454601382081, 49.25000573077640098 ) ) ;
#41722=CARTESIAN_POINT ( 'NONE',  ( -16.44909385650551670, -8.104110260919579645, 48.81699501597546487 ) ) ;
#41723=CYLINDRICAL_SURFACE ( 'NONE', #46831, 1.249999999999998668 ) ;
#41724=FACE_OUTER_BOUND ( 'NONE', #32678, .T. ) ;
#41729=CARTESIAN_POINT ( 'NONE',  ( -16.42409385650551812, -6.426201560718813433, 50.50509628382439331 ) ) ;
#41736=CARTESIAN_POINT ( 'NONE',  ( -14.23034385650551492, -9.794322478646142471, 51.19202720610083901 ) ) ;
#41768=ORIENTED_EDGE ( 'NONE', *, *, #35181, .F. ) ;
#41771=CARTESIAN_POINT ( 'NONE',  ( -14.36784385541283982, -9.357632978295985282, 49.97845033065656395 ) ) ;
#41787=VECTOR ( 'NONE', #21272, 1000.000000000000000 ) ;
#41798=CIRCLE ( 'NONE', #15001, 0.1000000000000000056 ) ;
#41803=CARTESIAN_POINT ( 'NONE',  ( -16.11159385650551457, -6.922745924619793101, 51.69366785382590024 ) ) ;
#41818=ORIENTED_EDGE ( 'NONE', *, *, #3191, .T. ) ;
#41822=CARTESIAN_POINT ( 'NONE',  ( 22.62590614458706639, 1.890747609047893185, 50.53028072113869484 ) ) ;
#41824=CARTESIAN_POINT ( 'NONE',  ( -22.72409385759798894, -9.359200813967568422, 50.49621490985803263 ) ) ;
#41847=CARTESIAN_POINT ( 'NONE',  ( -20.72409385650551883, -6.426201560718812544, 50.50509628382439331 ) ) ;
#41884=CARTESIAN_POINT ( 'NONE',  ( -18.78659385650551528, -9.302874398569244363, 51.68646062012417985 ) ) ;
#41889=CARTESIAN_POINT ( 'NONE',  ( -16.67409385541329669, -6.859212275519744217, 50.50378509014024075 ) ) ;
#41899=CARTESIAN_POINT ( 'NONE',  ( -21.93659385759799108, -8.995762431863214559, 51.38120296130585274 ) ) ;
#41901=ADVANCED_FACE ( 'NONE', ( #44344 ), #25855, .T. ) ;
#41912=ADVANCED_FACE ( 'NONE', ( #48251 ), #6898, .T. ) ;
#41935=CARTESIAN_POINT ( 'NONE',  ( -18.30534385541304232, -7.595227055684743434, 51.75156210489596020 ) ) ;
#41938=CARTESIAN_POINT ( 'NONE',  ( -36.42409385541304800, -8.109206544743658540, 50.50000000000030553 ) ) ;
#41951=EDGE_CURVE ( 'NONE', #29468, #4941, #38639, .T. ) ;
#41952=CARTESIAN_POINT ( 'NONE',  ( -18.86784385650552309, -6.428312510596451368, 51.20221977374900035 ) ) ;
#41959=DIRECTION ( 'NONE',  ( 1.000000000000000000, -4.164305804376849172E-17, 1.614929280266638808E-16 ) ) ;
#41976=ORIENTED_EDGE ( 'NONE', *, *, #31358, .T. ) ;
#41977=CARTESIAN_POINT ( 'NONE',  ( -22.41159385541304161, -8.990409506049200417, 49.61344411288074951 ) ) ;
#42000=ORIENTED_EDGE ( 'NONE', *, *, #36181, .T. ) ;
#42029=ORIENTED_EDGE ( 'NONE', *, *, #12473, .F. ) ;
#42039=CARTESIAN_POINT ( 'NONE',  ( -14.19909385650551847, -8.114302828567740988, 52.18300498402516041 ) ) ;
#42058=CIRCLE ( 'NONE', #28698, 1.900000000000000133 ) ;
#42061=VERTEX_POINT ( 'NONE', #31251 ) ;
#42066=DIRECTION ( 'NONE',  ( 4.115385489419892128E-17, 0.9999954153791273948, 0.003028072113818697231 ) ) ;
#42078=ADVANCED_FACE ( 'NONE', ( #28538 ), #47247, .T. ) ;
#42081=DIRECTION ( 'NONE',  ( 0.000000000000000000, 1.000000000000000000, 5.551115123125785858E-15 ) ) ;
#42082=CARTESIAN_POINT ( 'NONE',  ( -22.18659385650551741, -9.302874398569244363, 51.68646062012417985 ) ) ;
#42089=ORIENTED_EDGE ( 'NONE', *, *, #19746, .T. ) ;
#42097=VECTOR ( 'NONE', #28693, 1000.000000000000000 ) ;
#42121=CARTESIAN_POINT ( 'NONE',  ( -18.33659385650551243, -6.915538690918075382, 49.31353937987644542 ) ) ;
#42127=FACE_BOUND ( 'NONE', #31807, .T. ) ;
#42141=CARTESIAN_POINT ( 'NONE',  ( -20.69909385759799036, -8.105421454601382081, 49.25000573077640098 ) ) ;
#42151=LINE ( 'NONE', #38188, #13236 ) ;
#42159=CARTESIAN_POINT ( 'NONE',  ( -22.24284385650551954, -8.811426318492348031, 52.18089403414751359 ) ) ;
#42190=DIRECTION ( 'NONE',  ( -1.000000000000000000, -1.669677910507523057E-21, -6.493791346278465266E-22 ) ) ;
#42191=CARTESIAN_POINT ( 'NONE',  ( -17.18034385650551954, -6.424090610841176385, 49.80797279389978627 ) ) ;
#42212=CARTESIAN_POINT ( 'NONE',  ( 8.575906144586951996, 11.89145878086734065, 50.31056258843197782 ) ) ;
#42216=CARTESIAN_POINT ( 'NONE',  ( -23.36784385541304232, -9.357632978295830739, 49.97845033065684106 ) ) ;
#42226=DIRECTION ( 'NONE',  ( -4.115385489419834812E-17, -0.9999954153791275058, -0.003028072113822189229 ) ) ;
#42266=VERTEX_POINT ( 'NONE', #3148 ) ;
#42283=CARTESIAN_POINT ( 'NONE',  ( -13.18659385650551918, -9.302874398569244363, 51.68646062012417985 ) ) ;
#42291=CARTESIAN_POINT ( 'NONE',  ( -20.89284385541298761, -8.630756214087167422, 51.74842643355258076 ) ) ;
#42298=DIRECTION ( 'NONE',  ( 0.000000000000000000, 0.9999954153791273948, 0.003028072113819836077 ) ) ;
#42302=CIRCLE ( 'NONE', #32855, 1.700000000000001954 ) ;
#42317=DIRECTION ( 'NONE',  ( 1.000000000000000000, -4.164305804376849172E-17, 1.614929280266638808E-16 ) ) ;
#42326=DIRECTION ( 'NONE',  ( -1.000000000000000000, 4.164305804376849172E-17, -1.614929280266638808E-16 ) ) ;
#42327=CARTESIAN_POINT ( 'NONE',  ( -20.38659385650551670, -9.302874398569244363, 51.68646062012417985 ) ) ;
#42338=AXIS2_PLACEMENT_3D ( 'NONE', #40483, #40728, #22266 ) ;
#42367=CARTESIAN_POINT ( 'NONE',  ( -17.83034385650552167, -9.794322478646142471, 51.19202720610083190 ) ) ;
#42370=AXIS2_PLACEMENT_3D ( 'NONE', #20709, #47049, #17236 ) ;
#42378=DIRECTION ( 'NONE',  ( 0.000000000000000000, 0.007114381193220285608, -0.9999746924698833528 ) ) ;
#42388=CIRCLE ( 'NONE', #10141, 1.249999999999999556 ) ;
#42406=CARTESIAN_POINT ( 'NONE',  ( -22.52409385650551954, -6.426201560718812544, 50.50509628382439331 ) ) ;
#42434=CARTESIAN_POINT ( 'NONE',  ( 18.82590614458706924, 1.890747609047893185, 50.53028072113869484 ) ) ;
#42435=FACE_OUTER_BOUND ( 'NONE', #23656, .T. ) ;
#42441=CARTESIAN_POINT ( 'NONE',  ( -16.61784385650551954, -9.790100578890868377, 49.79778022625163203 ) ) ;
#42458=VECTOR ( 'NONE', #6402, 1000.000000000000000 ) ;
#42466=CARTESIAN_POINT ( 'NONE',  ( -21.06159385541304374, -7.228003583438117552, 51.38655588711986155 ) ) ;
#42479=CARTESIAN_POINT ( 'NONE',  ( -33.42409385541304800, -9.359200813967566646, 50.49621490985803263 ) ) ;
#42487=CARTESIAN_POINT ( 'NONE',  ( -19.63034385759798894, -6.857644439848014528, 49.98602051094138687 ) ) ;
#42533=CARTESIAN_POINT ( 'NONE',  ( -13.69284385650552061, -7.406986770994973490, 48.81910596585309747 ) ) ;
#42556=ORIENTED_EDGE ( 'NONE', *, *, #9282, .F. ) ;
#42558=PRODUCT ( 'Speed Governor Worm Gear Train', 'Speed Governor Worm Gear Train', '', ( #26982 ) ) ;
#42572=ORIENTED_EDGE ( 'NONE', *, *, #20848, .F. ) ;
#42585=CARTESIAN_POINT ( 'NONE',  ( -21.84909385650551528, -8.104110260919577868, 48.81699501597546487 ) ) ;
#42599=ORIENTED_EDGE ( 'NONE', *, *, #29935, .T. ) ;
#42603=CARTESIAN_POINT ( 'NONE',  ( -36.42409385541304800, -8.109206544743658540, 50.50000000000030553 ) ) ;
#42621=CARTESIAN_POINT ( 'NONE',  ( -16.48034385650551670, -6.424090610841176385, 49.80797279389978627 ) ) ;
#42630=CARTESIAN_POINT ( 'NONE',  ( 18.62590614458706995, 1.890747609047893185, 50.53028072113869484 ) ) ;
#42650=LINE ( 'NONE', #1991, #7484 ) ;
#42655=CARTESIAN_POINT ( 'NONE',  ( -21.79284385650551314, -7.406986770994973490, 48.81910596585309747 ) ) ;
#42685=CARTESIAN_POINT ( 'NONE',  ( -16.67409385650551812, -9.792211528768504536, 50.49490371617623197 ) ) ;
#42690=VERTEX_POINT ( 'NONE', #43175 ) ;
#42697=DIRECTION ( 'NONE',  ( 1.000000000000000000, -4.164305804376849172E-17, 1.614929280266638808E-16 ) ) ;
#42713=CARTESIAN_POINT ( 'NONE',  ( -20.33034385541304800, -6.857644439848013640, 49.98602051094139398 ) ) ;
#42728=ORIENTED_EDGE ( 'NONE', *, *, #649, .T. ) ;
#42757=CARTESIAN_POINT ( 'NONE',  ( -16.36784385759798965, -9.357632978295836068, 49.97845033065684106 ) ) ;
#42764=CARTESIAN_POINT ( 'NONE',  ( -23.06159385650551386, -9.295667164867525756, 49.30633214617472504 ) ) ;
#42769=CARTESIAN_POINT ( 'NONE',  ( -22.04909385650551457, -8.104110260919577868, 48.81699501597546487 ) ) ;
#42804=AXIS2_PLACEMENT_3D ( 'NONE', #23668, #9621, #43593 ) ;
#42810=CARTESIAN_POINT ( 'NONE',  ( -20.10534385650551670, -8.801233750844183135, 48.81488406609782515 ) ) ;
#42829=CARTESIAN_POINT ( 'NONE',  ( -13.69284385541286753, -8.630756214087254463, 51.74842643355279392 ) ) ;
#42851=CARTESIAN_POINT ( 'NONE',  ( -17.88659385650551670, -9.302874398569244363, 51.68646062012417985 ) ) ;
#42863=ORIENTED_EDGE ( 'NONE', *, *, #16755, .F. ) ;
#42869=CARTESIAN_POINT ( 'NONE',  ( -18.44909385759799036, -8.112991634885936776, 51.74999426922421719 ) ) ;
#42918=CARTESIAN_POINT ( 'NONE',  ( -16.56159385650551386, -9.295667164867525756, 49.30633214617472504 ) ) ;
#42941=CARTESIAN_POINT ( 'NONE',  ( -21.11784385541304943, -6.860780111191487229, 51.02154966934377001 ) ) ;
#42986=ORIENTED_EDGE ( 'NONE', *, *, #29940, .F. ) ;
#42994=CARTESIAN_POINT ( 'NONE',  ( -20.58659385650551599, -9.302874398569244363, 51.68646062012417985 ) ) ;
#42999=CARTESIAN_POINT ( 'NONE',  ( -22.78034385650551741, -6.424090610841176385, 49.80797279389977916 ) ) ;
#43007=CARTESIAN_POINT ( 'NONE',  ( -21.11784385541296061, -6.860780111191562725, 51.02154966934399027 ) ) ;
#43020=VERTEX_POINT ( 'NONE', #8258 ) ;
#43023=EDGE_CURVE ( 'NONE', #43233, #20025, #30434, .T. ) ;
#43027=DIRECTION ( 'NONE',  ( 1.000000000000000000, -4.164305804376849172E-17, 1.614929280266638808E-16 ) ) ;
#43045=CARTESIAN_POINT ( 'NONE',  ( -18.98034385650551670, -6.424090610841176385, 49.80797279389977916 ) ) ;
#43060=CARTESIAN_POINT ( 'NONE',  ( 8.575906144586951996, -6.109215713985405749, 50.50605614422795497 ) ) ;
#43074=CARTESIAN_POINT ( 'NONE',  ( -22.55534385759798965, -8.623186033802570094, 49.24843789510466507 ) ) ;
#43096=ORIENTED_EDGE ( 'NONE', *, *, #22500, .F. ) ;
#43103=CARTESIAN_POINT ( 'NONE',  ( -19.29284385759799036, -8.630756214087126565, 51.74842643355248129 ) ) ;
#43118=CARTESIAN_POINT ( 'NONE',  ( 18.54465614458695200, 0.6407533398237036382, 50.52649563099625851 ) ) ;
#43120=CARTESIAN_POINT ( 'NONE',  ( 8.575906144586953772, 2.171027184030513979, 40.53108358537571831 ) ) ;
#43130=FACE_OUTER_BOUND ( 'NONE', #3766, .T. ) ;
#43145=EDGE_CURVE ( 'NONE', #28258, #48324, #27925, .T. ) ;
#43151=CIRCLE ( 'NONE', #18747, 1.249999999999999556 ) ;
#43161=CARTESIAN_POINT ( 'NONE',  ( -16.33659385650551599, -6.915538690918074494, 49.31353937987644542 ) ) ;
#43175=CARTESIAN_POINT ( 'NONE',  ( 18.57590614458706924, 3.151498850453803957, 50.28409723815717314 ) ) ;
#43189=AXIS2_PLACEMENT_3D ( 'NONE', #13551, #47316, #20962 ) ;
#43192=CARTESIAN_POINT ( 'NONE',  ( -18.13659385541304303, -8.995762431863214559, 51.38120296130585274 ) ) ;
#43196=VECTOR ( 'NONE', #38792, 1000.000000000000000 ) ;
#43203=CARTESIAN_POINT ( 'NONE',  ( -36.42409385541304800, -6.859212275519750435, 50.50378509014258555 ) ) ;
#43233=VERTEX_POINT ( 'NONE', #17793 ) ;
#43251=CARTESIAN_POINT ( 'NONE',  ( -22.55534385650551599, -7.417179338643134834, 52.18511593390279302 ) ) ;
#43256=( BOUNDED_CURVE ( )  B_SPLINE_CURVE ( 2, ( #30154, #44935, #22505, #48599, #30396, #4056, #10939, #22020, #3541 ),
 .UNSPECIFIED., .F., .F. ) 
 B_SPLINE_CURVE_WITH_KNOTS ( ( 3, 2, 2, 2, 3 ),
 ( 0.1250000000000000555, 0.1354166666666666852, 0.1458333333333333703, 0.1562500000000000000, 0.1666666666666666297 ),
 .UNSPECIFIED. ) 
 CURVE ( )  GEOMETRIC_REPRESENTATION_ITEM ( )  RATIONAL_B_SPLINE_CURVE ( ( 0.9999999999999995559, 0.9238795325112871826, 1.000000000000000000, 0.9238795325112867385, 1.000000000000000000, 0.9238795325112867385, 1.000000000000000000, 0.9238795325112869605, 0.9999999999999997780 ) ) 
 REPRESENTATION_ITEM ( '' )  );
#43257=CARTESIAN_POINT ( 'NONE',  ( -23.17409385650551457, -9.792211528768504536, 50.49490371617623197 ) ) ;
#43300=CARTESIAN_POINT ( 'NONE',  ( -17.85534385650552025, -7.417179338643134834, 52.18511593390279302 ) ) ;
#43314=CARTESIAN_POINT ( 'NONE',  ( -22.91784385541302882, -6.860780111191215447, 51.02154966934360658 ) ) ;
#43331=CIRCLE ( 'NONE', #44922, 1.949999999999999734 ) ;
#43341=CARTESIAN_POINT ( 'NONE',  ( -15.29909385650551634, -8.114302828567740988, 52.18300498402516041 ) ) ;
#43344=CARTESIAN_POINT ( 'NONE',  ( -20.47409385759799250, -6.859212275519751323, 50.50378509014259265 ) ) ;
#43363=CARTESIAN_POINT ( 'NONE',  ( -17.09909385759799250, -8.105421454601382081, 49.25000573077640098 ) ) ;
#43396=ORIENTED_EDGE ( 'NONE', *, *, #40384, .F. ) ;
#43398=CARTESIAN_POINT ( 'NONE',  ( -18.22409385759798894, -9.359200813967568422, 50.49621490985803263 ) ) ;
#43399=PLANE ( 'NONE',  #6893 ) ;
#43403=CARTESIAN_POINT ( 'NONE',  ( -22.78034385650551741, -6.424090610841176385, 49.80797279389978627 ) ) ;
#43416=CARTESIAN_POINT ( 'NONE',  ( -13.97409385650551528, -9.792211528768506312, 50.49490371617623197 ) ) ;
#43417=VERTEX_POINT ( 'NONE', #29877 ) ;
#43428=DIRECTION ( 'NONE',  ( 1.000000000000000000, -4.164305804376849172E-17, 1.614929280266638808E-16 ) ) ;
#43439=CARTESIAN_POINT ( 'NONE',  ( -18.47409385541304161, -6.859212275519751323, 50.50378509014259265 ) ) ;
#43463=CARTESIAN_POINT ( 'NONE',  ( -17.57409385541300395, -6.859212275519753099, 50.50378509014294792 ) ) ;
#43496=CARTESIAN_POINT ( 'NONE',  ( -18.05534385650551599, -7.417179338643134834, 52.18511593390279302 ) ) ;
#43500=CARTESIAN_POINT ( 'NONE',  ( -19.74284385650551599, -8.811426318492348031, 52.18089403414751359 ) ) ;
#43544=CARTESIAN_POINT ( 'NONE',  ( -16.95534385650551812, -7.417179338643134834, 52.18511593390279302 ) ) ;
#43560=CARTESIAN_POINT ( 'NONE',  ( -21.17409385650551812, -9.792211528768504536, 50.49490371617623197 ) ) ;
#43564=PLANE ( 'NONE',  #33157 ) ;
#43569=DIRECTION ( 'NONE',  ( 0.000000000000000000, 0.9999954153791273948, 0.003028072113819836077 ) ) ;
#43571=LINE ( 'NONE', #24617, #46206 ) ;
#43581=CARTESIAN_POINT ( 'NONE',  ( -14.79284385759798859, -8.630756214087126565, 51.74842643355248129 ) ) ;
#43586=CARTESIAN_POINT ( 'NONE',  ( -14.96159385650551776, -9.295667164867525756, 49.30633214617472504 ) ) ;
#43589=ADVANCED_FACE ( 'NONE', ( #11577 ), #38151, .F. ) ;
#43593=DIRECTION ( 'NONE',  ( 4.115385489419834812E-17, 0.9999954153791273948, 0.003028072113822188795 ) ) ;
#43596=DIRECTION ( 'NONE',  ( -1.000000000000000000, 4.164305804376849172E-17, -1.614929280266638808E-16 ) ) ;
#43597=EDGE_CURVE ( 'NONE', #3423, #27443, #30068, .T. ) ;
#43599=VERTEX_POINT ( 'NONE', #7170 ) ;
#43602=ORIENTED_EDGE ( 'NONE', *, *, #1575, .F. ) ;
#43604=CARTESIAN_POINT ( 'NONE',  ( -19.01159385759799036, -8.990409506049200417, 49.61344411288074951 ) ) ;
#43623=CARTESIAN_POINT ( 'NONE',  ( 18.62590614458706995, 0.6407533398239845246, 50.52649563099625851 ) ) ;
#43644=CARTESIAN_POINT ( 'NONE',  ( 18.57590614458706924, 3.116243883476995880, 50.28399048308531860 ) ) ;
#43653=CARTESIAN_POINT ( 'NONE',  ( -17.94284385759799250, -7.587656875400192291, 49.25157356644813689 ) ) ;
#43662=DIRECTION ( 'NONE',  ( -1.000000000000000000, 4.164305804376849172E-17, -1.614929280266638808E-16 ) ) ;
#43683=CARTESIAN_POINT ( 'NONE',  ( -18.30534385541304232, -7.595227055684746986, 51.75156210489594599 ) ) ;
#43702=CARTESIAN_POINT ( 'NONE',  ( 18.57590614458706924, 0.6667653706756797582, 50.27657325150221368 ) ) ;
#43723=CARTESIAN_POINT ( 'NONE',  ( -18.02409385541303877, -9.359200813967568422, 50.49621490985803263 ) ) ;
#43725=ORIENTED_EDGE ( 'NONE', *, *, #1349, .F. ) ;
#43736=CARTESIAN_POINT ( 'NONE',  ( -19.34909385650551883, -8.104110260919579645, 48.81699501597546487 ) ) ;
#43741=CARTESIAN_POINT ( 'NONE',  ( -19.91159385650551528, -6.922745924619793101, 51.69366785382590024 ) ) ;
#43794=EDGE_CURVE ( 'NONE', #19879, #29515, #43571, .T. ) ;
#43801=CARTESIAN_POINT ( 'NONE',  ( -19.31784385650551528, -9.790100578890868377, 49.79778022625163203 ) ) ;
#43812=FACE_OUTER_BOUND ( 'NONE', #21223, .T. ) ;
#43819=AXIS2_PLACEMENT_3D ( 'NONE', #34252, #30593, #15783 ) ;
#43828=CARTESIAN_POINT ( 'NONE',  ( -14.34284385650551741, -8.811426318492348031, 52.18089403414752070 ) ) ;
#43835=ORIENTED_EDGE ( 'NONE', *, *, #36722, .F. ) ;
#43847=CARTESIAN_POINT ( 'NONE',  ( -19.18034385759799321, -9.360768649639302552, 51.01397948905922419 ) ) ;
#43849=DIRECTION ( 'NONE',  ( -1.669677910507523245E-21, 1.000000000000000000, -1.084253996632606407E-42 ) ) ;
#43852=ORIENTED_EDGE ( 'NONE', *, *, #7915, .F. ) ;
#43866=ADVANCED_FACE ( 'NONE', ( #43812 ), #16947, .T. ) ;
#43892=ORIENTED_EDGE ( 'NONE', *, *, #19931, .T. ) ;
#43899=CARTESIAN_POINT ( 'NONE',  ( -13.63659385650551847, -6.915538690918075382, 49.31353937987644542 ) ) ;
#43928=CARTESIAN_POINT ( 'NONE',  ( -17.12409385541304374, -9.359200813967568422, 50.49621490985803263 ) ) ;
#43933=FACE_OUTER_BOUND ( 'NONE', #15220, .T. ) ;
#43945=CARTESIAN_POINT ( 'NONE',  ( -13.52409385541304410, -9.359200813967568422, 50.49621490985803263 ) ) ;
#43949=CARTESIAN_POINT ( 'NONE',  ( -12.97364571557156232, -9.395203622806569399, 49.41430056510258595 ) ) ;
#43957=DIRECTION ( 'NONE',  ( 1.000000000000000000, 1.669677910507523057E-21, 6.493791346278465266E-22 ) ) ;
#43982=CARTESIAN_POINT ( 'NONE',  ( -21.99284385759798965, -8.630756214087126565, 51.74842643355248129 ) ) ;
#43983=VERTEX_POINT ( 'NONE', #30005 ) ;
#43985=CARTESIAN_POINT ( 'NONE',  ( -17.99909385650551741, -8.114302828567740988, 52.18300498402516041 ) ) ;
#43990=CARTESIAN_POINT ( 'NONE',  ( -20.53034385650551386, -9.794322478646142471, 51.19202720610083901 ) ) ;
#43991=( BOUNDED_CURVE ( )  B_SPLINE_CURVE ( 2, ( #40763, #18098, #7537, #36559, #29444, #36805, #33114, #22544, #40517 ),
 .UNSPECIFIED., .F., .F. ) 
 B_SPLINE_CURVE_WITH_KNOTS ( ( 3, 2, 2, 2, 3 ),
 ( 0.05114234498029770343, 0.05212596529054528555, 0.05310958560079286073, 0.05409320591104042897, 0.05507682622128801109 ),
 .UNSPECIFIED. ) 
 CURVE ( )  GEOMETRIC_REPRESENTATION_ITEM ( )  RATIONAL_B_SPLINE_CURVE ( ( 0.9999999999995229372, 0.9238795325117638013, 1.000000000000000000, 0.9238795325112867385, 1.000000000000000000, 0.9238795325112867385, 1.000000000000000000, 0.9238795325105971790, 1.000000000000689671 ) ) 
 REPRESENTATION_ITEM ( '' )  );
#43992=ORIENTED_EDGE ( 'NONE', *, *, #34835, .F. ) ;
#44006=EDGE_LOOP ( 'NONE', ( #37370, #37526, #16949, #15700, #6354 ) ) ;
#44009=CARTESIAN_POINT ( 'NONE',  ( -17.06784385541249094, -9.357632978292226511, 49.97845033065324571 ) ) ;
#44035=CIRCLE ( 'NONE', #3123, 0.09999999999999939493 ) ;
#44054=CARTESIAN_POINT ( 'NONE',  ( -20.72409385650551883, -6.426201560718812544, 50.50509628382439331 ) ) ;
#44058=DIRECTION ( 'NONE',  ( -0.9524241471993248886, 0.0009228828802128809673, -0.3047743298226214259 ) ) ;
#44080=CARTESIAN_POINT ( 'NONE',  ( -13.49909385650551563, -8.114302828567740988, 52.18300498402516041 ) ) ;
#44097=CARTESIAN_POINT ( 'NONE',  ( -14.79284385759798859, -8.630756214087126565, 51.74842643355248129 ) ) ;
#44109=AXIS2_PLACEMENT_3D ( 'NONE', #15094, #42190, #34793 ) ;
#44122=ORIENTED_EDGE ( 'NONE', *, *, #13388, .F. ) ;
#44164=FACE_BOUND ( 'NONE', #29905, .T. ) ;
#44180=CARTESIAN_POINT ( 'NONE',  ( -19.14909385541304232, -8.112991634885936776, 51.74999426922421719 ) ) ;
#44195=CARTESIAN_POINT ( 'NONE',  ( -20.44284385541303095, -7.587656875400184298, 49.25157356644812268 ) ) ;
#44202=CIRCLE ( 'NONE', #27653, 1.249999999999999334 ) ;
#44210=VECTOR ( 'NONE', #48204, 1000.000000000000114 ) ;
#44230=CARTESIAN_POINT ( 'NONE',  ( -17.04284385650551670, -8.811426318492348031, 52.18089403414751359 ) ) ;
#44231=DIRECTION ( 'NONE',  ( -0.9524241471993249997, -0.3047743298226212594, -0.0009228828802129952422 ) ) ;
#44232=CYLINDRICAL_SURFACE ( 'NONE', #33915, 1.249999999999998668 ) ;
#44233=CARTESIAN_POINT ( 'NONE',  ( -19.12409385650551741, -6.426201560718813433, 50.50509628382439331 ) ) ;
#44247=CARTESIAN_POINT ( 'NONE',  ( -16.89909385541303877, -8.105421454601382081, 49.25000573077640098 ) ) ;
#44261=ORIENTED_EDGE ( 'NONE', *, *, #47231, .T. ) ;
#44277=EDGE_CURVE ( 'NONE', #43233, #26444, #42302, .T. ) ;
#44280=CARTESIAN_POINT ( 'NONE',  ( -13.21784385759799108, -6.860780111191489006, 51.02154966934379132 ) ) ;
#44285=CARTESIAN_POINT ( 'NONE',  ( -17.32409385759798681, -9.359200813967568422, 50.49621490985803263 ) ) ;
#44290=CARTESIAN_POINT ( 'NONE',  ( -18.86784385650551954, -6.428312510596451368, 51.20221977374900035 ) ) ;
#44318=ORIENTED_EDGE ( 'NONE', *, *, #6334, .F. ) ;
#44330=CARTESIAN_POINT ( 'NONE',  ( -16.81784385759798894, -6.860780111191487229, 51.02154966934377001 ) ) ;
#44344=FACE_OUTER_BOUND ( 'NONE', #48412, .T. ) ;
#44345=SURFACE_STYLE_FILL_AREA ( #3202 ) ;
#44349=VERTEX_POINT ( 'NONE', #29209 ) ;
#44367=CARTESIAN_POINT ( 'NONE',  ( -13.94909385759799214, -8.112991634885936776, 51.74999426922421719 ) ) ;
#44377=CARTESIAN_POINT ( 'NONE',  ( -13.02466918351366054, -9.790356719747981273, 49.88236859574130477 ) ) ;
#44383=CARTESIAN_POINT ( 'NONE',  ( -13.33034385650551812, -9.794322478646142471, 51.19202720610083901 ) ) ;
#44393=CARTESIAN_POINT ( 'NONE',  ( -12.72364920584387349, -9.064356868646193277, 49.69365772853683438 ) ) ;
#44394=ADVANCED_BREP_SHAPE_REPRESENTATION ( '', ( #32048, #29031 ), #9367 ) ;
#44404=CARTESIAN_POINT ( 'NONE',  ( -15.26784385541304090, -9.357632978295830739, 49.97845033065684106 ) ) ;
#44438=CARTESIAN_POINT ( 'NONE',  ( -22.01784385650551812, -9.790100578890868377, 49.79778022625162492 ) ) ;
#44446=CARTESIAN_POINT ( 'NONE',  ( -17.79909385541294142, -8.105421454601382081, 49.25000573077622334 ) ) ;
#44450=CARTESIAN_POINT ( 'NONE',  ( -19.93659385650551741, -6.915538690918074494, 49.31353937987644542 ) ) ;
#44456=CARTESIAN_POINT ( 'NONE',  ( -13.61159385650551457, -6.922745924619793101, 51.69366785382590024 ) ) ;
#44460=CARTESIAN_POINT ( 'NONE',  ( -20.24909385650551386, -8.104110260919579645, 48.81699501597546487 ) ) ;
#44472=CARTESIAN_POINT ( 'NONE',  ( -19.43034385541290732, -6.857644439847486950, 49.98602051094174215 ) ) ;
#44512=CARTESIAN_POINT ( 'NONE',  ( -13.27409385759798965, -6.859212275519751323, 50.50378509014259265 ) ) ;
#44513=VERTEX_POINT ( 'NONE', #16783 ) ;
#44521=CARTESIAN_POINT ( 'NONE',  ( -17.68659385650551741, -9.302874398569244363, 51.68646062012417985 ) ) ;
#44554=CARTESIAN_POINT ( 'NONE',  ( 18.46573386768564973, 1.644457370994424572, 49.30478444670940519 ) ) ;
#44560=CARTESIAN_POINT ( 'NONE',  ( -16.59284385759799108, -8.630756214087126565, 51.74842643355248129 ) ) ;
#44568=DIRECTION ( 'NONE',  ( 0.000000000000000000, 0.000000000000000000, 1.000000000000000000 ) ) ;
#44574=( NAMED_UNIT ( * ) PLANE_ANGLE_UNIT ( ) SI_UNIT ( $, .RADIAN. ) );
#44581=AXIS2_PLACEMENT_3D ( 'NONE', #46975, #13220, #42081 ) ;
#44600=CARTESIAN_POINT ( 'NONE',  ( -22.55534385650551954, -7.417179338643134834, 52.18511593390279302 ) ) ;
#44633=CARTESIAN_POINT ( 'NONE',  ( -12.77466994470616690, -9.357823239324572384, 50.04128243944182231 ) ) ;
#44634=CARTESIAN_POINT ( 'NONE',  ( 18.51825960693461681, 3.132802701810887935, 50.36638420821972062 ) ) ;
#44643=CARTESIAN_POINT ( 'NONE',  ( -14.03034385541304374, -6.857644439848014528, 49.98602051094140819 ) ) ;
#44660=ORIENTED_EDGE ( 'NONE', *, *, #32280, .T. ) ;
#44666=DIRECTION ( 'NONE',  ( 0.000000000000000000, -0.9999954153791273948, -0.003028072113819838245 ) ) ;
#44681=EDGE_CURVE ( 'NONE', #12464, #3912, #36938, .T. ) ;
#44695=CARTESIAN_POINT ( 'NONE',  ( -16.28034385650551741, -6.424090610841176385, 49.80797279389977916 ) ) ;
#44696=AXIS2_PLACEMENT_3D ( 'NONE', #46670, #43957, #2328 ) ;
#44705=CARTESIAN_POINT ( 'NONE',  ( -15.24284385650551776, -8.811426318492348031, 52.18089403414752070 ) ) ;
#44709=CARTESIAN_POINT ( 'NONE',  ( -14.96159385650551776, -9.295667164867525756, 49.30633214617472504 ) ) ;
#44711=( BOUNDED_CURVE ( )  B_SPLINE_CURVE ( 2, ( #31489, #43314, #12776, #24603, #16205, #24107, #27792, #39601, #9094 ),
 .UNSPECIFIED., .F., .F. ) 
 B_SPLINE_CURVE_WITH_KNOTS ( ( 3, 2, 2, 2, 3 ),
 ( 0.003933667230126343395, 0.004917278694326980212, 0.005900890158527617030, 0.006884501622728254715, 0.007868113086928890665 ),
 .UNSPECIFIED. ) 
 CURVE ( )  GEOMETRIC_REPRESENTATION_ITEM ( )  RATIONAL_B_SPLINE_CURVE ( ( 1.000000000000037526, 0.9238795325112491019, 1.000000000000000000, 0.9238795325112867385, 1.000000000000000000, 0.9238795325112867385, 1.000000000000000000, 0.9238795325090227717, 1.000000000002263967 ) ) 
 REPRESENTATION_ITEM ( '' )  );
#44754=ADVANCED_FACE ( 'NONE', ( #30808 ), #30325, .T. ) ;
#44757=ORIENTED_EDGE ( 'NONE', *, *, #10091, .T. ) ;
#44766=ORIENTED_EDGE ( 'NONE', *, *, #28770, .F. ) ;
#44776=CARTESIAN_POINT ( 'NONE',  ( -19.37409385650551741, -9.792211528768504536, 50.49490371617623197 ) ) ;
#44789=EDGE_LOOP ( 'NONE', ( #5751, #41976, #16167 ) ) ;
#44803=ORIENTED_EDGE ( 'NONE', *, *, #1578, .T. ) ;
#44815=FACE_OUTER_BOUND ( 'NONE', #8347, .T. ) ;
#44817=CARTESIAN_POINT ( 'NONE',  ( -16.93034385759798965, -6.857644439848013640, 49.98602051094139398 ) ) ;
#44832=VECTOR ( 'NONE', #2905, 1000.000000000000114 ) ;
#44854=CARTESIAN_POINT ( 'NONE',  ( -21.20534385650551812, -8.801233750844183135, 48.81488406609782515 ) ) ;
#44863=FACE_OUTER_BOUND ( 'NONE', #6089, .T. ) ;
#44871=CARTESIAN_POINT ( 'NONE',  ( -36.42409385541304800, -9.359200813967566646, 50.49621490985803263 ) ) ;
#44891=CARTESIAN_POINT ( 'NONE',  ( 23.62590614458706639, 1.890747609047893185, 50.53028072113869484 ) ) ;
#44893=DIRECTION ( 'NONE',  ( -3.361323641615342917E-32, -0.9999954153791273948, -0.003028072113822189229 ) ) ;
#44899=CARTESIAN_POINT ( 'NONE',  ( -13.32679657360227488, -8.507250439495127381, 49.03377012338315666 ) ) ;
#44901=CARTESIAN_POINT ( 'NONE',  ( -15.97409385759799072, -6.859212275519751323, 50.50378509014259265 ) ) ;
#44906=ORIENTED_EDGE ( 'NONE', *, *, #10542, .T. ) ;
#44913=AXIS2_PLACEMENT_3D ( 'NONE', #12664, #42226, #614 ) ;
#44922=AXIS2_PLACEMENT_3D ( 'NONE', #37716, #4006, #7956 ) ;
#44932=CARTESIAN_POINT ( 'NONE',  ( -19.03659385650551528, -6.915538690918074494, 49.31353937987644542 ) ) ;
#44935=CARTESIAN_POINT ( 'NONE',  ( -21.31784385759798184, -6.860780111191487229, 51.02154966934377001 ) ) ;
#44947=CARTESIAN_POINT ( 'NONE',  ( -15.26784385650551989, -6.428312510596451368, 51.20221977374900035 ) ) ;
#44949=EDGE_CURVE ( 'NONE', #31311, #3912, #15264, .T. ) ;
#44957=CARTESIAN_POINT ( 'NONE',  ( -15.74909385650551386, -8.104110260919579645, 48.81699501597546487 ) ) ;
#44960=CARTESIAN_POINT ( 'NONE',  ( -36.42409385541304800, -8.109206544743658540, 50.50000000000030553 ) ) ;
#44961=CARTESIAN_POINT ( 'NONE',  ( -16.19909385650551670, -8.114302828567740988, 52.18300498402516041 ) ) ;
#44968=AXIS2_PLACEMENT_3D ( 'NONE', #38722, #819, #1286 ) ;
#44986=CARTESIAN_POINT ( 'NONE',  ( -22.27409385759798965, -6.859212275519751323, 50.50378509014259265 ) ) ;
#44995=CARTESIAN_POINT ( 'NONE',  ( -14.59284385541304907, -8.630756214087124789, 51.74842643355248129 ) ) ;
#45020=TOROIDAL_SURFACE ( 'NONE', #13513, 2.000000000000001776, 1.249999999999999334 ) ;
#45024=CARTESIAN_POINT ( 'NONE',  ( -16.39284385650552167, -7.406986770994973490, 48.81910596585309747 ) ) ;
#45036=EDGE_CURVE ( 'NONE', #12877, #43417, #40355, .T. ) ;
#45040=ORIENTED_EDGE ( 'NONE', *, *, #559, .F. ) ;
#45051=PLANE ( 'NONE',  #2710 ) ;
#45068=CARTESIAN_POINT ( 'NONE',  ( -13.94909385759799214, -8.112991634885936776, 51.74999426922421719 ) ) ;
#45075=( NAMED_UNIT ( * ) PLANE_ANGLE_UNIT ( ) SI_UNIT ( $, .RADIAN. ) );
#45082=DIRECTION ( 'NONE',  ( 0.000000000000000000, -0.9999954153791273948, -0.003028072113819838245 ) ) ;
#45095=ORIENTED_EDGE ( 'NONE', *, *, #19931, .F. ) ;
#45103=CARTESIAN_POINT ( 'NONE',  ( -21.09284385650552096, -7.406986770994972602, 48.81910596585309747 ) ) ;
#45136=DIRECTION ( 'NONE',  ( 1.000000000000000000, -4.164305804376849172E-17, 1.614929280266638808E-16 ) ) ;
#45142=CARTESIAN_POINT ( 'NONE',  ( -13.58034385541304445, -9.360768649639302552, 51.01397948905922419 ) ) ;
#45144=EDGE_CURVE ( 'NONE', #9318, #3630, #36671, .T. ) ;
#45176=CARTESIAN_POINT ( 'NONE',  ( -19.31784385650551528, -9.790100578890868377, 49.79778022625163203 ) ) ;
#45177=TOROIDAL_SURFACE ( 'NONE', #12118, 2.000000000000001776, 1.249999999999999334 ) ;
#45189=CARTESIAN_POINT ( 'NONE',  ( -14.53659385650551705, -6.915538690918075382, 49.31353937987644542 ) ) ;
#45191=DIRECTION ( 'NONE',  ( 0.000000000000000000, -0.9999954153791273948, -0.003028072113819838245 ) ) ;
#45197=CARTESIAN_POINT ( 'NONE',  ( -15.69284385650551172, -7.406986770994973490, 48.81910596585309747 ) ) ;
#45199=CARTESIAN_POINT ( 'NONE',  ( -16.08659385650551599, -9.302874398569244363, 51.68646062012417985 ) ) ;
#45216=B_SPLINE_CURVE_WITH_KNOTS ( 'NONE', 3,
 ( #26291, #33168, #10781, #209 ),
 .UNSPECIFIED., .F., .F.,
 ( 4, 4 ),
 ( 0.000000000000000000, 0.0006999999967409871416 ),
 .UNSPECIFIED. ) ;
#45225=CARTESIAN_POINT ( 'NONE',  ( -19.82409385541304303, -9.359200813967568422, 50.49621490985803263 ) ) ;
#45230=CARTESIAN_POINT ( 'NONE',  ( 18.57132275349405148, 1.979029260061309081, 49.27200896079489922 ) ) ;
#45232=DIRECTION ( 'NONE',  ( 1.000000000000000000, -4.164305804376849172E-17, 1.614929280266638808E-16 ) ) ;
#45255=CARTESIAN_POINT ( 'NONE',  ( -20.16159385541303095, -7.228003583438104229, 51.38655588711987576 ) ) ;
#45257=VERTEX_POINT ( 'NONE', #16670 ) ;
#45261=CARTESIAN_POINT ( 'NONE',  ( -36.42409385541304800, -9.359200813967566646, 50.49621490985803263 ) ) ;
#45263=CARTESIAN_POINT ( 'NONE',  ( -17.18034385650552309, -6.424090610841176385, 49.80797279389977916 ) ) ;
#45267=( BOUNDED_CURVE ( )  B_SPLINE_CURVE ( 2, ( #11262, #3882, #7576 ),
 .UNSPECIFIED., .F., .T. ) 
 B_SPLINE_CURVE_WITH_KNOTS ( ( 3, 3 ),
 ( 0.08654929933941044040, 0.08742189555105450705 ),
 .UNSPECIFIED. ) 
 CURVE ( )  GEOMETRIC_REPRESENTATION_ITEM ( )  RATIONAL_B_SPLINE_CURVE ( ( 0.9999999999999626965, 0.9324910878627294952, 0.9847253504145836445 ) ) 
 REPRESENTATION_ITEM ( '' )  );
#45293=CARTESIAN_POINT ( 'NONE',  ( -18.47409385541327964, -6.859212275519742441, 50.50378509014038997 ) ) ;
#45302=DIRECTION ( 'NONE',  ( -2.231660450020913765E-16, -0.9999954153791275058, -0.003028072113822189229 ) ) ;
#45304=DIRECTION ( 'NONE',  ( 6.374839753205895344E-22, 0.007114381193220357599, -0.9999746924698832418 ) ) ;
#45305=CARTESIAN_POINT ( 'NONE',  ( -12.93659385759799285, -8.995762431863214559, 51.38120296130585274 ) ) ;
#45336=DIRECTION ( 'NONE',  ( -1.616182858256118536E-16, -0.003028072113822188795, 0.9999954153791273948 ) ) ;
#45337=CARTESIAN_POINT ( 'NONE',  ( -19.29284385650551670, -7.406986770994972602, 48.81910596585309747 ) ) ;
#45342=ORIENTED_EDGE ( 'NONE', *, *, #24895, .F. ) ;
#45367=ORIENTED_EDGE ( 'NONE', *, *, #26430, .T. ) ;
#45390=LINE ( 'NONE', #5002, #1397 ) ;
#45407=CARTESIAN_POINT ( 'NONE',  ( -19.26159385650551670, -9.295667164867525756, 49.30633214617472504 ) ) ;
#45425=CARTESIAN_POINT ( 'NONE',  ( -13.63659385650551847, -6.915538690918075382, 49.31353937987644542 ) ) ;
#45435=CARTESIAN_POINT ( 'NONE',  ( -15.86159385650551634, -9.295667164867525756, 49.30633214617472504 ) ) ;
#45439=CARTESIAN_POINT ( 'NONE',  ( -16.70534385650551457, -8.801233750844183135, 48.81488406609782515 ) ) ;
#45478=VECTOR ( 'NONE', #6867, 1000.000000000000114 ) ;
#45488=EDGE_CURVE ( 'NONE', #26444, #43233, #3815, .T. ) ;
#45489=DIRECTION ( 'NONE',  ( 1.000000000000000000, -4.164305804376849172E-17, 1.614929280266638808E-16 ) ) ;
#45494=ORIENTED_EDGE ( 'NONE', *, *, #11172, .F. ) ;
#45495=EDGE_CURVE ( 'NONE', #37274, #16463, #3354, .T. ) ;
#45501=EDGE_CURVE ( 'NONE', #37274, #41647, #35124, .T. ) ;
#45502=CARTESIAN_POINT ( 'NONE',  ( -16.67409385650551812, -9.792211528768504536, 50.49490371617623197 ) ) ;
#45518=EDGE_LOOP ( 'NONE', ( #12352, #47667, #48073, #707 ) ) ;
#45525=CARTESIAN_POINT ( 'NONE',  ( -23.42409385541304090, -9.359200813967568422, 50.49621490985803263 ) ) ;
#45547=CARTESIAN_POINT ( 'NONE',  ( -21.34284385650552096, -8.811426318492348031, 52.18089403414751359 ) ) ;
#45563=ORIENTED_EDGE ( 'NONE', *, *, #27963, .F. ) ;
#45576=CARTESIAN_POINT ( 'NONE',  ( 18.57590614458706924, 2.137037847100829335, 51.75577699556788502 ) ) ;
#45587=ORIENTED_EDGE ( 'NONE', *, *, #9770, .F. ) ;
#45588=CARTESIAN_POINT ( 'NONE',  ( -17.26784385759799179, -9.357632978295821857, 49.97845033065681974 ) ) ;
#45593=CARTESIAN_POINT ( 'NONE',  ( -21.26159385650551314, -9.295667164867525756, 49.30633214617472504 ) ) ;
#45612=CARTESIAN_POINT ( 'NONE',  ( -22.66784385759799392, -9.357632978295830739, 49.97845033065684106 ) ) ;
#45642=DIRECTION ( 'NONE',  ( 1.000000000000000000, -4.164305804376849788E-17, 1.614929280266638808E-16 ) ) ;
#45658=CARTESIAN_POINT ( 'NONE',  ( -17.32409385759798681, -9.359200813967568422, 50.49621490985803263 ) ) ;
#45663=CARTESIAN_POINT ( 'NONE',  ( -21.00534385650551883, -8.801233750844183135, 48.81488406609782515 ) ) ;
#45676=CARTESIAN_POINT ( 'NONE',  ( -14.64909385650551776, -8.104110260919579645, 48.81699501597546487 ) ) ;
#45683=CARTESIAN_POINT ( 'NONE',  ( -23.03034385541304729, -6.857644439848013640, 49.98602051094139398 ) ) ;
#45739=LINE ( 'NONE', #23805, #19445 ) ;
#45753=EDGE_CURVE ( 'NONE', #34525, #17998, #40169, .T. ) ;
#45754=CARTESIAN_POINT ( 'NONE',  ( -14.25534385650552238, -7.417179338643134834, 52.18511593390279302 ) ) ;
#45772=DIRECTION ( 'NONE',  ( -1.000000000000000000, 4.164305804376849172E-17, -1.614929280266638808E-16 ) ) ;
#45793=CARTESIAN_POINT ( 'NONE',  ( -22.29909385650551812, -8.114302828567740988, 52.18300498402516041 ) ) ;
#45804=VERTEX_POINT ( 'NONE', #12121 ) ;
#45809=CARTESIAN_POINT ( 'NONE',  ( -14.93034385541216480, -6.857644439842304429, 49.98602051094714938 ) ) ;
#45826=CARTESIAN_POINT ( 'NONE',  ( -17.49284385650551599, -7.406986770994972602, 48.81910596585309747 ) ) ;
#45834=CARTESIAN_POINT ( 'NONE',  ( -15.71784385541289275, -6.860780111191378872, 51.02154966934401159 ) ) ;
#45844=CARTESIAN_POINT ( 'NONE',  ( -20.81159385759798752, -8.990409506049200417, 49.61344411288074951 ) ) ;
#45882=VERTEX_POINT ( 'NONE', #24179 ) ;
#45892=CARTESIAN_POINT ( 'NONE',  ( -14.98659385650551457, -9.302874398569244363, 51.68646062012417985 ) ) ;
#45898=CARTESIAN_POINT ( 'NONE',  ( -19.37409385541300111, -6.859212275519753099, 50.50378509014300477 ) ) ;
#45916=CARTESIAN_POINT ( 'NONE',  ( -21.45534385541304445, -8.623186033802570094, 49.24843789510466507 ) ) ;
#45936=ADVANCED_FACE ( 'NONE', ( #48027 ), #17964, .F. ) ;
#45948=ORIENTED_EDGE ( 'NONE', *, *, #43023, .F. ) ;
#45962=CARTESIAN_POINT ( 'NONE',  ( -16.08659385759798965, -7.222650657624104298, 49.61879703869476543 ) ) ;
#45970=CARTESIAN_POINT ( 'NONE',  ( -23.11784385650551954, -9.790100578890868377, 49.79778022625162492 ) ) ;
#45979=CARTESIAN_POINT ( 'NONE',  ( -20.75534385650551528, -7.417179338643134834, 52.18511593390279302 ) ) ;
#46020=CARTESIAN_POINT ( 'NONE',  ( 8.575906144586953772, -0.1092432217106413528, 50.52422457691089619 ) ) ;
#46022=CARTESIAN_POINT ( 'NONE',  ( -20.49909385650551741, -8.114302828567740988, 52.18300498402516041 ) ) ;
#46055=CARTESIAN_POINT ( 'NONE',  ( -16.16784385541286895, -9.357632978295828963, 49.97845033065649289 ) ) ;
#46056=CARTESIAN_POINT ( 'NONE',  ( -17.99909385650551741, -8.114302828567740988, 52.18300498402516041 ) ) ;
#46061=VERTEX_POINT ( 'NONE', #15484 ) ;
#46065=CARTESIAN_POINT ( 'NONE',  ( -15.60534385541290980, -7.595227055684650175, 51.75156210489618758 ) ) ;
#46093=ORIENTED_EDGE ( 'NONE', *, *, #41060, .T. ) ;
#46099=CIRCLE ( 'NONE', #48441, 0.2499999999999976408 ) ;
#46120=CARTESIAN_POINT ( 'NONE',  ( -17.71784385759799108, -6.860780111191487229, 51.02154966934377711 ) ) ;
#46125=CARTESIAN_POINT ( 'NONE',  ( -14.76159385650551847, -9.295667164867525756, 49.30633214617472504 ) ) ;
#46135=DIRECTION ( 'NONE',  ( 0.000000000000000000, -0.9999954153791273948, -0.003028072113819838245 ) ) ;
#46139=VECTOR ( 'NONE', #4925, 1000.000000000000000 ) ;
#46150=CARTESIAN_POINT ( 'NONE',  ( -20.38659385541304303, -7.222650657624104298, 49.61879703869476543 ) ) ;
#46166=AXIS2_PLACEMENT_3D ( 'NONE', #30913, #41489, #33851 ) ;
#46188=CARTESIAN_POINT ( 'NONE',  ( -17.77409385759798965, -6.859212275519751323, 50.50378509014259265 ) ) ;
#46206=VECTOR ( 'NONE', #29018, 1000.000000000000000 ) ;
#46209=CARTESIAN_POINT ( 'NONE',  ( -20.98034385650551314, -6.424090610841176385, 49.80797279389977916 ) ) ;
#46216=CARTESIAN_POINT ( 'NONE',  ( -21.93659385650551741, -6.915538690918074494, 49.31353937987644542 ) ) ;
#46235=AXIS2_PLACEMENT_3D ( 'NONE', #3650, #22878, #7367 ) ;
#46242=ORIENTED_EDGE ( 'NONE', *, *, #7401, .T. ) ;
#46257=ORIENTED_EDGE ( 'NONE', *, *, #41490, .F. ) ;
#46261=CARTESIAN_POINT ( 'NONE',  ( -13.10534385759798681, -7.595227055684746986, 51.75156210489594599 ) ) ;
#46277=( BOUNDED_CURVE ( )  B_SPLINE_CURVE ( 2, ( #11976, #41771, #19346, #3595, #15888, #23545, #15641, #23297, #26252 ),
 .UNSPECIFIED., .F., .F. ) 
 B_SPLINE_CURVE_WITH_KNOTS ( ( 3, 2, 2, 2, 3 ),
 ( 0.07868091852197928171, 0.07966438894987652730, 0.08064785937777378677, 0.08163132980567104624, 0.08261480023356829183 ),
 .UNSPECIFIED. ) 
 CURVE ( )  GEOMETRIC_REPRESENTATION_ITEM ( )  RATIONAL_B_SPLINE_CURVE ( ( 0.9999999999999700240, 0.9238795325113167145, 1.000000000000000000, 0.9238795325112867385, 1.000000000000000000, 0.9238795325112867385, 1.000000000000000000, 0.9238795325111349710, 1.000000000000151656 ) ) 
 REPRESENTATION_ITEM ( '' )  );
#46296=EDGE_LOOP ( 'NONE', ( #32499, #32437, #41768, #714 ) ) ;
#46304=CARTESIAN_POINT ( 'NONE',  ( -15.86159385650551634, -9.295667164867525756, 49.30633214617472504 ) ) ;
#46339=CARTESIAN_POINT ( 'NONE',  ( -22.01784385650551812, -9.790100578890868377, 49.79778022625162492 ) ) ;
#46344=PRODUCT_DEFINITION_FORMATION_WITH_SPECIFIED_SOURCE ( 'ANY', '', #42558, .NOT_KNOWN. ) ;
#46346=ORIENTED_EDGE ( 'NONE', *, *, #3068, .T. ) ;
#46348=AXIS2_PLACEMENT_3D ( 'NONE', #25888, #21950, #40902 ) ;
#46373=CARTESIAN_POINT ( 'NONE',  ( -17.99909385759799108, -8.105421454601382081, 49.25000573077640098 ) ) ;
#46374=CARTESIAN_POINT ( 'NONE',  ( -15.49284385650551421, -7.406986770994972602, 48.81910596585309747 ) ) ;
#46396=CARTESIAN_POINT ( 'NONE',  ( -16.53659385759799250, -8.995762431863214559, 51.38120296130585274 ) ) ;
#46400=CARTESIAN_POINT ( 'NONE',  ( -20.10534385541304658, -7.595227055684746986, 51.75156210489594599 ) ) ;
#46418=ORIENTED_EDGE ( 'NONE', *, *, #34795, .F. ) ;
#46429=LINE ( 'NONE', #12684, #36808 ) ;
#46438=CARTESIAN_POINT ( 'NONE',  ( 18.57590614458706924, 1.637040139411203965, 51.75426295951086075 ) ) ;
#46443=VERTEX_POINT ( 'NONE', #10398 ) ;
#46461=CARTESIAN_POINT ( 'NONE',  ( -20.41784385650551314, -9.790100578890868377, 49.79778022625163203 ) ) ;
#46468=CARTESIAN_POINT ( 'NONE',  ( -13.52409385650551599, -6.426201560718813433, 50.50509628382439331 ) ) ;
#46483=ORIENTED_EDGE ( 'NONE', *, *, #1246, .F. ) ;
#46491=DIRECTION ( 'NONE',  ( 0.000000000000000000, -0.9999954153791273948, -0.003028072113819838245 ) ) ;
#46512=DIRECTION ( 'NONE',  ( 0.000000000000000000, 0.9999954153791273948, 0.003028072113819836077 ) ) ;
#46514=CARTESIAN_POINT ( 'NONE',  ( -16.78659385650551883, -9.302874398569244363, 51.68646062012417985 ) ) ;
#46518=EDGE_CURVE ( 'NONE', #20335, #29820, #30652, .T. ) ;
#46556=CARTESIAN_POINT ( 'NONE',  ( -15.58034385650551634, -6.424090610841176385, 49.80797279389978627 ) ) ;
#46569=ORIENTED_EDGE ( 'NONE', *, *, #39883, .T. ) ;
#46575=CARTESIAN_POINT ( 'NONE',  ( -22.61159385759798823, -8.990409506049200417, 49.61344411288074951 ) ) ;
#46597=DIRECTION ( 'NONE',  ( 1.000000000000000000, -4.164305804376849172E-17, 1.614929280266638808E-16 ) ) ;
#46622=CARTESIAN_POINT ( 'NONE',  ( -15.83034385650551634, -9.794322478646142471, 51.19202720610083190 ) ) ;
#46641=CARTESIAN_POINT ( 'NONE',  ( -36.42409385541304800, -6.859212275519750435, 50.50378509014258555 ) ) ;
#46646=CARTESIAN_POINT ( 'NONE',  ( -21.84909385541304161, -8.112991634885936776, 51.74999426922421719 ) ) ;
#46649=EDGE_CURVE ( 'NONE', #16353, #31311, #19762, .T. ) ;
#46670=CARTESIAN_POINT ( 'NONE',  ( 18.57590614458706924, 1.890747609047893185, 50.53028072113869484 ) ) ;
#46686=EDGE_LOOP ( 'NONE', ( #45040, #1231 ) ) ;
#46696=CARTESIAN_POINT ( 'NONE',  ( -22.38659385650551670, -9.302874398569244363, 51.68646062012417985 ) ) ;
#46703=CARTESIAN_POINT ( 'NONE',  ( -21.37409385650551741, -9.792211528768504536, 50.49490371617623197 ) ) ;
#46708=AXIS2_PLACEMENT_3D ( 'NONE', #2025, #17020, #35986 ) ;
#46747=CARTESIAN_POINT ( 'NONE',  ( -17.63034385650551528, -9.794322478646142471, 51.19202720610083901 ) ) ;
#46778=CARTESIAN_POINT ( 'NONE',  ( -14.62409385759799108, -9.359200813967568422, 50.49621490985803263 ) ) ;
#46802=CARTESIAN_POINT ( 'NONE',  ( -17.66159385759798894, -7.228003583438117552, 51.38655588711986155 ) ) ;
#46814=DIRECTION ( 'NONE',  ( 1.616182858256114592E-16, 0.003028072113811714535, -0.9999954153791273948 ) ) ;
#46831=AXIS2_PLACEMENT_3D ( 'NONE', #23502, #19552, #27674 ) ;
#46835=CARTESIAN_POINT ( 'NONE',  ( -36.42409385541304800, -8.109206544743658540, 50.50000000000030553 ) ) ;
#46836=ORIENTED_EDGE ( 'NONE', *, *, #26430, .F. ) ;
#46837=FACE_OUTER_BOUND ( 'NONE', #1652, .T. ) ;
#46839=ADVANCED_FACE ( 'NONE', ( #37823 ), #14904, .T. ) ;
#46853=CARTESIAN_POINT ( 'NONE',  ( -18.11159385759799179, -8.990409506049200417, 49.61344411288074951 ) ) ;
#46854=CARTESIAN_POINT ( 'NONE',  ( -16.78659385650551883, -9.302874398569244363, 51.68646062012417985 ) ) ;
#46874=CARTESIAN_POINT ( 'NONE',  ( -16.81784385759798894, -6.860780111191492558, 51.02154966934378422 ) ) ;
#46879=CARTESIAN_POINT ( 'NONE',  ( -18.69909385541304303, -8.105421454601382081, 49.25000573077640098 ) ) ;
#46926=CARTESIAN_POINT ( 'NONE',  ( -15.18659385759799108, -7.222650657624104298, 49.61879703869476543 ) ) ;
#46930=CARTESIAN_POINT ( 'NONE',  ( -21.82409385650551670, -6.426201560718813433, 50.50509628382439331 ) ) ;
#46934=CARTESIAN_POINT ( 'NONE',  ( -21.26159385650551314, -9.295667164867525756, 49.30633214617472504 ) ) ;
#46975=CARTESIAN_POINT ( 'NONE',  ( 18.57590614458706924, 1.890747609047612077, 50.53028072113853142 ) ) ;
#46977=CARTESIAN_POINT ( 'NONE',  ( -19.59909385650551883, -8.114302828567740988, 52.18300498402516041 ) ) ;
#47011=AXIS2_PLACEMENT_3D ( 'NONE', #30527, #22896, #34682 ) ;
#47018=CARTESIAN_POINT ( 'NONE',  ( -14.23034385650551492, -9.794322478646142471, 51.19202720610083190 ) ) ;
#47019=ORIENTED_EDGE ( 'NONE', *, *, #38149, .F. ) ;
#47040=CARTESIAN_POINT ( 'NONE',  ( -17.38034385759798894, -9.360768649639302552, 51.01397948905922419 ) ) ;
#47049=DIRECTION ( 'NONE',  ( 1.000000000000000000, 1.669677910507523057E-21, 6.493791346278465266E-22 ) ) ;
#47081=FACE_OUTER_BOUND ( 'NONE', #40852, .T. ) ;
#47123=CARTESIAN_POINT ( 'NONE',  ( -16.78659385541304161, -7.222650657624104298, 49.61879703869476543 ) ) ;
#47130=ADVANCED_FACE ( 'NONE', ( #14590 ), #2813, .T. ) ;
#47157=CARTESIAN_POINT ( 'NONE',  ( -13.17364477763805652, -9.395196358873663556, 49.41429196092195042 ) ) ;
#47166=LINE ( 'NONE', #16379, #9800 ) ;
#47167=ORIENTED_EDGE ( 'NONE', *, *, #24780, .F. ) ;
#47177=CARTESIAN_POINT ( 'NONE',  ( -18.11159385650551457, -6.922745924619793101, 51.69366785382590024 ) ) ;
#47179=CIRCLE ( 'NONE', #35361, 2.000000000000000000 ) ;
#47182=CARTESIAN_POINT ( 'NONE',  ( -18.50534385650551883, -8.801233750844183135, 48.81488406609782515 ) ) ;
#47191=AXIS2_PLACEMENT_3D ( 'NONE', #34013, #33764, #18010 ) ;
#47213=DIRECTION ( 'NONE',  ( -1.000000000000000000, 4.164305804376849172E-17, -1.614929280266638808E-16 ) ) ;
#47228=CARTESIAN_POINT ( 'NONE',  ( -19.14909385650551954, -8.104110260919579645, 48.81699501597546487 ) ) ;
#47231=EDGE_CURVE ( 'NONE', #44513, #21655, #11671, .T. ) ;
#47242=DIRECTION ( 'NONE',  ( -1.674255585786183705E-21, 0.9999746924698832418, 0.007114381193220235301 ) ) ;
#47244=CARTESIAN_POINT ( 'NONE',  ( -21.23034385650552025, -9.794322478646142471, 51.19202720610083901 ) ) ;
#47247=CYLINDRICAL_SURFACE ( 'NONE', #7626, 1.249999999999999334 ) ;
#47271=ORIENTED_EDGE ( 'NONE', *, *, #45488, .F. ) ;
#47273=VECTOR ( 'NONE', #17130, 1000.000000000000114 ) ;
#47274=CARTESIAN_POINT ( 'NONE',  ( -13.33034385650551812, -9.794322478646142471, 51.19202720610083190 ) ) ;
#47276=CARTESIAN_POINT ( 'NONE',  ( 23.62590614458706639, 1.890747609047893185, 50.53028072113869484 ) ) ;
#47295=CARTESIAN_POINT ( 'NONE',  ( -20.24909385759799108, -8.112991634885936776, 51.74999426922421719 ) ) ;
#47316=DIRECTION ( 'NONE',  ( -1.000000000000000000, -1.669677910507523057E-21, -6.493791346278465266E-22 ) ) ;
#47355=DIRECTION ( 'NONE',  ( -1.616182858256118536E-16, -0.003028072113822188795, 0.9999954153791273948 ) ) ;
#47374=VERTEX_POINT ( 'NONE', #35758 ) ;
#47375=CARTESIAN_POINT ( 'NONE',  ( -16.28034385541304019, -9.360768649639302552, 51.01397948905922419 ) ) ;
#47383=ORIENTED_EDGE ( 'NONE', *, *, #30701, .F. ) ;
#47411=CARTESIAN_POINT ( 'NONE',  ( 18.57590614458706924, 1.644457370994464540, 49.30478444670960414 ) ) ;
#47422=CARTESIAN_POINT ( 'NONE',  ( -21.82409385759798681, -9.359200813967568422, 50.49621490985803263 ) ) ;
#47426=CARTESIAN_POINT ( 'NONE',  ( -17.83034385650551457, -9.794322478646142471, 51.19202720610083901 ) ) ;
#47430=CARTESIAN_POINT ( 'NONE',  ( -18.95534385650551457, -7.417179338643134834, 52.18511593390279302 ) ) ;
#47438=VERTEX_POINT ( 'NONE', #8962 ) ;
#47460=VERTEX_POINT ( 'NONE', #16564 ) ;
#47475=CARTESIAN_POINT ( 'NONE',  ( -16.73034385650551670, -9.794322478646142471, 51.19202720610083901 ) ) ;
#47480=CARTESIAN_POINT ( 'NONE',  ( 18.57590614458706924, 2.144561833755798563, 49.27104351578925900 ) ) ;
#47486=VECTOR ( 'NONE', #15013, 1000.000000000000114 ) ;
#47491=CARTESIAN_POINT ( 'NONE',  ( -19.54284385650551670, -8.811426318492348031, 52.18089403414751359 ) ) ;
#47506=CIRCLE ( 'NONE', #32567, 2.000000000000001776 ) ;
#47514=CARTESIAN_POINT ( 'NONE',  ( -15.24284385650551599, -8.811426318492348031, 52.18089403414752070 ) ) ;
#47531=CARTESIAN_POINT ( 'NONE',  ( -17.15534385759799108, -8.623186033802570094, 49.24843789510466507 ) ) ;
#47554=CARTESIAN_POINT ( 'NONE',  ( -36.42409385541304800, -6.859212275519750435, 50.50378509014258555 ) ) ;
#47574=( BOUNDED_CURVE ( )  B_SPLINE_CURVE ( 2, ( #31500, #24363, #31254, #28297, #27564, #42829, #28039, #9345, #9102 ),
 .UNSPECIFIED., .F., .F. ) 
 B_SPLINE_CURVE_WITH_KNOTS ( ( 3, 2, 2, 2, 3 ),
 ( 0.08261480023356829183, 0.08359842501002882897, 0.08458204978648936612, 0.08556567456294990326, 0.08654929933941044040 ),
 .UNSPECIFIED. ) 
 CURVE ( )  GEOMETRIC_REPRESENTATION_ITEM ( )  RATIONAL_B_SPLINE_CURVE ( ( 0.9999999999998482325, 0.9238795325114385060, 1.000000000000000000, 0.9238795325112867385, 1.000000000000000000, 0.9238795325112867385, 1.000000000000000000, 0.9238795325112502121, 1.000000000000036415 ) ) 
 REPRESENTATION_ITEM ( '' )  );
#47579=CARTESIAN_POINT ( 'NONE',  ( -13.35534385650551492, -7.417179338643134834, 52.18511593390279302 ) ) ;
#47589=CARTESIAN_POINT ( 'NONE',  ( -13.22466687598806523, -9.790356633151166221, 49.88233999786937289 ) ) ;
#47591=CARTESIAN_POINT ( 'NONE',  ( -18.81159385541304019, -8.990409506049205746, 49.61344411288074951 ) ) ;
#47602=CARTESIAN_POINT ( 'NONE',  ( -21.79284385541302527, -8.630756214087140776, 51.74842643355251681 ) ) ;
#47610=CARTESIAN_POINT ( 'NONE',  ( -17.40534385541304374, -7.595227055684746986, 51.75156210489594599 ) ) ;
#47635=DIRECTION ( 'NONE',  ( 1.000000000000000000, -4.164305804376849172E-17, 1.614929280266638808E-16 ) ) ;
#47638=CARTESIAN_POINT ( 'NONE',  ( -22.86159385650551457, -9.295667164867525756, 49.30633214617472504 ) ) ;
#47656=CARTESIAN_POINT ( 'NONE',  ( -20.08034385650552167, -6.424090610841176385, 49.80797279389977916 ) ) ;
#47659=CARTESIAN_POINT ( 'NONE',  ( -17.15534385650551741, -7.417179338643134834, 52.18511593390279302 ) ) ;
#47667=ORIENTED_EDGE ( 'NONE', *, *, #20252, .T. ) ;
#47677=CARTESIAN_POINT ( 'NONE',  ( -17.12409385541300111, -9.359200813967566646, 50.49621490985766314 ) ) ;
#47679=ORIENTED_EDGE ( 'NONE', *, *, #26674, .F. ) ;
#47688=DIRECTION ( 'NONE',  ( 0.000000000000000000, -0.9999954153791273948, -0.003028072113819838245 ) ) ;
#47708=AXIS2_PLACEMENT_3D ( 'NONE', #11548, #4402, #30770 ) ;
#47718=CARTESIAN_POINT ( 'NONE',  ( -18.75534385650551528, -7.417179338643134834, 52.18511593390279302 ) ) ;
#47727=EDGE_CURVE ( 'NONE', #45804, #16655, #20943, .T. ) ;
#47760=CARTESIAN_POINT ( 'NONE',  ( -14.00534385759799427, -7.595227055684746986, 51.75156210489594599 ) ) ;
#47804=LINE ( 'NONE', #13807, #1881 ) ;
#47840=CARTESIAN_POINT ( 'NONE',  ( -16.67409385541304445, -6.859212275519751323, 50.50378509014259265 ) ) ;
#47842=CARTESIAN_POINT ( 'NONE',  ( -15.58034385759799001, -9.360768649639298999, 51.01397948905923130 ) ) ;
#47849=CARTESIAN_POINT ( 'NONE',  ( -20.13659385759799036, -8.995762431863214559, 51.38120296130585274 ) ) ;
#47882=CARTESIAN_POINT ( 'NONE',  ( 10.57590614458695377, -0.1092432217106413528, 50.52422457691089619 ) ) ;
#47893=VECTOR ( 'NONE', #35628, 1000.000000000000114 ) ;
#47900=CARTESIAN_POINT ( 'NONE',  ( -19.68659385650551386, -9.302874398569244363, 51.68646062012417985 ) ) ;
#47901=PLANE ( 'NONE',  #30756 ) ;
#47902=CARTESIAN_POINT ( 'NONE',  ( -19.06784385650551528, -6.428312510596451368, 51.20221977374900035 ) ) ;
#47935=DIRECTION ( 'NONE',  ( 1.674255585786183705E-21, -0.9999746924698832418, -0.007114381193220357599 ) ) ;
#47944=EDGE_CURVE ( 'NONE', #32426, #15477, #34190, .T. ) ;
#47961=CIRCLE ( 'NONE', #47191, 0.7499999999999998890 ) ;
#47965=CARTESIAN_POINT ( 'NONE',  ( -18.41784385650552736, -9.790100578890868377, 49.79778022625163203 ) ) ;
#47976=DIRECTION ( 'NONE',  ( -1.000000000000000000, -1.669677910507523057E-21, -6.493791346278465266E-22 ) ) ;
#48007=CARTESIAN_POINT ( 'NONE',  ( -13.44284385759799605, -7.587656875400194068, 49.25157356644813689 ) ) ;
#48027=FACE_OUTER_BOUND ( 'NONE', #35478, .T. ) ;
#48035=VERTEX_POINT ( 'NONE', #20884 ) ;
#48054=CARTESIAN_POINT ( 'NONE',  ( -14.36784385650551599, -6.428312510596451368, 51.20221977374900035 ) ) ;
#48064=DIRECTION ( 'NONE',  ( 0.000000000000000000, -0.9999954153791273948, -0.003028072113819838245 ) ) ;
#48073=ORIENTED_EDGE ( 'NONE', *, *, #6552, .F. ) ;
#48080=DIRECTION ( 'NONE',  ( -1.616182858256118783E-16, -0.003028072113822189229, 0.9999954153791275058 ) ) ;
#48085=CARTESIAN_POINT ( 'NONE',  ( -15.94284385541304161, -7.587656875400192291, 49.25157356644813689 ) ) ;
#48100=ORIENTED_EDGE ( 'NONE', *, *, #45501, .T. ) ;
#48115=CARTESIAN_POINT ( 'NONE',  ( -22.18659385650551741, -9.302874398569244363, 51.68646062012417985 ) ) ;
#48139=CARTESIAN_POINT ( 'NONE',  ( -16.70534385650551457, -8.801233750844183135, 48.81488406609782515 ) ) ;
#48143=CARTESIAN_POINT ( 'NONE',  ( -18.16784385650552025, -6.428312510596451368, 51.20221977374900035 ) ) ;
#48168=CARTESIAN_POINT ( 'NONE',  ( 18.46573386768564973, 1.644457370994424572, 49.30478444670940519 ) ) ;
#48201=CARTESIAN_POINT ( 'NONE',  ( -19.59909385650551883, -8.114302828567740988, 52.18300498402516041 ) ) ;
#48204=DIRECTION ( 'NONE',  ( -1.616182858256118536E-16, -0.003028072113822188795, 0.9999954153791273948 ) ) ;
#48237=CARTESIAN_POINT ( 'NONE',  ( -15.91784385759799392, -6.860780111191487229, 51.02154966934377711 ) ) ;
#48251=FACE_OUTER_BOUND ( 'NONE', #20450, .T. ) ;
#48254=CARTESIAN_POINT ( 'NONE',  ( -36.42409385541304800, -8.109206544743658540, 50.50000000000030553 ) ) ;
#48278=CARTESIAN_POINT ( 'NONE',  ( -19.57409385650551670, -9.792211528768504536, 50.49490371617623197 ) ) ;
#48316=CARTESIAN_POINT ( 'NONE',  ( -14.42409385541304090, -9.359200813967568422, 50.49621490985803263 ) ) ;
#48319=DIRECTION ( 'NONE',  ( 1.000000000000000000, -4.164305804376849172E-17, 1.614929280266638808E-16 ) ) ;
#48324=VERTEX_POINT ( 'NONE', #5762 ) ;
#48332=EDGE_CURVE ( 'NONE', #48324, #2071, #6238, .T. ) ;
#48337=CARTESIAN_POINT ( 'NONE',  ( -18.41784385541318159, -6.860780111190566188, 51.02154966934286762 ) ) ;
#48353=ORIENTED_EDGE ( 'NONE', *, *, #37081, .F. ) ;
#48364=CARTESIAN_POINT ( 'NONE',  ( -13.52409385650551599, -6.426201560718813433, 50.50509628382439331 ) ) ;
#48368=CARTESIAN_POINT ( 'NONE',  ( -21.93659385759799108, -8.995762431863214559, 51.38120296130585274 ) ) ;
#48372=CARTESIAN_POINT ( 'NONE',  ( -16.14284385650552167, -8.811426318492348031, 52.18089403414751359 ) ) ;
#48376=CARTESIAN_POINT ( 'NONE',  ( -16.59284385650551741, -7.406986770994973490, 48.81910596585309747 ) ) ;
#48380=CARTESIAN_POINT ( 'NONE',  ( -36.42409385541304800, -8.109206544743658540, 50.50000000000030553 ) ) ;
#48391=EDGE_CURVE ( 'NONE', #3423, #12981, #41175, .T. ) ;
#48408=CARTESIAN_POINT ( 'NONE',  ( 18.46573386768564973, 2.144455078683989768, 49.30629848276630156 ) ) ;
#48412=EDGE_LOOP ( 'NONE', ( #35595, #33061, #33711, #40173 ) ) ;
#48421=CARTESIAN_POINT ( 'NONE',  ( -33.42409385541304800, -9.159201730891741278, 50.49682052428079970 ) ) ;
#48432=ORIENTED_EDGE ( 'NONE', *, *, #21964, .F. ) ;
#48439=CARTESIAN_POINT ( 'NONE',  ( -19.65534385650552451, -7.417179338643134834, 52.18511593390279302 ) ) ;
#48441=AXIS2_PLACEMENT_3D ( 'NONE', #31248, #47242, #39603 ) ;
#48444=CARTESIAN_POINT ( 'NONE',  ( 18.57590614458706924, 1.636933384339416264, 51.78951792648781804 ) ) ;
#48480=CARTESIAN_POINT ( 'NONE',  ( -15.58034385759798823, -9.360768649639302552, 51.01397948905922419 ) ) ;
#48482=CARTESIAN_POINT ( 'NONE',  ( 18.57590614458706924, 1.890747609047893185, 50.53028072113869484 ) ) ;
#48494=EDGE_LOOP ( 'NONE', ( #39669, #8816, #27342, #43835 ) ) ;
#48519=CARTESIAN_POINT ( 'NONE',  ( -20.19284385650551528, -7.406986770994972602, 48.81910596585309747 ) ) ;
#48520=EDGE_CURVE ( 'NONE', #39727, #47438, #42151, .T. ) ;
#48550=CARTESIAN_POINT ( 'NONE',  ( 18.57590614458695200, 3.149984814396855182, 50.78409494584673922 ) ) ;
#48566=CARTESIAN_POINT ( 'NONE',  ( -13.37522125781897664, -8.785794273635769258, 49.36370281465616472 ) ) ;
#48579=CARTESIAN_POINT ( 'NONE',  ( -18.73034385759799036, -6.857644439848019857, 49.98602051094138687 ) ) ;
#48595=FACE_OUTER_BOUND ( 'NONE', #812, .T. ) ;
#48596=CARTESIAN_POINT ( 'NONE',  ( -21.34284385650552096, -8.811426318492348031, 52.18089403414751359 ) ) ;
#48599=CARTESIAN_POINT ( 'NONE',  ( -21.20534385759799179, -7.595227055684746986, 51.75156210489594599 ) ) ;
#48611=EDGE_LOOP ( 'NONE', ( #28986, #326, #43892, #48432 ) ) ;
#48613=CARTESIAN_POINT ( 'NONE',  ( -14.31159385650551741, -6.922745924619793101, 51.69366785382590024 ) ) ;
#48624=CARTESIAN_POINT ( 'NONE',  ( -13.94909385650551492, -8.104110260919579645, 48.81699501597546487 ) ) ;
#48628=CARTESIAN_POINT ( 'NONE',  ( -16.36784385650551954, -6.428312510596451368, 51.20221977374900035 ) ) ;
#48629=ORIENTED_EDGE ( 'NONE', *, *, #20116, .F. ) ;
#48651=CYLINDRICAL_SURFACE ( 'NONE', #1854, 1.249999999999998668 ) ;
#48658=EDGE_LOOP ( 'NONE', ( #27927, #7271, #7577 ) ) ;
#48680=ADVANCED_FACE ( 'NONE', ( #5701 ), #14801, .T. ) ;
#48685=AXIS2_PLACEMENT_3D ( 'NONE', #29017, #34711, #24369 ) ;
#48691=CARTESIAN_POINT ( 'NONE',  ( -14.53659385650551705, -6.915538690918075382, 49.31353937987644542 ) ) ;
#48701=DIRECTION ( 'NONE',  ( 6.374839753205895344E-22, 0.007114381193220357599, -0.9999746924698832418 ) ) ;
#48703=CARTESIAN_POINT ( 'NONE',  ( -35.42409385541304800, -9.359200813967566646, 50.49621490985803263 ) ) ;
ENDSEC;
END-ISO-10303-21;
